ISO-10303-21;
HEADER;
/* Generated by software containing ST-Developer
 * from STEP Tools, Inc. (www.steptools.com) 
 */

FILE_DESCRIPTION(
/* description */ (
'Independent welded steel electronics enclosure with removable sealed 
lid, internal mounting tray and two threaded cable entries. 300 x 220 
mm body. No ingress or electrical safety rating assigned.'),
/* implementation_level */ '2;1');

FILE_NAME(
/* name */ 'Socket head cap screw M6x12.step',
/* time_stamp */ '2026-11-14T09:13:27-08:00',
/* author */ (''),
/* organization */ (''),
/* preprocessor_version */ 'ST-DEVELOPER v20.2',
/* originating_system */ 'Autodesk Translation Framework v15.17.0.0',
/* authorisation */ '');

FILE_SCHEMA (('AUTOMOTIVE_DESIGN { 1 0 10303 214 3 1 1 }'));
ENDSEC;

DATA;
#10=MECHANICAL_DESIGN_GEOMETRIC_PRESENTATION_REPRESENTATION('',(#971),#94412);
#151=CONICAL_SURFACE('',#8632,2.5,0.785398163397449);
#158=B_SPLINE_SURFACE_WITH_KNOTS('',3,3,((#47555,#47556,#47557,#47558,#47559,
#47560,#47561,#47562,#47563,#47564,#47565,#47566,#47567,#47568,#47569,#47570,
#47571,#47572,#47573,#47574,#47575,#47576,#47577,#47578,#47579,#47580,#47581,
#47582,#47583,#47584,#47585,#47586,#47587,#47588,#47589,#47590,#47591,#47592,
#47593,#47594,#47595,#47596,#47597,#47598,#47599,#47600,#47601,#47602,#47603,
#47604,#47605,#47606,#47607,#47608,#47609,#47610,#47611,#47612,#47613,#47614,
#47615,#47616,#47617,#47618,#47619,#47620,#47621,#47622,#47623,#47624,#47625,
#47626,#47627,#47628,#47629,#47630,#47631),(#47632,#47633,#47634,#47635,
#47636,#47637,#47638,#47639,#47640,#47641,#47642,#47643,#47644,#47645,#47646,
#47647,#47648,#47649,#47650,#47651,#47652,#47653,#47654,#47655,#47656,#47657,
#47658,#47659,#47660,#47661,#47662,#47663,#47664,#47665,#47666,#47667,#47668,
#47669,#47670,#47671,#47672,#47673,#47674,#47675,#47676,#47677,#47678,#47679,
#47680,#47681,#47682,#47683,#47684,#47685,#47686,#47687,#47688,#47689,#47690,
#47691,#47692,#47693,#47694,#47695,#47696,#47697,#47698,#47699,#47700,#47701,
#47702,#47703,#47704,#47705,#47706,#47707,#47708),(#47709,#47710,#47711,
#47712,#47713,#47714,#47715,#47716,#47717,#47718,#47719,#47720,#47721,#47722,
#47723,#47724,#47725,#47726,#47727,#47728,#47729,#47730,#47731,#47732,#47733,
#47734,#47735,#47736,#47737,#47738,#47739,#47740,#47741,#47742,#47743,#47744,
#47745,#47746,#47747,#47748,#47749,#47750,#47751,#47752,#47753,#47754,#47755,
#47756,#47757,#47758,#47759,#47760,#47761,#47762,#47763,#47764,#47765,#47766,
#47767,#47768,#47769,#47770,#47771,#47772,#47773,#47774,#47775,#47776,#47777,
#47778,#47779,#47780,#47781,#47782,#47783,#47784,#47785),(#47786,#47787,
#47788,#47789,#47790,#47791,#47792,#47793,#47794,#47795,#47796,#47797,#47798,
#47799,#47800,#47801,#47802,#47803,#47804,#47805,#47806,#47807,#47808,#47809,
#47810,#47811,#47812,#47813,#47814,#47815,#47816,#47817,#47818,#47819,#47820,
#47821,#47822,#47823,#47824,#47825,#47826,#47827,#47828,#47829,#47830,#47831,
#47832,#47833,#47834,#47835,#47836,#47837,#47838,#47839,#47840,#47841,#47842,
#47843,#47844,#47845,#47846,#47847,#47848,#47849,#47850,#47851,#47852,#47853,
#47854,#47855,#47856,#47857,#47858,#47859,#47860,#47861,#47862)),
 .UNSPECIFIED.,.F.,.F.,.F.,(4,4),(4,1,1,1,1,1,1,1,1,1,1,1,1,1,1,1,1,1,1,
1,1,1,1,1,1,1,1,1,1,1,1,1,1,1,1,1,1,1,1,1,1,1,1,1,1,1,1,1,1,1,1,1,1,1,1,
1,1,1,1,1,1,1,1,1,1,1,1,1,1,1,1,1,1,1,4),(-0.000421138100199735,0.0663160893162111),
(11.6145651291772,12.6023632471184,13.5896936464185,14.5770240457187,15.5643544450188,
16.551684844319,17.5390152436191,18.5263456429193,19.5136760422194,20.5010064415196,
21.4883368408197,22.4756672401199,23.46299763942,24.4503280387202,25.4376584380203,
26.4249888373205,27.4123192366206,28.3996496359208,29.3869800352209,30.3743104345211,
31.3616408338212,32.3489712331214,33.3363016324215,34.3236320317217,35.3109624310218,
36.298292830322,37.2856232296221,38.2729536289223,39.2602840282224,40.2476144275226,
41.2349448268227,42.2222752261229,43.209605625423,44.1969360247232,45.1842664240233,
46.1715968233235,47.1589272226236,48.1462576219238,49.1335880212239,50.1209184205241,
51.1082488198242,52.0955792191244,53.0829096184245,54.0702400177247,55.0575704170248,
56.0449008163249,57.0322312156251,58.0195616149252,59.0068920142254,59.9942224135255,
60.9815528128257,61.9688832121258,62.956213611426,63.9435440107261,64.9308744100263,
65.9182048093264,66.9055352086266,67.8928656079267,68.8801960072269,69.867526406527,
70.8548568058272,71.8421872051273,72.8295176044275,73.8168480037276,74.8041784030278,
75.7915088023279,76.7788392016281,77.7661696009282,78.7535000002284,79.7408303995285,
80.7281607988287,81.7154911981288,82.702821597429,83.6901519967291,84.6779516871444),
 .UNSPECIFIED.);
#159=B_SPLINE_SURFACE_WITH_KNOTS('',3,3,((#47951,#47952,#47953,#47954,#47955,
#47956,#47957,#47958,#47959,#47960,#47961,#47962,#47963,#47964,#47965,#47966,
#47967,#47968,#47969,#47970,#47971,#47972,#47973,#47974,#47975,#47976,#47977,
#47978,#47979,#47980,#47981,#47982,#47983,#47984,#47985,#47986,#47987,#47988,
#47989,#47990,#47991,#47992,#47993,#47994,#47995,#47996,#47997,#47998,#47999,
#48000,#48001,#48002,#48003,#48004,#48005,#48006,#48007,#48008,#48009,#48010,
#48011,#48012,#48013,#48014,#48015,#48016,#48017,#48018,#48019,#48020,#48021,
#48022,#48023,#48024,#48025,#48026,#48027,#48028,#48029),(#48030,#48031,
#48032,#48033,#48034,#48035,#48036,#48037,#48038,#48039,#48040,#48041,#48042,
#48043,#48044,#48045,#48046,#48047,#48048,#48049,#48050,#48051,#48052,#48053,
#48054,#48055,#48056,#48057,#48058,#48059,#48060,#48061,#48062,#48063,#48064,
#48065,#48066,#48067,#48068,#48069,#48070,#48071,#48072,#48073,#48074,#48075,
#48076,#48077,#48078,#48079,#48080,#48081,#48082,#48083,#48084,#48085,#48086,
#48087,#48088,#48089,#48090,#48091,#48092,#48093,#48094,#48095,#48096,#48097,
#48098,#48099,#48100,#48101,#48102,#48103,#48104,#48105,#48106,#48107,#48108),
(#48109,#48110,#48111,#48112,#48113,#48114,#48115,#48116,#48117,#48118,
#48119,#48120,#48121,#48122,#48123,#48124,#48125,#48126,#48127,#48128,#48129,
#48130,#48131,#48132,#48133,#48134,#48135,#48136,#48137,#48138,#48139,#48140,
#48141,#48142,#48143,#48144,#48145,#48146,#48147,#48148,#48149,#48150,#48151,
#48152,#48153,#48154,#48155,#48156,#48157,#48158,#48159,#48160,#48161,#48162,
#48163,#48164,#48165,#48166,#48167,#48168,#48169,#48170,#48171,#48172,#48173,
#48174,#48175,#48176,#48177,#48178,#48179,#48180,#48181,#48182,#48183,#48184,
#48185,#48186,#48187),(#48188,#48189,#48190,#48191,#48192,#48193,#48194,
#48195,#48196,#48197,#48198,#48199,#48200,#48201,#48202,#48203,#48204,#48205,
#48206,#48207,#48208,#48209,#48210,#48211,#48212,#48213,#48214,#48215,#48216,
#48217,#48218,#48219,#48220,#48221,#48222,#48223,#48224,#48225,#48226,#48227,
#48228,#48229,#48230,#48231,#48232,#48233,#48234,#48235,#48236,#48237,#48238,
#48239,#48240,#48241,#48242,#48243,#48244,#48245,#48246,#48247,#48248,#48249,
#48250,#48251,#48252,#48253,#48254,#48255,#48256,#48257,#48258,#48259,#48260,
#48261,#48262,#48263,#48264,#48265,#48266)),.UNSPECIFIED.,.F.,.F.,.F.,(4,
4),(4,1,1,1,1,1,1,1,1,1,1,1,1,1,1,1,1,1,1,1,1,1,1,1,1,1,1,1,1,1,1,1,1,1,
1,1,1,1,1,1,1,1,1,1,1,1,1,1,1,1,1,1,1,1,1,1,1,1,1,1,1,1,1,1,1,1,1,1,1,1,
1,1,1,1,1,1,4),(-0.000470199680981362,0.066270318112471),(8.30747755240104,
9.2960444961263,10.2846114398516,11.2731783835768,12.2617453273021,13.2503122710274,
14.2388792147526,15.2274461584779,16.2160131022032,17.2045800459284,18.1931469896537,
19.181713933379,20.1702808771042,21.1588478208295,22.1474147645547,23.13598170828,
24.1245486520053,25.1131155957305,26.1016825394558,27.0902494831811,28.0788164269063,
29.0673833706316,30.0559503143569,31.0445172580821,32.0330842018074,33.0216511455327,
34.0102180892579,34.9987850329832,35.9873519767085,36.9759189204337,37.964485864159,
38.9530528078842,39.9416197516095,40.9301866953348,41.91875363906,42.9073205827853,
43.8958875265106,44.8844544702358,45.8730214139611,46.8615883576864,47.8501553014116,
48.8387222451369,49.8272891888622,50.8158561325874,51.8044230763127,52.792990020038,
53.7815569637632,54.7701239074885,55.7586908512138,56.747257794939,57.7358247386643,
58.7243916823895,59.7129586261148,60.7015255698401,61.6900925135653,62.6786594572906,
63.6672264010159,64.6557933447411,65.6443602884664,66.6329272321917,67.6214941759169,
68.6100611196422,69.5986280633675,70.5871950070927,71.575761950818,72.5643288945433,
73.5528958382685,74.5414627819938,75.530029725719,76.5185966694443,77.5071636131696,
78.4957305568948,79.4842975006201,80.4728644443454,81.4614313880706,82.4499983317959,
83.4390354752022),.UNSPECIFIED.);
#473=B_SPLINE_CURVE_WITH_KNOTS('',3,(#40987,#40988,#40989,#40990,#40991,
#40992,#40993,#40994,#40995,#40996,#40997,#40998,#40999,#41000,#41001,#41002,
#41003,#41004,#41005,#41006,#41007,#41008,#41009,#41010,#41011,#41012,#41013,
#41014,#41015,#41016,#41017,#41018,#41019,#41020,#41021,#41022,#41023,#41024,
#41025,#41026,#41027,#41028,#41029,#41030,#41031,#41032,#41033,#41034,#41035,
#41036,#41037,#41038,#41039,#41040,#41041,#41042,#41043,#41044,#41045,#41046,
#41047,#41048,#41049,#41050,#41051,#41052,#41053,#41054,#41055,#41056,#41057,
#41058,#41059,#41060,#41061,#41062,#41063,#41064,#41065,#41066,#41067,#41068,
#41069,#41070,#41071,#41072,#41073,#41074,#41075,#41076,#41077,#41078,#41079,
#41080,#41081,#41082,#41083,#41084,#41085,#41086,#41087,#41088,#41089,#41090,
#41091,#41092,#41093,#41094,#41095,#41096,#41097,#41098,#41099,#41100,#41101,
#41102,#41103,#41104,#41105,#41106,#41107,#41108,#41109,#41110,#41111,#41112,
#41113,#41114,#41115,#41116,#41117,#41118,#41119,#41120,#41121,#41122,#41123,
#41124,#41125,#41126,#41127,#41128,#41129,#41130,#41131,#41132,#41133,#41134,
#41135,#41136,#41137,#41138,#41139,#41140,#41141,#41142,#41143,#41144,#41145,
#41146),.UNSPECIFIED.,.F.,.F.,(4,3,3,3,3,3,3,3,3,3,3,3,3,3,3,3,3,3,3,3,
3,3,3,3,3,3,3,3,3,3,3,3,3,3,3,3,3,3,3,3,3,3,3,3,3,3,3,3,3,3,3,3,3,4),(10.3765884621259,
10.476062504193,10.575701989116,10.6749488225681,10.7741470583041,10.8733291136227,
10.9732914311112,11.0725937393473,11.1728860614621,11.2731783835768,11.3739734315995,
11.4746293425727,11.5751758025763,11.675662893882,11.7761214170926,11.8765821358525,
11.9771435293855,12.0777554996725,12.1785433307966,12.2617453273021,12.3622418849439,
12.4625938656695,12.5628296768858,12.6630021764353,12.7631426194066,12.8632822204417,
12.963519970855,13.0638064174393,13.1642692822289,13.2503122710274,13.3509733722753,
13.4514920114239,13.5518968662201,13.6522397819783,13.7525517715489,13.8528638085318,
13.9532741952591,14.0537336534519,14.1543681892404,14.2388792147526,14.3395272139403,
14.4400329912056,14.5404254117544,14.6407561617772,14.7410562727562,14.8413567371902,
14.94175611485,15.0422048581083,15.1428292957157,15.2274461584779,15.3337058424558,
15.4397656277915,15.5455522467424,15.6354744060799),.UNSPECIFIED.);
#474=B_SPLINE_CURVE_WITH_KNOTS('',3,(#41149,#41150,#41151,#41152,#41153,
#41154,#41155,#41156,#41157,#41158,#41159,#41160,#41161,#41162,#41163,#41164,
#41165,#41166,#41167,#41168,#41169,#41170,#41171,#41172,#41173,#41174,#41175,
#41176,#41177,#41178,#41179,#41180,#41181,#41182,#41183,#41184,#41185,#41186,
#41187,#41188,#41189,#41190,#41191,#41192,#41193,#41194,#41195,#41196,#41197,
#41198,#41199,#41200,#41201,#41202,#41203,#41204,#41205,#41206,#41207,#41208,
#41209,#41210,#41211,#41212,#41213,#41214,#41215,#41216,#41217,#41218,#41219,
#41220,#41221,#41222,#41223,#41224,#41225,#41226,#41227,#41228,#41229,#41230,
#41231,#41232,#41233,#41234,#41235,#41236,#41237,#41238,#41239,#41240,#41241,
#41242,#41243,#41244,#41245,#41246,#41247,#41248,#41249,#41250,#41251,#41252,
#41253,#41254,#41255,#41256,#41257,#41258,#41259,#41260,#41261,#41262,#41263,
#41264,#41265,#41266,#41267,#41268,#41269,#41270,#41271,#41272),
 .UNSPECIFIED.,.F.,.F.,(4,3,3,3,3,3,3,3,3,3,3,3,3,3,3,3,3,3,3,3,3,3,3,3,
3,3,3,3,3,3,3,3,3,3,3,3,3,3,3,3,3,4),(11.6150328478182,11.7179803808624,
11.8208668123936,11.923743825148,12.0266196557919,12.1295192791407,12.2324676902163,
12.3355662546403,12.4387454167019,12.542116677988,12.6023632471184,12.7020014773053,
12.8014824096587,12.9008317510654,13.000108664494,13.099345507238,13.1985745856525,
13.2978965799461,13.3972630234654,13.4968082248626,13.5896936464185,13.6904969772465,
13.7911583780746,13.8917060070265,13.9921916408381,14.0926460713056,14.1931000507582,
14.2936502312469,14.394248707087,14.4950184335624,14.5770240457187,14.6778335761568,
14.7785042978673,14.8790659281952,14.979568424407,15.0800425628274,15.1805190830172,
15.2810961053189,15.3817238399707,15.4825265426885,15.5643544450188,15.6355313030285),
 .UNSPECIFIED.);
#475=B_SPLINE_CURVE_WITH_KNOTS('',3,(#41278,#41279,#41280,#41281,#41282,
#41283,#41284,#41285,#41286,#41287,#41288,#41289,#41290,#41291,#41292,#41293,
#41294,#41295,#41296,#41297,#41298,#41299,#41300,#41301,#41302,#41303,#41304,
#41305,#41306,#41307,#41308,#41309,#41310,#41311,#41312,#41313,#41314,#41315,
#41316,#41317,#41318,#41319,#41320,#41321,#41322,#41323,#41324,#41325,#41326,
#41327,#41328,#41329,#41330,#41331,#41332,#41333,#41334,#41335,#41336,#41337,
#41338,#41339,#41340,#41341,#41342,#41343,#41344,#41345,#41346,#41347,#41348,
#41349,#41350,#41351,#41352,#41353,#41354,#41355,#41356,#41357,#41358,#41359,
#41360,#41361,#41362,#41363,#41364,#41365,#41366,#41367,#41368,#41369,#41370,
#41371,#41372,#41373,#41374,#41375,#41376,#41377,#41378,#41379,#41380,#41381,
#41382,#41383,#41384,#41385,#41386,#41387,#41388,#41389,#41390,#41391,#41392,
#41393,#41394,#41395,#41396,#41397,#41398,#41399,#41400,#41401,#41402,#41403,
#41404,#41405,#41406,#41407,#41408,#41409,#41410,#41411,#41412,#41413,#41414,
#41415,#41416,#41417,#41418,#41419,#41420,#41421,#41422,#41423,#41424,#41425,
#41426,#41427,#41428,#41429,#41430,#41431,#41432,#41433,#41434,#41435,#41436,
#41437,#41438,#41439,#41440,#41441,#41442,#41443,#41444,#41445,#41446,#41447,
#41448,#41449,#41450,#41451,#41452,#41453,#41454,#41455,#41456,#41457,#41458,
#41459,#41460,#41461),.UNSPECIFIED.,.F.,.F.,(4,2,2,2,2,2,2,2,2,2,2,2,2,
2,2,2,2,2,2,2,2,2,2,2,2,2,2,2,2,2,2,2,2,2,2,2,2,2,2,2,2,2,2,2,2,2,2,2,2,
2,2,2,2,2,2,2,2,2,2,2,2,2,2,2,2,2,2,2,2,2,2,2,2,2,2,2,2,2,2,2,2,2,2,2,2,
2,2,2,2,2,2,4),(-1.47798032885567,-1.43330105002829,-1.42266852888909,-1.41621704688726,
-1.41027667209523,-1.40235146932106,-1.38344869116994,-1.35396756134988,
-1.3091633574122,-1.30211462050817,-1.29824709869633,-1.29489743491915,
-1.29022623422255,-1.27832883877505,-1.25912318836693,-1.19890762103143,
-1.18784880209941,-1.1813102518222,-1.17539478173152,-1.16765724412668,
-1.14999889591902,-1.1235476371968,-1.08192378164802,-1.06959618943341,
-1.06474023502206,-1.06136355574123,-1.05758671301682,-1.05077554176365,
-1.01806758726353,-0.962977770637023,-0.952336094674094,-0.945882670659189,
-0.939942764890604,-0.93202156547281,-0.9131465496835,-0.88373568893161,
-0.838807211319577,-0.831771220103658,-0.827906481021687,-0.82455656142266,
-0.819881135432661,-0.807951240464271,-0.788664305236778,-0.728660656187504,
-0.717559851953047,-0.711013527078348,-0.705101348091632,-0.697383101725452,
-0.679842868340105,-0.653664381381004,-0.612777103535746,-0.599561789074333,
-0.594580702093023,-0.591217259868671,-0.587506562220662,-0.581007157752874,
-0.572743609204568,-0.553375085000751,-0.493566314178682,-0.482423023175997,
-0.475867857016003,-0.469957418340135,-0.462255416920299,-0.444819551716769,
-0.418879940450158,-0.378623921495441,-0.36464191210661,-0.359556448377355,
-0.356173850391463,-0.352497902133166,-0.346169854884155,-0.338192522185705,
-0.31989959428381,-0.257381885070499,-0.246832400336662,-0.2403970147588,
-0.234449302618064,-0.226480297593191,-0.207281769146584,-0.177040028124113,
-0.133597692724678,-0.126444614393014,-0.122554866839668,-0.119213442765481,
-0.114589088484696,-0.102989423542528,-0.0845016583938039,-0.0329586557572508,
-0.0160821659939653,-0.00847164830242694,-0.00409788643911735,-0.000676582743011211),
 .UNSPECIFIED.);
#476=B_SPLINE_CURVE_WITH_KNOTS('',3,(#41462,#41463,#41464,#41465),
 .UNSPECIFIED.,.F.,.F.,(4,4),(15.6354744060799,15.7079632677027),
 .UNSPECIFIED.);
#477=B_SPLINE_CURVE_WITH_KNOTS('',3,(#41467,#41468,#41469,#41470),
 .UNSPECIFIED.,.F.,.F.,(4,4),(15.6355313030285,15.7079632679489),
 .UNSPECIFIED.);
#478=B_SPLINE_CURVE_WITH_KNOTS('',3,(#41471,#41472,#41473,#41474,#41475,
#41476,#41477,#41478,#41479,#41480,#41481,#41482,#41483,#41484,#41485,#41486,
#41487,#41488,#41489,#41490,#41491,#41492,#41493,#41494,#41495,#41496,#41497,
#41498,#41499,#41500,#41501,#41502,#41503,#41504,#41505,#41506,#41507,#41508,
#41509,#41510,#41511,#41512,#41513,#41514,#41515,#41516,#41517,#41518,#41519,
#41520,#41521,#41522,#41523,#41524,#41525,#41526,#41527,#41528,#41529,#41530,
#41531,#41532,#41533,#41534,#41535,#41536,#41537,#41538,#41539,#41540,#41541,
#41542,#41543,#41544,#41545,#41546,#41547,#41548,#41549,#41550,#41551,#41552,
#41553,#41554,#41555,#41556,#41557,#41558,#41559,#41560,#41561,#41562,#41563,
#41564,#41565,#41566,#41567,#41568,#41569,#41570,#41571,#41572,#41573,#41574,
#41575,#41576,#41577,#41578,#41579,#41580,#41581,#41582,#41583,#41584,#41585,
#41586,#41587,#41588,#41589,#41590,#41591,#41592,#41593,#41594,#41595,#41596,
#41597,#41598,#41599,#41600,#41601,#41602,#41603,#41604,#41605,#41606,#41607,
#41608,#41609,#41610,#41611,#41612,#41613,#41614,#41615,#41616,#41617,#41618,
#41619,#41620,#41621,#41622,#41623,#41624,#41625,#41626,#41627,#41628,#41629,
#41630,#41631,#41632,#41633,#41634,#41635,#41636,#41637,#41638,#41639,#41640,
#41641,#41642,#41643,#41644,#41645,#41646),.UNSPECIFIED.,.F.,.F.,(4,2,2,
2,2,2,2,2,2,2,2,2,2,2,2,2,2,2,2,2,2,2,2,2,2,2,2,2,2,2,2,2,2,2,2,2,2,2,2,
2,2,2,2,2,2,2,2,2,2,2,2,2,2,2,2,2,2,2,2,2,2,2,2,2,2,2,2,2,2,2,2,2,2,2,2,
2,2,2,2,2,2,2,2,2,2,2,2,4),(-2.98914895289037,-2.92873298419057,-2.91557163843783,
-2.90851700668525,-2.90251005083803,-2.89513756844254,-2.88357783616708,
-2.82436448753581,-2.80641267797751,-2.79499011906609,-2.79032938790222,
-2.78690735675631,-2.78283376851302,-2.77514768041812,-2.74274361420564,
-2.712729735914,-2.68565752927767,-2.67659514414619,-2.6703109293323,-2.66390874398197,
-2.65422566793543,-2.62169798390984,-2.58559988663249,-2.56308780984347,
-2.55724497620969,-2.55359428444409,-2.55037600554499,-2.54488793851854,
-2.52828106190174,-2.47617012571485,-2.45094016063448,-2.44207653621755,
-2.43583961700925,-2.42941077081661,-2.41953799437294,-2.38097245010046,
-2.35217056537171,-2.32842811017426,-2.32252209973905,-2.31886943808619,
-2.31567471695582,-2.31028656663783,-2.29455324852778,-2.25152087325597,
-2.22467561339994,-2.21131814894629,-2.20419919317128,-2.19815544289559,
-2.19075783572952,-2.17590297969063,-2.12392107427581,-2.1036799968007,
-2.09131052756701,-2.08649194610422,-2.08304040155196,-2.07903831159411,
-2.07168601841267,-2.0302764061936,-1.9991916879254,-1.9857341978946,-1.97473076940944,
-1.96807318546886,-1.96194506926809,-1.95390177747934,-1.93962735355907,
-1.88876658204379,-1.86882473320778,-1.85657172497545,-1.8517651228926,
-1.8483119790225,-1.84429763895165,-1.83688783626045,-1.78557122892761,
-1.76081295925951,-1.74382015979252,-1.73605165035796,-1.72997662243179,
-1.72311212880431,-1.71138977724004,-1.64550743179752,-1.62384772720852,
-1.61807613133524,-1.61445116995907,-1.61123326167678,-1.6057250927514,
-1.5888725507394,-1.52239112292902,-1.5122482337056),.UNSPECIFIED.);
#479=B_SPLINE_CURVE_WITH_KNOTS('',3,(#41651,#41652,#41653,#41654,#41655,
#41656,#41657,#41658,#41659,#41660,#41661,#41662,#41663,#41664,#41665,#41666,
#41667,#41668,#41669,#41670,#41671,#41672,#41673,#41674,#41675,#41676,#41677,
#41678,#41679,#41680,#41681,#41682,#41683,#41684,#41685,#41686,#41687,#41688,
#41689,#41690,#41691,#41692,#41693,#41694,#41695,#41696,#41697,#41698,#41699,
#41700,#41701,#41702,#41703,#41704,#41705,#41706,#41707,#41708,#41709,#41710,
#41711,#41712,#41713,#41714,#41715,#41716,#41717,#41718,#41719,#41720,#41721,
#41722,#41723,#41724,#41725,#41726,#41727,#41728,#41729,#41730,#41731,#41732,
#41733,#41734,#41735,#41736,#41737,#41738,#41739,#41740,#41741,#41742,#41743,
#41744,#41745,#41746,#41747,#41748,#41749,#41750,#41751,#41752,#41753,#41754,
#41755,#41756,#41757,#41758,#41759,#41760,#41761,#41762,#41763,#41764,#41765,
#41766,#41767,#41768,#41769,#41770,#41771,#41772,#41773,#41774,#41775,#41776,
#41777,#41778,#41779,#41780,#41781,#41782,#41783,#41784,#41785,#41786,#41787,
#41788,#41789,#41790,#41791,#41792,#41793,#41794,#41795,#41796,#41797,#41798,
#41799,#41800,#41801,#41802,#41803,#41804,#41805,#41806,#41807,#41808,#41809,
#41810,#41811,#41812,#41813,#41814,#41815,#41816,#41817,#41818,#41819,#41820,
#41821,#41822,#41823,#41824,#41825,#41826,#41827,#41828,#41829,#41830,#41831,
#41832,#41833,#41834,#41835,#41836,#41837,#41838,#41839,#41840,#41841,#41842,
#41843,#41844),.UNSPECIFIED.,.F.,.F.,(4,2,2,2,2,2,2,2,2,2,2,2,2,2,2,2,2,
2,2,2,2,2,2,2,2,2,2,2,2,2,2,2,2,2,2,2,2,2,2,2,2,2,2,2,2,2,2,2,2,2,2,2,2,
2,2,2,2,2,2,2,2,2,2,2,2,2,2,2,2,2,2,2,2,2,2,2,2,2,2,2,2,2,2,2,2,2,2,2,2,
2,2,2,2,2,2,2,4),(-2.97274808995521,-2.9640236472047,-2.95348427225043,
-2.94901602775192,-2.94571010502777,-2.9423799428634,-2.93840614716746,
-2.93085861552232,-2.90087241224702,-2.86180870102341,-2.84018005884101,
-2.83159264178222,-2.82554402332727,-2.8193129722081,-2.80977031046813,
-2.77679441215418,-2.74252183651167,-2.7258834978171,-2.71507553790633,
-2.71056794796063,-2.70723687863763,-2.70326996368559,-2.69552335076595,
-2.66352120051562,-2.62676763795099,-2.61165712902711,-2.59972363568552,
-2.59300760017189,-2.58712348657146,-2.57969079658784,-2.5675960404565,
-2.51387425148791,-2.49304943582902,-2.48441129141955,-2.4776896882762,
-2.47393129906078,-2.47054696725103,-2.46564674441967,-2.45304579248103,
-2.4066702531642,-2.38334206226959,-2.36708320757952,-2.35957023449622,
-2.35367846775746,-2.34701275133626,-2.33563756635945,-2.29396326529225,
-2.26232848687584,-2.24627499211812,-2.24108783663789,-2.23765216846806,
-2.23399976311814,-2.22777900848114,-2.19251209728969,-2.15620489824737,
-2.13409952585812,-2.12574258082685,-2.11973381380674,-2.11343723379616,
-2.10356944174534,-2.06337947624062,-2.02930305555997,-2.01146750304277,
-2.0061040285687,-2.00263368022068,-1.9994783002486,-1.99396391983363,-1.97599426442391,
-1.91006906850456,-1.89568388821476,-1.88849842755302,-1.88319914011093,
-1.8765164238814,-1.86505879860271,-1.82657694156904,-1.79264819722716,
-1.77599453154855,-1.77074576917699,-1.76729847897115,-1.76366583687039,
-1.75753641811003,-1.72775772653704,-1.68662224085544,-1.66388369827819,
-1.65545058559946,-1.64942935756776,-1.64315651564052,-1.63340388715119,
-1.59433835042962,-1.55815798263997,-1.54095617863748,-1.53565317271213,
-1.53219522158039,-1.52857876487849,-1.52252452838479,-1.49551164359983,
-1.47798032885567),.UNSPECIFIED.);
#480=B_SPLINE_CURVE_WITH_KNOTS('',3,(#41845,#41846,#41847,#41848,#41849,
#41850,#41851,#41852,#41853,#41854,#41855,#41856,#41857,#41858,#41859,#41860,
#41861,#41862,#41863,#41864,#41865,#41866,#41867,#41868,#41869,#41870,#41871,
#41872,#41873,#41874,#41875,#41876,#41877,#41878,#41879,#41880,#41881,#41882,
#41883,#41884,#41885,#41886,#41887,#41888,#41889,#41890,#41891,#41892,#41893,
#41894,#41895,#41896,#41897,#41898,#41899,#41900,#41901,#41902,#41903,#41904,
#41905,#41906,#41907,#41908,#41909,#41910,#41911,#41912,#41913,#41914,#41915,
#41916,#41917,#41918,#41919,#41920,#41921,#41922,#41923,#41924,#41925,#41926,
#41927,#41928,#41929,#41930,#41931,#41932,#41933,#41934,#41935,#41936,#41937,
#41938,#41939,#41940,#41941,#41942,#41943,#41944,#41945,#41946,#41947,#41948,
#41949,#41950,#41951,#41952,#41953,#41954,#41955,#41956,#41957,#41958,#41959,
#41960,#41961,#41962,#41963,#41964,#41965,#41966,#41967,#41968,#41969,#41970,
#41971,#41972,#41973,#41974,#41975,#41976,#41977,#41978,#41979,#41980,#41981,
#41982,#41983,#41984,#41985,#41986,#41987,#41988,#41989,#41990,#41991,#41992,
#41993,#41994,#41995,#41996,#41997,#41998,#41999,#42000,#42001,#42002,#42003,
#42004,#42005,#42006,#42007,#42008,#42009,#42010,#42011,#42012,#42013,#42014,
#42015,#42016,#42017,#42018,#42019,#42020,#42021,#42022,#42023,#42024,#42025,
#42026),.UNSPECIFIED.,.F.,.F.,(4,2,2,2,2,2,2,2,2,2,2,2,2,2,2,2,2,2,2,2,
2,2,2,2,2,2,2,2,2,2,2,2,2,2,2,2,2,2,2,2,2,2,2,2,2,2,2,2,2,2,2,2,2,2,2,2,
2,2,2,2,2,2,2,2,2,2,2,2,2,2,2,2,2,2,2,2,2,2,2,2,2,2,2,2,2,2,2,2,2,2,4),
(-1.5122482337056,-1.50772542513188,-1.50035846230784,-1.49489987394033,
-1.48797405338146,-1.47562536103928,-1.45991055432274,-1.41752610048913,
-1.38983746359247,-1.38365368734325,-1.37994094669798,-1.37635789481356,
-1.37078982936435,-1.35173470670003,-1.3067976258637,-1.27831789422885,
-1.26884624678052,-1.26313112407836,-1.25693462816383,-1.24829850699851,
-1.22510288341081,-1.18252099732315,-1.15508616577586,-1.14891064752082,
-1.14519909407883,-1.14161431561776,-1.13603811019637,-1.11688852049896,
-1.07140854713519,-1.04346491180145,-1.03404764333776,-1.02834218426725,
-1.02213864785108,-1.01345943662038,-0.989893809829303,-0.945832431633345,
-0.9201913339134,-0.914091173173159,-0.910395957622099,-0.906798821014502,
-0.901161874026297,-0.88128153350777,-0.831217203568471,-0.807539369798536,
-0.798640523854862,-0.792460683310774,-0.786057130955777,-0.776305747126482,
-0.739022113301222,-0.687985932876878,-0.680518493001488,-0.676492020185392,
-0.67304305770072,-0.668261655524246,-0.656173077550299,-0.636642848035639,
-0.577749184812847,-0.566384531927911,-0.559655172273088,-0.553550988884097,
-0.545530950763918,-0.526938396743792,-0.498439726677072,-0.452308710537718,
-0.44526763531528,-0.441373227883966,-0.437886630791347,-0.432842424602708,
-0.41880488843608,-0.394015180370477,-0.342646677984083,-0.331454568756659,
-0.324760053346076,-0.318646059672227,-0.31055172393684,-0.29146048132108,
-0.261706745715902,-0.217916538552625,-0.210730749320117,-0.206764377280321,
-0.20330067367785,-0.198408320850292,-0.185532114874522,-0.163984773395862,
-0.106200338112068,-0.0958600959611263,-0.0893383548318248,-0.083157605038447,
-0.0746178047795694,-0.0522232617175424,-0.0181623686306291),
 .UNSPECIFIED.);
#481=B_SPLINE_CURVE_WITH_KNOTS('',3,(#42032,#42033,#42034,#42035,#42036,
#42037,#42038,#42039,#42040,#42041,#42042,#42043,#42044,#42045,#42046,#42047,
#42048,#42049,#42050,#42051,#42052,#42053,#42054,#42055,#42056,#42057,#42058,
#42059,#42060,#42061,#42062,#42063,#42064,#42065,#42066,#42067,#42068,#42069,
#42070,#42071,#42072,#42073,#42074,#42075,#42076,#42077,#42078,#42079,#42080,
#42081,#42082,#42083,#42084,#42085,#42086,#42087,#42088,#42089,#42090,#42091,
#42092,#42093,#42094,#42095,#42096,#42097,#42098,#42099,#42100,#42101,#42102,
#42103,#42104,#42105,#42106,#42107,#42108,#42109,#42110,#42111,#42112,#42113,
#42114,#42115,#42116,#42117,#42118,#42119,#42120,#42121,#42122,#42123,#42124,
#42125,#42126,#42127,#42128,#42129,#42130,#42131,#42132,#42133,#42134,#42135,
#42136,#42137,#42138,#42139,#42140,#42141,#42142,#42143,#42144,#42145,#42146,
#42147,#42148,#42149,#42150,#42151,#42152,#42153,#42154,#42155,#42156,#42157,
#42158,#42159,#42160,#42161,#42162,#42163,#42164,#42165,#42166,#42167,#42168,
#42169,#42170,#42171,#42172,#42173,#42174,#42175,#42176,#42177,#42178,#42179,
#42180,#42181,#42182,#42183,#42184,#42185,#42186,#42187,#42188,#42189,#42190,
#42191,#42192,#42193,#42194,#42195,#42196,#42197,#42198,#42199,#42200,#42201,
#42202,#42203,#42204,#42205,#42206,#42207,#42208,#42209),.UNSPECIFIED.,
 .F.,.F.,(4,2,2,2,2,2,2,2,2,2,2,2,2,2,2,2,2,2,2,2,2,2,2,2,2,2,2,2,2,2,2,
2,2,2,2,2,2,2,2,2,2,2,2,2,2,2,2,2,2,2,2,2,2,2,2,2,2,2,2,2,2,2,2,2,2,2,2,
2,2,2,2,2,2,2,2,2,2,2,2,2,2,2,2,2,2,2,2,2,4),(-1.4777460824475,-1.47573978689171,
-1.46618077890607,-1.42946098154568,-1.37702591149363,-1.36982749058004,
-1.36592864696727,-1.36258738617596,-1.35797547138166,-1.34647594486204,
-1.32823061002263,-1.26670142863415,-1.25556300132005,-1.24900975001786,
-1.24310044149456,-1.23539904509031,-1.21796048791087,-1.19201282697499,
-1.1517362206291,-1.13778908053883,-1.13270933081852,-1.12932894721775,
-1.12565532017276,-1.11932860968657,-1.08139798378654,-1.03185411698654,
-1.0205978945993,-1.0140209026593,-1.00811727050498,-1.00046196495041,-0.983312743943603,
-0.958022872794609,-0.907373812178612,-0.899863490423314,-0.895898763938141,
-0.892569323425368,-0.88806376458844,-0.877259378847734,-0.86062674071379,
-0.826350549151681,-0.793464788560218,-0.7839315132419,-0.777704518404759,
-0.771658292452442,-0.763071631932232,-0.738978265771288,-0.692305104954863,
-0.669320532771877,-0.663427440968239,-0.659846413083829,-0.656364513410194,
-0.650938634201847,-0.632386345995213,-0.589795975442162,-0.558250512578107,
-0.548786776467311,-0.542573453910063,-0.536517178466571,-0.527875507423322,
-0.503280280406226,-0.454232936447933,-0.433908046004194,-0.428186881703376,
-0.424642617772866,-0.421128728299778,-0.415550004391565,-0.395128302092214,
-0.340541670586779,-0.320493766122117,-0.312207870985494,-0.306213243181289,
-0.299898698101786,-0.28993175752408,-0.243536204030134,-0.201674328221789,
-0.194434036500395,-0.190526073901684,-0.187522265175158,-0.183144207166153,
-0.173130113941981,-0.158231371441998,-0.102854711434871,-0.0847466893602929,
-0.0775112901881956,-0.0715235085403913,-0.06531131571646,-0.0558539703595871,
-0.041686806976749,-0.000673344736818981),.UNSPECIFIED.);
#482=B_SPLINE_CURVE_WITH_KNOTS('',3,(#42210,#42211,#42212,#42213),
 .UNSPECIFIED.,.F.,.F.,(4,4),(-2.98989863407752,-2.97274808995521),
 .UNSPECIFIED.);
#483=B_SPLINE_CURVE_WITH_KNOTS('',3,(#42215,#42216,#42217,#42218),
 .UNSPECIFIED.,.F.,.F.,(4,4),(-0.0181623686306291,-0.000670468894133524),
 .UNSPECIFIED.);
#484=B_SPLINE_CURVE_WITH_KNOTS('',3,(#42219,#42220,#42221,#42222,#42223,
#42224,#42225,#42226,#42227,#42228,#42229,#42230,#42231,#42232,#42233,#42234,
#42235,#42236,#42237,#42238,#42239,#42240,#42241,#42242,#42243,#42244,#42245,
#42246,#42247,#42248,#42249,#42250,#42251,#42252,#42253,#42254,#42255,#42256,
#42257,#42258,#42259,#42260,#42261,#42262,#42263,#42264,#42265,#42266,#42267,
#42268,#42269,#42270,#42271,#42272,#42273,#42274,#42275,#42276,#42277,#42278,
#42279,#42280,#42281,#42282,#42283,#42284,#42285,#42286,#42287,#42288,#42289,
#42290,#42291,#42292,#42293,#42294,#42295,#42296,#42297,#42298,#42299,#42300,
#42301,#42302,#42303,#42304,#42305,#42306,#42307,#42308,#42309,#42310,#42311,
#42312,#42313,#42314,#42315,#42316,#42317,#42318,#42319,#42320,#42321,#42322,
#42323,#42324,#42325,#42326,#42327,#42328,#42329,#42330,#42331,#42332,#42333,
#42334,#42335,#42336,#42337,#42338,#42339,#42340,#42341,#42342,#42343,#42344,
#42345,#42346,#42347,#42348,#42349,#42350,#42351,#42352,#42353,#42354,#42355,
#42356,#42357,#42358,#42359,#42360,#42361,#42362,#42363,#42364,#42365,#42366,
#42367,#42368,#42369,#42370,#42371,#42372,#42373,#42374,#42375,#42376,#42377,
#42378,#42379,#42380,#42381,#42382,#42383,#42384,#42385,#42386,#42387,#42388,
#42389,#42390,#42391,#42392,#42393,#42394,#42395,#42396,#42397,#42398,#42399,
#42400,#42401,#42402,#42403,#42404),.UNSPECIFIED.,.F.,.F.,(4,2,2,2,2,2,
2,2,2,2,2,2,2,2,2,2,2,2,2,2,2,2,2,2,2,2,2,2,2,2,2,2,2,2,2,2,2,2,2,2,2,2,
2,2,2,2,2,2,2,2,2,2,2,2,2,2,2,2,2,2,2,2,2,2,2,2,2,2,2,2,2,2,2,2,2,2,2,2,
2,2,2,2,2,2,2,2,2,2,2,2,2,2,4),(-2.98908487091722,-2.96886855829473,-2.96450205707518,
-2.96117612391201,-2.95775733401322,-2.95342242295158,-2.94410224265239,
-2.90147405121839,-2.86461822457242,-2.85165208120246,-2.84460439146685,
-2.83855011127857,-2.83104843045247,-2.81912520641453,-2.76073307004609,
-2.74293070077161,-2.73156074721739,-2.72688652967381,-2.72348020146249,
-2.71940239891614,-2.71169066217723,-2.68008656356456,-2.64341671589513,
-2.62111565549577,-2.61258814368928,-2.60640976797286,-2.59988468845634,
-2.58952636135325,-2.53182902609499,-2.51021838400767,-2.50132651405739,
-2.49441955208431,-2.49055312559073,-2.48709534551545,-2.48201703008245,
-2.46872894727117,-2.41305544126296,-2.38723337185768,-2.37830875503061,
-2.37206189959498,-2.36565047559016,-2.35586078008269,-2.31992548948552,
-2.27044235473586,-2.26109308774307,-2.25675260348975,-2.25333336365217,
-2.24896794365217,-2.23947783105127,-2.19528354486361,-2.1680635499048,
-2.15557724201101,-2.14517925025786,-2.13864572125017,-2.13247051390237,
-2.12396557467725,-2.10341298706472,-2.04979098138973,-2.02941193917131,
-2.0237344600582,-2.02012859466126,-2.01689392977582,-2.01129707047237,
-1.99348520446533,-1.92698093979589,-1.91303898508549,-1.90580451154975,
-1.89975675013751,-1.8924688277342,-1.87868572678518,-1.82567481587226,
-1.80518343015311,-1.79657086485733,-1.78982837142721,-1.78599635911805,
-1.78252406094718,-1.77819267307977,-1.76701723046152,-1.72460308979061,
-1.69802649616672,-1.68023268405016,-1.67233507652708,-1.66624522771497,
-1.65945214727735,-1.64777405605952,-1.59192109787737,-1.57073892565109,
-1.55800167319201,-1.55312817927367,-1.54966703105588,-1.54569058373772,
-1.53845859496727,-1.51233049812282),.UNSPECIFIED.);
#485=B_SPLINE_CURVE_WITH_KNOTS('',3,(#42409,#42410,#42411,#42412,#42413,
#42414,#42415,#42416,#42417,#42418,#42419,#42420,#42421,#42422,#42423,#42424,
#42425,#42426,#42427,#42428,#42429,#42430,#42431,#42432,#42433,#42434,#42435,
#42436,#42437,#42438,#42439,#42440,#42441,#42442,#42443,#42444,#42445,#42446,
#42447,#42448,#42449,#42450,#42451,#42452,#42453,#42454,#42455,#42456,#42457,
#42458,#42459,#42460,#42461,#42462,#42463,#42464,#42465,#42466,#42467,#42468,
#42469,#42470,#42471,#42472,#42473,#42474,#42475,#42476,#42477,#42478,#42479,
#42480,#42481,#42482,#42483,#42484,#42485,#42486,#42487,#42488,#42489,#42490,
#42491,#42492,#42493,#42494,#42495,#42496,#42497,#42498,#42499,#42500,#42501,
#42502,#42503,#42504,#42505,#42506,#42507,#42508,#42509,#42510,#42511,#42512,
#42513,#42514,#42515,#42516,#42517,#42518,#42519,#42520,#42521,#42522,#42523,
#42524,#42525,#42526,#42527,#42528,#42529,#42530,#42531,#42532,#42533,#42534,
#42535,#42536,#42537,#42538,#42539,#42540,#42541,#42542,#42543,#42544,#42545,
#42546,#42547,#42548,#42549,#42550,#42551,#42552,#42553,#42554,#42555,#42556,
#42557,#42558,#42559,#42560,#42561,#42562,#42563,#42564,#42565,#42566,#42567,
#42568,#42569,#42570,#42571,#42572,#42573,#42574,#42575,#42576,#42577,#42578,
#42579,#42580,#42581,#42582,#42583,#42584,#42585,#42586,#42587,#42588,#42589,
#42590),.UNSPECIFIED.,.F.,.F.,(4,2,2,2,2,2,2,2,2,2,2,2,2,2,2,2,2,2,2,2,
2,2,2,2,2,2,2,2,2,2,2,2,2,2,2,2,2,2,2,2,2,2,2,2,2,2,2,2,2,2,2,2,2,2,2,2,
2,2,2,2,2,2,2,2,2,2,2,2,2,2,2,2,2,2,2,2,2,2,2,2,2,2,2,2,2,2,2,2,2,2,4),
(-2.97165059380248,-2.92985561646699,-2.90664980664673,-2.89816571205665,
-2.89213883549381,-2.88662716188596,-2.87761848441644,-2.85112920410734,
-2.79237798509216,-2.7817480326958,-2.77727045252068,-2.7739441805029,-2.76996172162346,
-2.76236468760279,-2.72985809350361,-2.69271539810152,-2.67113811733543,
-2.66285133733886,-2.65685765252881,-2.65130315593011,-2.64205070898714,
-2.61330081692205,-2.56801167805497,-2.54896851637548,-2.5435009653401,
-2.54001099237372,-2.53644152592569,-2.53060022117996,-2.50845534342929,
-2.46109680664917,-2.436860401744,-2.42825947219759,-2.42221157573852,-2.41598988703573,
-2.40647909790062,-2.37406135408483,-2.33942454343257,-2.3226741719821,
-2.31181911125481,-2.30730609971663,-2.3040060171452,-2.30006118022646,
-2.29264344181399,-2.24150833419156,-2.21646408953766,-2.1994241218767,
-2.19178718319025,-2.18588642470474,-2.17930113546562,-2.16800095288249,
-2.11902482674775,-2.08046920919528,-2.07419846877499,-2.07053710606172,
-2.06715096370826,-2.06203779157594,-2.04782997660692,-2.00779869866169,
-1.98194956430747,-1.96455377186536,-1.95685984188138,-1.950952030794,-1.94439617581489,
-1.93324256581522,-1.8735005604764,-1.85410511947647,-1.8421333884692,-1.83745275452307,
-1.8341031134667,-1.83024354880006,-1.82322685980951,-1.77819742072212,
-1.74889265130891,-1.73006196307184,-1.72214971052551,-1.71621323791485,
-1.70976041457717,-1.69911243766783,-1.63698185553424,-1.61850874363784,
-1.60691494836906,-1.60228920226273,-1.5989464888609,-1.59505609596995,
-1.58789650402166,-1.54467737183832,-1.51435025689767,-1.49512204388784,
-1.48794496120307,-1.48197166787465,-1.4777460824475),.UNSPECIFIED.);
#486=B_SPLINE_CURVE_WITH_KNOTS('',3,(#42591,#42592,#42593,#42594,#42595,
#42596,#42597,#42598,#42599,#42600,#42601,#42602,#42603,#42604,#42605,#42606,
#42607,#42608,#42609,#42610,#42611,#42612,#42613,#42614,#42615,#42616,#42617,
#42618,#42619,#42620,#42621,#42622,#42623,#42624,#42625,#42626,#42627,#42628,
#42629,#42630,#42631,#42632,#42633,#42634,#42635,#42636,#42637,#42638,#42639,
#42640,#42641,#42642,#42643,#42644,#42645,#42646,#42647,#42648,#42649,#42650,
#42651,#42652,#42653,#42654,#42655,#42656,#42657,#42658,#42659,#42660,#42661,
#42662,#42663,#42664,#42665,#42666,#42667,#42668,#42669,#42670,#42671,#42672,
#42673,#42674,#42675,#42676,#42677,#42678,#42679,#42680,#42681,#42682,#42683,
#42684,#42685,#42686,#42687,#42688,#42689,#42690,#42691,#42692,#42693,#42694,
#42695,#42696,#42697,#42698,#42699,#42700,#42701,#42702,#42703,#42704,#42705,
#42706,#42707,#42708,#42709,#42710,#42711,#42712,#42713,#42714,#42715,#42716,
#42717,#42718,#42719,#42720,#42721,#42722,#42723,#42724,#42725,#42726,#42727,
#42728,#42729,#42730,#42731,#42732,#42733,#42734,#42735,#42736,#42737,#42738,
#42739,#42740,#42741,#42742,#42743,#42744,#42745,#42746,#42747,#42748,#42749,
#42750,#42751,#42752,#42753,#42754,#42755,#42756,#42757,#42758,#42759,#42760,
#42761,#42762,#42763,#42764,#42765,#42766,#42767,#42768,#42769,#42770,#42771,
#42772,#42773,#42774,#42775,#42776),.UNSPECIFIED.,.F.,.F.,(4,2,2,2,2,2,
2,2,2,2,2,2,2,2,2,2,2,2,2,2,2,2,2,2,2,2,2,2,2,2,2,2,2,2,2,2,2,2,2,2,2,2,
2,2,2,2,2,2,2,2,2,2,2,2,2,2,2,2,2,2,2,2,2,2,2,2,2,2,2,2,2,2,2,2,2,2,2,2,
2,2,2,2,2,2,2,2,2,2,2,2,2,2,4),(-1.51233049812282,-1.49520335693357,-1.45341890982416,
-1.44179633687685,-1.43501448275276,-1.42892221739244,-1.42100365384326,
-1.40307666162952,-1.37618571162187,-1.33293026571111,-1.32266149263571,
-1.31847012783979,-1.31499447906295,-1.31106794433204,-1.30387191976979,
-1.29448320663815,-1.27077863110474,-1.21738804641697,-1.20643332393897,
-1.19978697260604,-1.19365780029338,-1.18545370203068,-1.16560011804255,
-1.13382929713325,-1.09370820494154,-1.08617021238293,-1.08212869115169,
-1.07902932792658,-1.07450155365158,-1.06405705714836,-1.04834628073441,
-1.01910222836283,-0.980492342424274,-0.970617949033637,-0.964189423944362,
-0.957953738999441,-0.949093672426513,-0.923901845062781,-0.872103253505443,
-0.855076986265714,-0.849550864306135,-0.846329101973191,-0.842706965479036,
-0.836951945327968,-0.81553272571764,-0.752350025092124,-0.740119777069768,
-0.732532379017395,-0.726471826127508,-0.71948612745093,-0.706840689927197,
-0.690611628062002,-0.644933748027284,-0.621247171007705,-0.615217829002575,
-0.611537412443848,-0.607927010256222,-0.602227544307099,-0.581557178844596,
-0.525543692297731,-0.507085354766102,-0.4996709517369,-0.493507919090064,
-0.487077773354796,-0.477194564606135,-0.436497505104086,-0.392439880641663,
-0.382774944748766,-0.378378828239623,-0.374959158200164,-0.370647958429207,
-0.361462417670658,-0.348373069524263,-0.30220794346562,-0.274713640483251,
-0.265459003477948,-0.259780921655329,-0.253552134851733,-0.244730887352929,
-0.219902010546971,-0.170050912909116,-0.151014058248076,-0.145300861927663,
-0.142044477138465,-0.138462511690016,-0.132902130437931,-0.113944075677719,
-0.0723202506959316,-0.0405572695984405,-0.0310096331612037,-0.0252806452145648,
-0.0195007169690655,-0.0181291440337079),.UNSPECIFIED.);
#487=B_SPLINE_CURVE_WITH_KNOTS('',3,(#42782,#42783,#42784,#42785,#42786,
#42787,#42788,#42789,#42790,#42791,#42792,#42793,#42794,#42795,#42796,#42797,
#42798,#42799,#42800,#42801,#42802,#42803,#42804,#42805,#42806,#42807,#42808,
#42809,#42810,#42811,#42812,#42813,#42814,#42815,#42816,#42817,#42818,#42819,
#42820,#42821,#42822,#42823,#42824,#42825,#42826,#42827,#42828,#42829,#42830,
#42831,#42832,#42833,#42834,#42835,#42836,#42837,#42838,#42839,#42840,#42841,
#42842,#42843,#42844,#42845,#42846,#42847,#42848,#42849,#42850,#42851,#42852,
#42853,#42854,#42855,#42856,#42857,#42858,#42859,#42860,#42861,#42862,#42863,
#42864,#42865,#42866,#42867,#42868,#42869,#42870,#42871,#42872,#42873,#42874,
#42875,#42876,#42877,#42878,#42879,#42880,#42881,#42882,#42883,#42884,#42885,
#42886,#42887,#42888,#42889,#42890,#42891,#42892,#42893,#42894,#42895,#42896,
#42897,#42898,#42899,#42900,#42901,#42902,#42903,#42904,#42905,#42906,#42907,
#42908,#42909,#42910,#42911,#42912,#42913,#42914,#42915,#42916,#42917,#42918,
#42919,#42920,#42921,#42922,#42923,#42924,#42925,#42926,#42927,#42928,#42929,
#42930,#42931,#42932,#42933,#42934,#42935,#42936,#42937,#42938,#42939,#42940,
#42941,#42942,#42943,#42944,#42945,#42946,#42947,#42948,#42949,#42950,#42951,
#42952,#42953,#42954,#42955,#42956,#42957,#42958,#42959,#42960,#42961,#42962,
#42963,#42964,#42965,#42966,#42967,#42968,#42969,#42970,#42971,#42972,#42973,
#42974,#42975),.UNSPECIFIED.,.F.,.F.,(4,2,2,2,2,2,2,2,2,2,2,2,2,2,2,2,2,
2,2,2,2,2,2,2,2,2,2,2,2,2,2,2,2,2,2,2,2,2,2,2,2,2,2,2,2,2,2,2,2,2,2,2,2,
2,2,2,2,2,2,2,2,2,2,2,2,2,2,2,2,2,2,2,2,2,2,2,2,2,2,2,2,2,2,2,2,2,2,2,2,
2,2,2,2,2,2,2,4),(-1.47740198524613,-1.45419209782398,-1.44032045971751,
-1.4352501292993,-1.43187101371906,-1.42819313379095,-1.42184832287723,
-1.41384206164589,-1.39543862935915,-1.33316152820262,-1.32255035193238,
-1.31610438786692,-1.31016435928457,-1.30223242871395,-1.28327390158397,
-1.25364515757429,-1.20914089113941,-1.20206732243934,-1.19819508434785,
-1.19484766352072,-1.19018811197207,-1.17836578113044,-1.15934145208305,
-1.09869918621491,-1.08773733534814,-1.0812197654682,-1.0753010762563,-1.06752689704047,
-1.04962249895316,-1.02258882149787,-0.979381500558301,-0.968901700613474,
-0.964786742597108,-0.961405132962325,-0.957646011017135,-0.950915371829222,
-0.942261411252994,-0.921365445595675,-0.867317357953329,-0.855520581228181,
-0.848172429018052,-0.8422975477032,-0.835529214059519,-0.823322601153206,
-0.80773920255148,-0.765666384383375,-0.737085149840926,-0.730980303476517,
-0.72735393822743,-0.723904999743672,-0.718642814307026,-0.701838814172476,
-0.66728983497446,-0.626452321077116,-0.616581878607501,-0.61028699035061,
-0.604282158373453,-0.595934562392113,-0.573883613892663,-0.537732734324123,
-0.502256062008874,-0.496026961049312,-0.492373954403145,-0.488941422419189,
-0.483764444369893,-0.4677889554156,-0.436423670465519,-0.394476418726455,
-0.383111768498982,-0.376450408138287,-0.370561372713379,-0.363050357603699,
-0.346789737931292,-0.323449907419803,-0.277011149509601,-0.264466005738296,
-0.259575807388622,-0.256194349316924,-0.252434396578643,-0.245700175762511,
-0.237040224633817,-0.216120757830807,-0.161978125765649,-0.150250295558495,
-0.14292122163854,-0.137047484638825,-0.130264958745839,-0.117987470160476,
-0.102281713933086,-0.060379973287392,-0.0319124698728966,-0.0257839457279635,
-0.0221524351675295,-0.0190288398810346,-0.0155703878589853,-0.00939615265272851,
-0.000672416806236772),.UNSPECIFIED.);
#488=B_SPLINE_CURVE_WITH_KNOTS('',3,(#42976,#42977,#42978,#42979),
 .UNSPECIFIED.,.F.,.F.,(4,4),(-2.9891163108282,-2.97165059380248),
 .UNSPECIFIED.);
#489=B_SPLINE_CURVE_WITH_KNOTS('',3,(#42981,#42982,#42983,#42984,#42985,
#42986),.UNSPECIFIED.,.F.,.F.,(4,2,4),(-0.0181291440337079,-0.0134571638401088,
-0.000668810733621533),.UNSPECIFIED.);
#490=B_SPLINE_CURVE_WITH_KNOTS('',3,(#42987,#42988,#42989,#42990,#42991,
#42992,#42993,#42994,#42995,#42996,#42997,#42998,#42999,#43000,#43001,#43002,
#43003,#43004,#43005,#43006,#43007,#43008,#43009,#43010,#43011,#43012,#43013,
#43014,#43015,#43016,#43017,#43018,#43019,#43020,#43021,#43022,#43023,#43024,
#43025,#43026,#43027,#43028,#43029,#43030,#43031,#43032,#43033,#43034,#43035,
#43036,#43037,#43038,#43039,#43040,#43041,#43042,#43043,#43044,#43045,#43046,
#43047,#43048,#43049,#43050,#43051,#43052,#43053,#43054,#43055,#43056,#43057,
#43058,#43059,#43060,#43061,#43062,#43063,#43064,#43065,#43066,#43067,#43068,
#43069,#43070,#43071,#43072,#43073,#43074,#43075,#43076,#43077,#43078,#43079,
#43080,#43081,#43082,#43083,#43084,#43085,#43086,#43087,#43088,#43089,#43090,
#43091,#43092,#43093,#43094,#43095,#43096,#43097,#43098,#43099,#43100,#43101,
#43102,#43103,#43104,#43105,#43106,#43107,#43108,#43109,#43110,#43111,#43112,
#43113,#43114,#43115,#43116,#43117,#43118,#43119,#43120,#43121,#43122,#43123,
#43124,#43125,#43126,#43127,#43128,#43129,#43130,#43131,#43132,#43133,#43134,
#43135,#43136,#43137,#43138,#43139,#43140,#43141,#43142,#43143,#43144,#43145,
#43146,#43147,#43148,#43149,#43150,#43151,#43152,#43153,#43154,#43155,#43156,
#43157,#43158,#43159,#43160,#43161,#43162,#43163,#43164,#43165,#43166),
 .UNSPECIFIED.,.F.,.F.,(4,2,2,2,2,2,2,2,2,2,2,2,2,2,2,2,2,2,2,2,2,2,2,2,
2,2,2,2,2,2,2,2,2,2,2,2,2,2,2,2,2,2,2,2,2,2,2,2,2,2,2,2,2,2,2,2,2,2,2,2,
2,2,2,2,2,2,2,2,2,2,2,2,2,2,2,2,2,2,2,2,2,2,2,2,2,2,2,2,2,4),(-2.98881938810218,
-2.93439497537859,-2.9145800492518,-2.90614190069954,-2.89950338942194,
-2.89569383111583,-2.89221221432576,-2.88783944062521,-2.87612034321371,
-2.829062810777,-2.80109454743576,-2.7876893881572,-2.78055730618365,-2.77450814625825,
-2.76711070710711,-2.75276469706528,-2.70042708522535,-2.68010482159931,
-2.66770201444379,-2.66287603700549,-2.65942194876788,-2.65542164570109,
-2.64807553758926,-2.60663019871394,-2.57557111169767,-2.56212174080765,
-2.55112457018215,-2.54447037600708,-2.53834529042842,-2.53030610745481,
-2.51247271231874,-2.45761655136665,-2.44235650375148,-2.43212163562672,
-2.42762893439963,-2.42453390605158,-2.42046934605467,-2.41282017713579,
-2.38239946644278,-2.35661588930368,-2.33497759196849,-2.31945630389264,
-2.31193610815551,-2.30588072152425,-2.29884717652222,-2.28631763288667,
-2.23177054917505,-2.21090286647497,-2.19828719256164,-2.19343107434001,
-2.18997276002405,-2.18598823095726,-2.17871673527048,-2.13635825847007,
-2.0909895213314,-2.0808190560409,-2.07433209400389,-2.06820373419418,-2.05960656820613,
-2.03842930636657,-1.97311389950393,-1.96265062722635,-1.95811981327767,
-1.95502021377962,-1.95098091708932,-1.94345322408305,-1.9035001161836,
-1.8716435726131,-1.85175855894381,-1.84355026667493,-1.83742052797324,
-1.83077598431345,-1.81983017266896,-1.76632252253541,-1.74265006321361,
-1.73326821121888,-1.72607672236816,-1.72215114226118,-1.71867513948953,
-1.71448236264089,-1.70420485872274,-1.66098552097911,-1.63411434959317,
-1.61619483341578,-1.60827748096783,-1.60218525173031,-1.59540251917259,
-1.58377621770273,-1.54207743820327,-1.51221321296554),.UNSPECIFIED.);
#491=B_SPLINE_CURVE_WITH_KNOTS('',3,(#43171,#43172,#43173,#43174,#43175,
#43176,#43177,#43178,#43179,#43180,#43181,#43182,#43183,#43184,#43185,#43186,
#43187,#43188,#43189,#43190,#43191,#43192,#43193,#43194,#43195,#43196,#43197,
#43198,#43199,#43200,#43201,#43202,#43203,#43204,#43205,#43206,#43207,#43208,
#43209,#43210,#43211,#43212,#43213,#43214,#43215,#43216,#43217,#43218,#43219,
#43220,#43221,#43222,#43223,#43224,#43225,#43226,#43227,#43228,#43229,#43230,
#43231,#43232,#43233,#43234,#43235,#43236,#43237,#43238,#43239,#43240,#43241,
#43242,#43243,#43244,#43245,#43246,#43247,#43248,#43249,#43250,#43251,#43252,
#43253,#43254,#43255,#43256,#43257,#43258,#43259,#43260,#43261,#43262,#43263,
#43264,#43265,#43266,#43267,#43268,#43269,#43270,#43271,#43272,#43273,#43274,
#43275,#43276,#43277,#43278,#43279,#43280,#43281,#43282,#43283,#43284,#43285,
#43286,#43287,#43288,#43289,#43290,#43291,#43292,#43293,#43294,#43295,#43296,
#43297,#43298,#43299,#43300,#43301,#43302,#43303,#43304,#43305,#43306,#43307,
#43308,#43309,#43310,#43311,#43312,#43313,#43314,#43315,#43316,#43317,#43318,
#43319,#43320,#43321,#43322,#43323,#43324,#43325,#43326,#43327,#43328,#43329,
#43330,#43331,#43332,#43333,#43334,#43335,#43336,#43337,#43338,#43339,#43340,
#43341,#43342,#43343,#43344,#43345,#43346,#43347,#43348,#43349,#43350,#43351,
#43352,#43353,#43354,#43355,#43356),.UNSPECIFIED.,.F.,.F.,(4,2,2,2,2,2,
2,2,2,2,2,2,2,2,2,2,2,2,2,2,2,2,2,2,2,2,2,2,2,2,2,2,2,2,2,2,2,2,2,2,2,2,
2,2,2,2,2,2,2,2,2,2,2,2,2,2,2,2,2,2,2,2,2,2,2,2,2,2,2,2,2,2,2,2,2,2,2,2,
2,2,2,2,2,2,2,2,2,2,2,2,2,2,4),(-2.9716555919461,-2.97154817145025,-2.96562500995768,
-2.96005983868355,-2.95383901635577,-2.94433737881855,-2.91042200232887,
-2.86852541548387,-2.8513991194649,-2.84610485960585,-2.84264957015553,
-2.8390325070509,-2.83297145461849,-2.80573416970697,-2.76262311128696,
-2.73937387006405,-2.73088303932833,-2.72485365470322,-2.71934120629572,
-2.71033477040861,-2.68389380009236,-2.62507751112293,-2.61443080687828,
-2.60994974676855,-2.60662230104157,-2.60264016113958,-2.59504803234435,
-2.56061750264067,-2.52552509769381,-2.51076101299859,-2.49903285782614,
-2.49235964550477,-2.4864721512604,-2.47897955202297,-2.46283025579605,
-2.40289420833313,-2.38185584238939,-2.37623055989595,-2.37270655457017,
-2.36917208392626,-2.36349800441212,-2.34383769818164,-2.29421154679409,
-2.26950356352012,-2.26084938984811,-2.25479028582538,-2.24857898769667,
-2.2391283201122,-2.20782648423084,-2.16496056829367,-2.14635185798616,
-2.14092024430943,-2.13743685635153,-2.13385655909084,-2.12796856647655,
-2.10509538831603,-2.05835465463885,-2.03424771442571,-2.02565895080156,
-2.01961163613887,-2.013383827537,-2.00385000383816,-1.97100922053,-1.9366573715958,
-1.91999726119949,-1.90918084326314,-1.90467288741157,-1.90134276866777,
-1.89737847087723,-1.88964090997174,-1.85773347962173,-1.82092565319927,
-1.79866573414472,-1.79029205047388,-1.78428228818944,-1.77799434293165,
-1.76816076292468,-1.7268722606643,-1.69256122991686,-1.67581401960605,
-1.67055687743046,-1.66710865618302,-1.6634801096047,-1.65736654063487,
-1.62841318210618,-1.58666063730659,-1.56376059691621,-1.55531002587557,
-1.54928716040567,-1.54302197764727,-1.53330094026359,-1.49453840988134,
-1.47740198524613),.UNSPECIFIED.);
#492=B_SPLINE_CURVE_WITH_KNOTS('',3,(#43357,#43358,#43359,#43360,#43361,
#43362,#43363,#43364,#43365,#43366,#43367,#43368,#43369,#43370,#43371,#43372,
#43373,#43374,#43375,#43376,#43377,#43378,#43379,#43380,#43381,#43382,#43383,
#43384,#43385,#43386,#43387,#43388,#43389,#43390,#43391,#43392,#43393,#43394,
#43395,#43396,#43397,#43398,#43399,#43400,#43401,#43402,#43403,#43404,#43405,
#43406,#43407,#43408,#43409,#43410,#43411,#43412,#43413,#43414,#43415,#43416,
#43417,#43418,#43419,#43420,#43421,#43422,#43423,#43424,#43425,#43426,#43427,
#43428,#43429,#43430,#43431,#43432,#43433,#43434,#43435,#43436,#43437,#43438,
#43439,#43440,#43441,#43442,#43443,#43444,#43445,#43446,#43447,#43448,#43449,
#43450,#43451,#43452,#43453,#43454,#43455,#43456,#43457,#43458,#43459,#43460,
#43461,#43462,#43463,#43464,#43465,#43466,#43467,#43468,#43469,#43470,#43471,
#43472,#43473,#43474,#43475,#43476,#43477,#43478,#43479,#43480,#43481,#43482,
#43483,#43484,#43485,#43486,#43487,#43488,#43489,#43490,#43491,#43492,#43493,
#43494,#43495,#43496,#43497,#43498,#43499,#43500,#43501,#43502,#43503,#43504,
#43505,#43506,#43507,#43508,#43509,#43510,#43511,#43512,#43513,#43514,#43515,
#43516,#43517,#43518,#43519,#43520,#43521,#43522,#43523,#43524,#43525,#43526,
#43527,#43528,#43529,#43530,#43531,#43532,#43533,#43534,#43535,#43536,#43537,
#43538,#43539,#43540,#43541,#43542),.UNSPECIFIED.,.F.,.F.,(4,2,2,2,2,2,
2,2,2,2,2,2,2,2,2,2,2,2,2,2,2,2,2,2,2,2,2,2,2,2,2,2,2,2,2,2,2,2,2,2,2,2,
2,2,2,2,2,2,2,2,2,2,2,2,2,2,2,2,2,2,2,2,2,2,2,2,2,2,2,2,2,2,2,2,2,2,2,2,
2,2,2,2,2,2,2,2,2,2,2,2,2,2,4),(-1.51221321296554,-1.51085484546286,-1.49484427234498,
-1.48956990796848,-1.48607821760021,-1.4822859170049,-1.4757319796956,-1.46743687932551,
-1.44817086842178,-1.38861439066354,-1.37738351716336,-1.37068117478839,
-1.3645694920746,-1.35649227251671,-1.3375169891521,-1.30805928939344,-1.26376081573809,
-1.25660526368414,-1.25264542141063,-1.24917991699939,-1.24427476966737,
-1.23130443964399,-1.2095066873353,-1.15225764308533,-1.14183767370461,
-1.13529983490702,-1.12912697543539,-1.12063568008592,-1.09862995947849,
-1.06288856704313,-1.02736365562602,-1.02102341321342,-1.01727665699929,
-1.01371634365497,-1.00826393385117,-0.9904932218741,-0.952110080253169,
-0.916210482773215,-0.906422808865517,-0.900011525037985,-0.893763900962858,
-0.88483664013308,-0.858996623044593,-0.803251455004088,-0.789990848365579,
-0.78491523699523,-0.781423330324444,-0.777541968066019,-0.770564575860217,
-0.761553469633356,-0.739452753531308,-0.682838850924898,-0.672325065863944,
-0.665768099625375,-0.659603789833833,-0.65116703023199,-0.629590554626786,
-0.592731122358163,-0.560392452056923,-0.552624309903082,-0.548534467194944,
-0.545129568803643,-0.540472601588181,-0.529216700190913,-0.511682420954267,
-0.455263475391965,-0.440581766892907,-0.433210612644359,-0.427161116294937,
-0.420003326845187,-0.406468599704118,-0.33913585792777,-0.321417424973873,
-0.315828066139664,-0.312594631019935,-0.3089867166535,-0.303300383466177,
-0.282806771731894,-0.228252557069223,-0.208469866538841,-0.200931991000315,
-0.19473877762972,-0.188350386942891,-0.178680975267564,-0.143101944131677,
-0.0935604393360744,-0.0847617326463241,-0.0804581162290219,-0.0769919585924988,
-0.0731442758265341,-0.066328792090819,-0.0575939795842131,-0.0178393446226998),
 .UNSPECIFIED.);
#493=B_SPLINE_CURVE_WITH_KNOTS('',3,(#43548,#43549,#43550,#43551,#43552,
#43553,#43554,#43555,#43556,#43557,#43558,#43559,#43560,#43561,#43562,#43563,
#43564,#43565,#43566,#43567,#43568,#43569,#43570,#43571,#43572,#43573,#43574,
#43575,#43576,#43577,#43578,#43579,#43580,#43581,#43582,#43583,#43584,#43585,
#43586,#43587,#43588,#43589,#43590,#43591,#43592,#43593,#43594,#43595,#43596,
#43597,#43598,#43599,#43600,#43601,#43602,#43603,#43604,#43605,#43606,#43607,
#43608,#43609,#43610,#43611,#43612,#43613,#43614,#43615,#43616,#43617,#43618,
#43619,#43620,#43621,#43622,#43623,#43624,#43625,#43626,#43627,#43628,#43629,
#43630,#43631,#43632,#43633,#43634,#43635,#43636,#43637,#43638,#43639,#43640,
#43641,#43642,#43643,#43644,#43645,#43646,#43647,#43648,#43649,#43650,#43651,
#43652,#43653,#43654,#43655,#43656,#43657,#43658,#43659,#43660,#43661,#43662,
#43663,#43664,#43665,#43666,#43667,#43668,#43669,#43670,#43671,#43672,#43673,
#43674,#43675,#43676,#43677,#43678,#43679,#43680,#43681,#43682,#43683,#43684,
#43685,#43686,#43687,#43688,#43689,#43690,#43691,#43692,#43693,#43694,#43695,
#43696,#43697,#43698,#43699,#43700,#43701,#43702,#43703,#43704,#43705,#43706,
#43707,#43708,#43709,#43710,#43711,#43712,#43713,#43714,#43715,#43716,#43717,
#43718,#43719,#43720,#43721,#43722,#43723,#43724,#43725),.UNSPECIFIED.,
 .F.,.F.,(4,2,2,2,2,2,2,2,2,2,2,2,2,2,2,2,2,2,2,2,2,2,2,2,2,2,2,2,2,2,2,
2,2,2,2,2,2,2,2,2,2,2,2,2,2,2,2,2,2,2,2,2,2,2,2,2,2,2,2,2,2,2,2,2,2,2,2,
2,2,2,2,2,2,2,2,2,2,2,2,2,2,2,2,2,2,2,2,2,4),(-1.47759266585272,-1.47583902726231,
-1.44357763760892,-1.40282698793516,-1.39145610972514,-1.38479306930802,
-1.37890371782198,-1.37139390483523,-1.35514289943167,-1.33182451894543,
-1.28552002324551,-1.27284185197666,-1.26793124540071,-1.26454620903653,
-1.26079442794825,-1.25410014054262,-1.24550819972451,-1.22486098243887,
-1.17181956373618,-1.15804517865605,-1.15088889585203,-1.14502343023918,
-1.1381019052825,-1.12511555701983,-1.08529653068715,-1.04219353760626,
-1.03502442930169,-1.03113152417172,-1.02778843535297,-1.02316470249161,
-1.01158823444863,-0.99316018795545,-0.930943083829598,-0.920317454469369,
-0.913868291989847,-0.90792886474967,-0.900003118701505,-0.881089033406792,
-0.851574886104677,-0.806854911075443,-0.799800666323608,-0.795932451125106,
-0.792583827677378,-0.787916278389732,-0.776039923746547,-0.756883711320975,
-0.696571545983134,-0.685538991332259,-0.679006748262875,-0.673091380849142,
-0.665345827782787,-0.647628761643719,-0.621037215485704,-0.579029457168609,
-0.567160937681541,-0.562379668855682,-0.559015233292986,-0.555205671877932,
-0.548233251102993,-0.509439276894764,-0.462137164521418,-0.450743910226097,
-0.444138518098801,-0.438239683105726,-0.430633358617338,-0.413792904738116,
-0.389194087090511,-0.336916459752479,-0.329687883995292,-0.325782357178985,
-0.322778032310721,-0.318396075404208,-0.308358989994193,-0.293411418199345,
-0.257639984165958,-0.223524409444837,-0.213959562965366,-0.207725653791638,
-0.201682678058227,-0.19311786264907,-0.16922825281877,-0.123469658836699,
-0.0993831546337505,-0.0934465306990903,-0.0898558423729977,-0.0863806053261936,
-0.080988929077923,-0.0628273352297112,-0.000673664115542865),
 .UNSPECIFIED.);
#494=B_SPLINE_CURVE_WITH_KNOTS('',3,(#43726,#43727,#43728,#43729,#43730,
#43731),.UNSPECIFIED.,.F.,.F.,(4,2,4),(-2.98910690514882,-2.9794000728681,
-2.9716555919461),.UNSPECIFIED.);
#495=B_SPLINE_CURVE_WITH_KNOTS('',3,(#43733,#43734,#43735,#43736),
 .UNSPECIFIED.,.F.,.F.,(4,4),(-0.0178393446226998,-0.000669879165383271),
 .UNSPECIFIED.);
#496=B_SPLINE_CURVE_WITH_KNOTS('',3,(#43737,#43738,#43739,#43740,#43741,
#43742,#43743,#43744,#43745,#43746,#43747,#43748,#43749,#43750,#43751,#43752,
#43753,#43754,#43755,#43756,#43757,#43758,#43759,#43760,#43761,#43762,#43763,
#43764,#43765,#43766,#43767,#43768,#43769,#43770,#43771,#43772,#43773,#43774,
#43775,#43776,#43777,#43778,#43779,#43780,#43781,#43782,#43783,#43784,#43785,
#43786,#43787,#43788,#43789,#43790,#43791,#43792,#43793,#43794,#43795,#43796,
#43797,#43798,#43799,#43800,#43801,#43802,#43803,#43804,#43805,#43806,#43807,
#43808,#43809,#43810,#43811,#43812,#43813,#43814,#43815,#43816,#43817,#43818,
#43819,#43820,#43821,#43822,#43823,#43824,#43825,#43826,#43827,#43828,#43829,
#43830,#43831,#43832,#43833,#43834,#43835,#43836,#43837,#43838,#43839,#43840,
#43841,#43842,#43843,#43844,#43845,#43846,#43847,#43848,#43849,#43850,#43851,
#43852,#43853,#43854,#43855,#43856,#43857,#43858,#43859,#43860,#43861,#43862,
#43863,#43864,#43865,#43866,#43867,#43868,#43869,#43870,#43871,#43872,#43873,
#43874,#43875,#43876,#43877,#43878,#43879,#43880,#43881,#43882,#43883,#43884,
#43885,#43886,#43887,#43888,#43889,#43890,#43891,#43892,#43893,#43894,#43895,
#43896,#43897,#43898,#43899,#43900,#43901,#43902,#43903,#43904,#43905,#43906,
#43907,#43908,#43909,#43910,#43911,#43912,#43913,#43914,#43915,#43916,#43917,
#43918),.UNSPECIFIED.,.F.,.F.,(4,2,2,2,2,2,2,2,2,2,2,2,2,2,2,2,2,2,2,2,
2,2,2,2,2,2,2,2,2,2,2,2,2,2,2,2,2,2,2,2,2,2,2,2,2,2,2,2,2,2,2,2,2,2,2,2,
2,2,2,2,2,2,2,2,2,2,2,2,2,2,2,2,2,2,2,2,2,2,2,2,2,2,2,2,2,2,2,2,2,2,4),
(-2.98894532842057,-2.96679766759181,-2.95895194939698,-2.95299040461239,
-2.94688554234206,-2.94015963035491,-2.92881155233073,-2.88051159025543,
-2.84886443595245,-2.83784551973106,-2.8332256742013,-2.82979396244754,
-2.82566495177523,-2.81745385019771,-2.77198792205609,-2.74433561670034,
-2.72608918694708,-2.71812198458179,-2.71202447485776,-2.70526903091423,
-2.69377513069564,-2.64604539526109,-2.60816966081843,-2.60102031220554,
-2.5971035383971,-2.59362484956453,-2.58863072902918,-2.57593175789617,
-2.51959588682296,-2.49367578698727,-2.48474120277274,-2.47849255209288,
-2.47208360061814,-2.46230643032818,-2.42691896305785,-2.38807462163282,
-2.37020233164769,-2.3647402752484,-2.36117821981831,-2.35743456252897,
-2.35110844570821,-2.31584339009273,-2.27994130921511,-2.26492263576045,
-2.25297939586326,-2.24613340943604,-2.24005431974874,-2.23225222737033,
-2.21572099481243,-2.15832914657657,-2.14326678316657,-2.13312386458711,
-2.12864610895088,-2.12522384127365,-2.12098533011795,-2.11219699852639,
-2.05080030250098,-2.02422687262648,-2.01522738099746,-2.00896703140146,
-2.00257390830332,-1.99287680613008,-1.95992483733062,-1.91899502335571,
-1.90068912626002,-1.89518693704619,-1.89161696413409,-1.88834931939354,
-1.88257538865616,-1.86290446052514,-1.81370721255665,-1.78901287109256,
-1.78020720307339,-1.77398163990907,-1.76830129606733,-1.7590311582901,
-1.73138176545606,-1.68534114535974,-1.66609182213885,-1.66050670321025,
-1.65692009052091,-1.65321108586562,-1.64704707731286,-1.61990304476685,
-1.57711487869409,-1.55386793511717,-1.54522603008742,-1.53902861293514,
-1.53331479880452,-1.52385069073556,-1.51202351089742),.UNSPECIFIED.);
#497=B_SPLINE_CURVE_WITH_KNOTS('',3,(#43923,#43924,#43925,#43926,#43927,
#43928,#43929,#43930,#43931,#43932,#43933,#43934,#43935,#43936,#43937,#43938,
#43939,#43940,#43941,#43942,#43943,#43944,#43945,#43946,#43947,#43948,#43949,
#43950,#43951,#43952,#43953,#43954,#43955,#43956,#43957,#43958,#43959,#43960,
#43961,#43962,#43963,#43964,#43965,#43966,#43967,#43968,#43969,#43970,#43971,
#43972,#43973,#43974,#43975,#43976,#43977,#43978,#43979,#43980,#43981,#43982,
#43983,#43984,#43985,#43986,#43987,#43988,#43989,#43990,#43991,#43992,#43993,
#43994,#43995,#43996,#43997,#43998,#43999,#44000,#44001,#44002,#44003,#44004,
#44005,#44006,#44007,#44008,#44009,#44010,#44011,#44012,#44013,#44014,#44015,
#44016,#44017,#44018,#44019,#44020,#44021,#44022,#44023,#44024,#44025,#44026,
#44027,#44028,#44029,#44030,#44031,#44032,#44033,#44034,#44035,#44036,#44037,
#44038,#44039,#44040,#44041,#44042,#44043,#44044,#44045,#44046,#44047,#44048,
#44049,#44050,#44051,#44052,#44053,#44054,#44055,#44056,#44057,#44058,#44059,
#44060,#44061,#44062,#44063,#44064,#44065,#44066,#44067,#44068,#44069,#44070,
#44071,#44072,#44073,#44074,#44075,#44076,#44077,#44078,#44079,#44080,#44081,
#44082,#44083,#44084,#44085,#44086,#44087,#44088,#44089,#44090,#44091,#44092,
#44093,#44094,#44095,#44096,#44097,#44098,#44099,#44100,#44101,#44102,#44103,
#44104,#44105,#44106,#44107,#44108),.UNSPECIFIED.,.F.,.F.,(4,2,2,2,2,2,
2,2,2,2,2,2,2,2,2,2,2,2,2,2,2,2,2,2,2,2,2,2,2,2,2,2,2,2,2,2,2,2,2,2,2,2,
2,2,2,2,2,2,2,2,2,2,2,2,2,2,2,2,2,2,2,2,2,2,2,2,2,2,2,2,2,2,2,2,2,2,2,2,
2,2,2,2,2,2,2,2,2,2,2,2,2,2,4),(-2.9718798661411,-2.92833422092586,-2.91754480451469,
-2.91304124566946,-2.90974131486556,-2.90578828592925,-2.89833497354585,
-2.84737885793396,-2.82224322820136,-2.80516076667878,-2.79751556758755,
-2.79161238385916,-2.78502841449271,-2.77374097876193,-2.72442391911659,
-2.6863392061329,-2.67996517302808,-2.67628113578022,-2.67290516971136,
-2.66785240361569,-2.65411145792008,-2.60891342949597,-2.58579311774677,
-2.56963426639711,-2.56214003685471,-2.55625224218432,-2.54957971525801,
-2.53816407024515,-2.49932129767375,-2.46563387246433,-2.44904378045224,
-2.44380253340108,-2.44035744773731,-2.43672415821915,-2.43058829529567,
-2.39964548903531,-2.35940066815492,-2.33690977930333,-2.3285081480383,
-2.32249373740921,-2.31621437322995,-2.30642278092401,-2.26575853088833,
-2.23090366431735,-2.2140222697628,-2.2087518173252,-2.20530103728228,-2.20167657954524,
-2.19558186336725,-2.16736205417542,-2.12503467590148,-2.10198455319833,
-2.09351645960803,-2.08749066622084,-2.08197310437768,-2.07293886603976,
-2.04618825963088,-1.9876284293558,-1.97705680568901,-1.97258748370793,
-1.96926086364871,-1.96527005268775,-1.95763720337968,-1.9259235242493,
-1.8889589752926,-1.8666494532543,-1.85826947025256,-1.85225844538663,-1.845972030648,
-1.83614692345946,-1.79663369523838,-1.76150029995517,-1.74394531245887,
-1.73860938034474,-1.73514542677704,-1.7315394766195,-1.7255318735531,-1.69960685868486,
-1.65540848140326,-1.63188891567363,-1.62336613668799,-1.61733049215749,
-1.6110851140738,-1.60146353288126,-1.56605727446876,-1.53231996876569,
-1.51696069078904,-1.50673255100101,-1.5023189224699,-1.49899692535738,
-1.49496616648127,-1.48688770425023,-1.47759266585272),.UNSPECIFIED.);
#498=B_SPLINE_CURVE_WITH_KNOTS('',3,(#44109,#44110,#44111,#44112,#44113,
#44114,#44115,#44116,#44117,#44118,#44119,#44120,#44121,#44122,#44123,#44124,
#44125,#44126,#44127,#44128,#44129,#44130,#44131,#44132,#44133,#44134,#44135,
#44136,#44137,#44138,#44139,#44140,#44141,#44142,#44143,#44144,#44145,#44146,
#44147,#44148,#44149,#44150,#44151,#44152,#44153,#44154,#44155,#44156,#44157,
#44158,#44159,#44160,#44161,#44162,#44163,#44164,#44165,#44166,#44167,#44168,
#44169,#44170,#44171,#44172,#44173,#44174,#44175,#44176,#44177,#44178,#44179,
#44180,#44181,#44182,#44183,#44184,#44185,#44186,#44187,#44188,#44189,#44190,
#44191,#44192,#44193,#44194,#44195,#44196,#44197,#44198,#44199,#44200,#44201,
#44202,#44203,#44204,#44205,#44206,#44207,#44208,#44209,#44210,#44211,#44212,
#44213,#44214,#44215,#44216,#44217,#44218,#44219,#44220,#44221,#44222,#44223,
#44224,#44225,#44226,#44227,#44228,#44229,#44230,#44231,#44232,#44233,#44234,
#44235,#44236,#44237,#44238,#44239,#44240,#44241,#44242,#44243,#44244,#44245,
#44246,#44247,#44248,#44249,#44250,#44251,#44252,#44253,#44254,#44255,#44256,
#44257,#44258,#44259,#44260,#44261,#44262,#44263,#44264,#44265,#44266,#44267,
#44268,#44269,#44270,#44271,#44272,#44273,#44274,#44275,#44276,#44277,#44278,
#44279,#44280,#44281,#44282,#44283,#44284,#44285,#44286,#44287,#44288,#44289,
#44290),.UNSPECIFIED.,.F.,.F.,(4,2,2,2,2,2,2,2,2,2,2,2,2,2,2,2,2,2,2,2,
2,2,2,2,2,2,2,2,2,2,2,2,2,2,2,2,2,2,2,2,2,2,2,2,2,2,2,2,2,2,2,2,2,2,2,2,
2,2,2,2,2,2,2,2,2,2,2,2,2,2,2,2,2,2,2,2,2,2,2,2,2,2,2,2,2,2,2,2,2,2,4),
(-1.51202351089742,-1.49449240811967,-1.45667173300721,-1.43227678108567,
-1.42622370023567,-1.42253844292242,-1.41893281371061,-1.41325518393757,
-1.39286349735994,-1.33909010650591,-1.31869231935832,-1.31021804321852,
-1.30404827134258,-1.29750531163309,-1.28705854709645,-1.27449300749082,
-1.24697289772713,-1.20192620313761,-1.19328075226823,-1.1890690690116,
-1.18598862455779,-1.18167885613466,-1.17249990441517,-1.15942318858956,
-1.11336386847791,-1.08577253446091,-1.07650881157454,-1.07082955720942,
-1.0646029030008,-1.0557913515612,-1.03104693085066,-0.981620263707763,
-0.962138817641369,-0.956388603537074,-0.953125416503227,-0.949550912447172,
-0.944026524766034,-0.925473119625564,-0.883272275422081,-0.851776518799035,
-0.842154500198513,-0.835775928968778,-0.829503648362441,-0.820440033989039,
-0.79320445428282,-0.763440710119895,-0.731148219548661,-0.723384167091417,
-0.719295260506067,-0.715890353808088,-0.711232334437589,-0.699968969113581,
-0.682417090596136,-0.625865676701502,-0.611465296223883,-0.604056643041399,
-0.59800613102232,-0.590881443815959,-0.577519130217075,-0.55077469138695,
-0.50809783953738,-0.491949968254766,-0.486512761700874,-0.483307183798012,
-0.479663483642516,-0.473805488927917,-0.450855961060644,-0.421495425269382,
-0.382785434418195,-0.372902320473972,-0.366472266931216,-0.360238101984609,
-0.351385408219891,-0.326260518998026,-0.27482914644042,-0.257429685626527,
-0.251869123788893,-0.248641189206723,-0.245027282671453,-0.23931102011774,
-0.218418076884369,-0.160464312214743,-0.143113177841032,-0.135285917195027,
-0.129204015954906,-0.122372217698661,-0.110500714053059,-0.0956018553195042,
-0.0455136996519052,-0.0233411546340862,-0.0179078448206664),
 .UNSPECIFIED.);
#499=B_SPLINE_CURVE_WITH_KNOTS('',3,(#44296,#44297,#44298,#44299,#44300,
#44301,#44302,#44303,#44304,#44305,#44306,#44307,#44308,#44309,#44310,#44311,
#44312,#44313,#44314,#44315,#44316,#44317,#44318,#44319,#44320,#44321,#44322,
#44323,#44324,#44325,#44326,#44327,#44328,#44329,#44330,#44331,#44332,#44333,
#44334,#44335,#44336,#44337,#44338,#44339,#44340,#44341,#44342,#44343,#44344,
#44345,#44346,#44347,#44348,#44349,#44350,#44351,#44352,#44353,#44354,#44355,
#44356,#44357,#44358,#44359,#44360,#44361,#44362,#44363,#44364,#44365,#44366,
#44367,#44368,#44369,#44370,#44371,#44372,#44373,#44374,#44375,#44376,#44377,
#44378,#44379,#44380,#44381,#44382,#44383,#44384,#44385,#44386,#44387,#44388,
#44389,#44390,#44391,#44392,#44393,#44394,#44395,#44396,#44397,#44398,#44399,
#44400,#44401,#44402,#44403,#44404,#44405,#44406,#44407,#44408,#44409,#44410,
#44411,#44412,#44413,#44414,#44415,#44416,#44417,#44418,#44419,#44420,#44421,
#44422,#44423,#44424,#44425,#44426,#44427,#44428,#44429,#44430,#44431,#44432,
#44433,#44434,#44435,#44436,#44437,#44438,#44439,#44440,#44441,#44442,#44443,
#44444,#44445,#44446,#44447,#44448,#44449,#44450,#44451,#44452,#44453,#44454,
#44455,#44456,#44457,#44458,#44459,#44460,#44461,#44462,#44463,#44464,#44465,
#44466,#44467,#44468,#44469,#44470,#44471,#44472,#44473,#44474,#44475,#44476,
#44477,#44478,#44479,#44480,#44481,#44482,#44483),.UNSPECIFIED.,.F.,.F.,
(4,2,2,2,2,2,2,2,2,2,2,2,2,2,2,2,2,2,2,2,2,2,2,2,2,2,2,2,2,2,2,2,2,2,2,
2,2,2,2,2,2,2,2,2,2,2,2,2,2,2,2,2,2,2,2,2,2,2,2,2,2,2,2,2,2,2,2,2,2,2,2,
2,2,2,2,2,2,2,2,2,2,2,2,2,2,2,2,2,2,2,2,2,2,4),(-1.47753946869224,-1.46618248352132,
-1.45691851919379,-1.45136133851937,-1.44536781524085,-1.4370870041636,
-1.41556570221468,-1.37860916525036,-1.34325380867798,-1.33703153954625,
-1.3333800194858,-1.32994688395311,-1.3247657300231,-1.30874770913032,-1.2772238021133,
-1.23550219801313,-1.22413729202231,-1.21747637383588,-1.21158808214697,
-1.20407850559651,-1.18782320912539,-1.16449365988635,-1.11810927644965,
-1.10551704404071,-1.10061988830811,-1.09723763413345,-1.09348144488119,
-1.08676374894339,-1.07813152235602,-1.05732120876362,-1.00361841829855,
-0.991564649268644,-0.984145642407389,-0.978265757513395,-0.971547452429796,
-0.959590138548559,-0.944434200786007,-0.907441973027564,-0.875735155161742,
-0.868104334406487,-0.864114602826274,-0.860788807267809,-0.85632061096433,
-0.845751433122958,-0.787224528868138,-0.760505684120399,-0.751476240724885,
-0.74596035248848,-0.73993534232369,-0.731466440891137,-0.708401842201584,
-0.666017075838354,-0.637839663340758,-0.63174657323786,-0.628122923275746,
-0.624672724341686,-0.619402944062406,-0.60251908955384,-0.567641895910534,
-0.527026487599689,-0.517261790184601,-0.510988704370244,-0.504972526134255,
-0.496555407958669,-0.473929093663006,-0.433192562673141,-0.402875551349121,
-0.39674253876911,-0.393110306139631,-0.38966557533869,-0.384424058309238,
-0.367823156862109,-0.334083134923481,-0.295387092282997,-0.283968265791485,
-0.277295805630139,-0.271998076212244,-0.264806017603035,-0.250373220942863,
-0.184319218400211,-0.166526503446687,-0.161028660228815,-0.157877333845171,
-0.154405702471056,-0.149030907458394,-0.131052134028601,-0.103753202124731,
-0.0587944974736545,-0.0480352831879279,-0.0415587955374134,-0.0358769710594849,
-0.0301150406546835,-0.0225717469071839,-0.000673031561821805),
 .UNSPECIFIED.);
#500=B_SPLINE_CURVE_WITH_KNOTS('',3,(#44484,#44485,#44486,#44487),
 .UNSPECIFIED.,.F.,.F.,(4,4),(-2.98904500870718,-2.9718798661411),
 .UNSPECIFIED.);
#501=B_SPLINE_CURVE_WITH_KNOTS('',3,(#44489,#44490,#44491,#44492,#44493,
#44494,#44495,#44496,#44497,#44498,#44499,#44500),.UNSPECIFIED.,.F.,.F.,
(4,2,2,2,2,4),(-0.0179078448206664,-0.0174171828290496,-0.0137593046355443,
-0.0105814554284645,-0.00598018056482628,-0.000668823528435467),
 .UNSPECIFIED.);
#502=B_SPLINE_CURVE_WITH_KNOTS('',3,(#44501,#44502,#44503,#44504,#44505,
#44506,#44507,#44508,#44509,#44510,#44511,#44512,#44513,#44514,#44515,#44516,
#44517,#44518,#44519,#44520,#44521,#44522,#44523,#44524,#44525,#44526,#44527,
#44528,#44529,#44530,#44531,#44532,#44533,#44534,#44535,#44536,#44537,#44538,
#44539,#44540,#44541,#44542,#44543,#44544,#44545,#44546,#44547,#44548,#44549,
#44550,#44551,#44552,#44553,#44554,#44555,#44556,#44557,#44558,#44559,#44560,
#44561,#44562,#44563,#44564,#44565,#44566,#44567,#44568,#44569,#44570,#44571,
#44572,#44573,#44574,#44575,#44576,#44577,#44578,#44579,#44580,#44581,#44582,
#44583,#44584,#44585,#44586,#44587,#44588,#44589,#44590,#44591,#44592,#44593,
#44594,#44595,#44596,#44597,#44598,#44599,#44600,#44601,#44602,#44603,#44604,
#44605,#44606,#44607,#44608,#44609,#44610,#44611,#44612,#44613,#44614,#44615,
#44616,#44617,#44618,#44619,#44620,#44621,#44622,#44623,#44624,#44625,#44626,
#44627,#44628,#44629,#44630,#44631,#44632,#44633,#44634,#44635,#44636,#44637,
#44638,#44639,#44640,#44641,#44642,#44643,#44644,#44645,#44646,#44647,#44648,
#44649,#44650,#44651,#44652,#44653,#44654,#44655,#44656,#44657,#44658,#44659,
#44660,#44661,#44662,#44663,#44664,#44665,#44666,#44667,#44668,#44669,#44670,
#44671,#44672,#44673,#44674,#44675,#44676),.UNSPECIFIED.,.F.,.F.,(4,2,2,
2,2,2,2,2,2,2,2,2,2,2,2,2,2,2,2,2,2,2,2,2,2,2,2,2,2,2,2,2,2,2,2,2,2,2,2,
2,2,2,2,2,2,2,2,2,2,2,2,2,2,2,2,2,2,2,2,2,2,2,2,2,2,2,2,2,2,2,2,2,2,2,2,
2,2,2,2,2,2,2,2,2,2,2,2,4),(-2.9893589500714,-2.95396180238871,-2.92167880417226,
-2.89897537225032,-2.89039827744236,-2.88421156194824,-2.87848314243502,
-2.86893603254614,-2.83859933256492,-2.79528018187012,-2.77651284475504,
-2.77096928492961,-2.76739100976997,-2.76367060426163,-2.75745352729353,
-2.72868485465799,-2.6871891202505,-2.66427774458408,-2.65567556146713,
-2.64948467221613,-2.64376190246831,-2.63424709836998,-2.60415218206783,
-2.56057742482876,-2.54176287545832,-2.5362151629149,-2.53263605008132,
-2.52891679696925,-2.52270508527172,-2.49408539926091,-2.45247093231994,
-2.4295280563586,-2.42092211318199,-2.41473061158603,-2.40900870563828,
-2.39949877201175,-2.36954676781733,-2.32584577114125,-2.30700805930769,
-2.30145832699222,-2.29787881513964,-2.29416013608815,-2.28795107984734,
-2.25943620007469,-2.21773930442969,-2.19477457467764,-2.18616601086925,
-2.17997407065333,-2.17425274676923,-2.16474614980756,-2.13488939141179,
-2.09110428883567,-2.07829060284367,-2.06924513546892,-2.06495945484263,
-2.061880061416,-2.05764571318632,-2.04887942275539,-2.00398066299054,-1.9765176231576,
-1.95834963862161,-1.95039421647341,-1.94429786304221,-1.93753582274803,
-1.92601041527089,-1.87893304191309,-1.8400010618519,-1.83311412112586,
-1.829251753799,-1.82579217605242,-1.82070344413138,-1.8073378147123,-1.76197160465683,
-1.73437690700031,-1.72103900827823,-1.71391878422196,-1.70786769452151,
-1.70045285734424,-1.68884209475638,-1.63453186031581,-1.61372033428905,
-1.60112564720196,-1.59627199375223,-1.59281360746012,-1.58882685126493,
-1.58154657646952,-1.53933447853739,-1.51257715954122),.UNSPECIFIED.);
#503=B_SPLINE_CURVE_WITH_KNOTS('',3,(#44681,#44682,#44683,#44684,#44685,
#44686,#44687,#44688,#44689,#44690,#44691,#44692,#44693,#44694,#44695,#44696,
#44697,#44698,#44699,#44700,#44701,#44702,#44703,#44704,#44705,#44706,#44707,
#44708,#44709,#44710,#44711,#44712,#44713,#44714,#44715,#44716,#44717,#44718,
#44719,#44720,#44721,#44722,#44723,#44724,#44725,#44726,#44727,#44728,#44729,
#44730,#44731,#44732,#44733,#44734,#44735,#44736,#44737,#44738,#44739,#44740,
#44741,#44742,#44743,#44744,#44745,#44746,#44747,#44748,#44749,#44750,#44751,
#44752,#44753,#44754,#44755,#44756,#44757,#44758,#44759,#44760,#44761,#44762,
#44763,#44764,#44765,#44766,#44767,#44768,#44769,#44770,#44771,#44772,#44773,
#44774,#44775,#44776,#44777,#44778,#44779,#44780,#44781,#44782,#44783,#44784,
#44785,#44786,#44787,#44788,#44789,#44790,#44791,#44792,#44793,#44794,#44795,
#44796,#44797,#44798,#44799,#44800,#44801,#44802,#44803,#44804,#44805,#44806,
#44807,#44808,#44809,#44810,#44811,#44812,#44813,#44814,#44815,#44816,#44817,
#44818,#44819,#44820,#44821,#44822,#44823,#44824,#44825,#44826,#44827,#44828,
#44829,#44830,#44831,#44832,#44833,#44834,#44835,#44836,#44837,#44838,#44839,
#44840,#44841,#44842,#44843,#44844,#44845,#44846,#44847,#44848,#44849,#44850,
#44851,#44852,#44853,#44854,#44855,#44856,#44857,#44858,#44859,#44860,#44861,
#44862),.UNSPECIFIED.,.F.,.F.,(4,2,2,2,2,2,2,2,2,2,2,2,2,2,2,2,2,2,2,2,
2,2,2,2,2,2,2,2,2,2,2,2,2,2,2,2,2,2,2,2,2,2,2,2,2,2,2,2,2,2,2,2,2,2,2,2,
2,2,2,2,2,2,2,2,2,2,2,2,2,2,2,2,2,2,2,2,2,2,2,2,2,2,2,2,2,2,2,2,2,2,4),
(-2.97128357771462,-2.96865392351007,-2.94839507124107,-2.89743779778867,
-2.87424675097357,-2.86575034232415,-2.85970887341184,-2.85343553355014,
-2.84372254817052,-2.80512921397255,-2.76888139095612,-2.75167646141285,
-2.74636299393873,-2.74289482553345,-2.73927080171485,-2.73318777092222,
-2.70540183360721,-2.66280405476377,-2.6396957081517,-2.63122186480837,
-2.62519536408187,-2.61967937212161,-2.61065280919548,-2.58399436181157,
-2.52532943588081,-2.51470033019289,-2.51022382573427,-2.50689960110064,
-2.50292240379257,-2.49533992985453,-2.46439673151686,-2.43759652774324,
-2.41661326589724,-2.40149715217623,-2.39418792858843,-2.38832206388745,
-2.38154008369257,-2.36958025763954,-2.31427702486669,-2.29306261007733,
-2.28433149290656,-2.27755752343797,-2.27379214458389,-2.27041571944382,
-2.26555014922623,-2.25315685078844,-2.20659774123285,-2.18324631269954,
-2.16697842734428,-2.15946529237677,-2.15357477231354,-2.14691174631869,
-2.13554374860428,-2.09444098992591,-2.06246445164476,-2.04632417711657,
-2.04112840198186,-2.03769134119473,-2.03404332448252,-2.02783718033924,
-1.99280148943343,-1.95636639207222,-1.93422852071963,-1.92587155874946,
-1.9198660034611,-1.91357562420648,-1.90372367178009,-1.86304824391755,
-1.82830275820345,-1.81144989803916,-1.80618357332534,-1.80273456002231,
-1.79911110429465,-1.79301662424825,-1.76473876971035,-1.72247310490631,
-1.69944253718217,-1.69097893907457,-1.68495576169298,-1.67944023333038,
-1.67040855311391,-1.64365922914048,-1.58512035514045,-1.57455119987541,
-1.57008335592917,-1.56675784628897,-1.56276826608674,-1.55513850805868,
-1.52344861547318,-1.49504695531263,-1.47753946869224),.UNSPECIFIED.);
#504=B_SPLINE_CURVE_WITH_KNOTS('',3,(#44863,#44864,#44865,#44866,#44867,
#44868,#44869,#44870,#44871,#44872,#44873,#44874,#44875,#44876,#44877,#44878,
#44879,#44880,#44881,#44882,#44883,#44884,#44885,#44886,#44887,#44888,#44889,
#44890,#44891,#44892,#44893,#44894,#44895,#44896,#44897,#44898,#44899,#44900,
#44901,#44902,#44903,#44904,#44905,#44906,#44907,#44908,#44909,#44910,#44911,
#44912,#44913,#44914,#44915,#44916,#44917,#44918,#44919,#44920,#44921,#44922,
#44923,#44924,#44925,#44926,#44927,#44928,#44929,#44930,#44931,#44932,#44933,
#44934,#44935,#44936,#44937,#44938,#44939,#44940,#44941,#44942,#44943,#44944,
#44945,#44946,#44947,#44948,#44949,#44950,#44951,#44952,#44953,#44954,#44955,
#44956,#44957,#44958,#44959,#44960,#44961,#44962,#44963,#44964,#44965,#44966,
#44967,#44968,#44969,#44970,#44971,#44972,#44973,#44974,#44975,#44976,#44977,
#44978,#44979,#44980,#44981,#44982,#44983,#44984,#44985,#44986,#44987,#44988,
#44989,#44990,#44991,#44992,#44993,#44994,#44995,#44996,#44997,#44998,#44999,
#45000,#45001,#45002,#45003,#45004,#45005,#45006,#45007,#45008,#45009,#45010,
#45011,#45012,#45013,#45014,#45015,#45016,#45017,#45018,#45019,#45020,#45021,
#45022,#45023,#45024,#45025,#45026,#45027,#45028,#45029,#45030,#45031,#45032,
#45033,#45034,#45035,#45036,#45037,#45038,#45039,#45040,#45041,#45042,#45043,
#45044,#45045,#45046,#45047,#45048,#45049,#45050,#45051,#45052),
 .UNSPECIFIED.,.F.,.F.,(4,2,2,2,2,2,2,2,2,2,2,2,2,2,2,2,2,2,2,2,2,2,2,2,
2,2,2,2,2,2,2,2,2,2,2,2,2,2,2,2,2,2,2,2,2,2,2,2,2,2,2,2,2,2,2,2,2,2,2,2,
2,2,2,2,2,2,2,2,2,2,2,2,2,2,2,2,2,2,2,2,2,2,2,2,2,2,2,2,2,2,2,2,2,2,4),
(-1.51257715954122,-1.50868742133966,-1.49533487415107,-1.48439664682859,
-1.47775337250042,-1.47162264174556,-1.4634097442554,-1.44349605745563,
-1.41156197950073,-1.37163042281252,-1.36412190088113,-1.36008640345056,
-1.35698548095647,-1.35244730746324,-1.34194205458545,-1.27645812943356,
-1.25548021491546,-1.24691136569469,-1.24072542154754,-1.23421220372519,
-1.22391623137693,-1.17835395477159,-1.13641975126835,-1.12911786017158,
-1.12512635660953,-1.12166924981505,-1.11682456796411,-1.10429140385316,
-1.0836392559053,-1.02996126523853,-1.01790672689637,-1.01036825263347,
-1.00431147151791,-0.997291145783022,-0.984467134770748,-0.935729749958118,
-0.9022517156857,-0.894560149693531,-0.890486462769247,-0.88707925026059,
-0.882398395641776,-0.870986077329699,-0.853087660077437,-0.793935948229813,
-0.781406214468887,-0.77437186552303,-0.768315389399056,-0.760793346275567,
-0.745266769469627,-0.723616522503956,-0.697810717945532,-0.667369937506699,
-0.659717484936392,-0.655651421174981,-0.652554121265546,-0.648056854209032,
-0.637807989600492,-0.622522149567441,-0.586094067756851,-0.553599773624756,
-0.543922700212964,-0.537530990548716,-0.531263006261938,-0.522236189919012,
-0.495419122025837,-0.438774520429816,-0.427067279172335,-0.422693862835207,
-0.419211562122838,-0.415404105964945,-0.408768356524173,-0.400334784303282,
-0.380534455343681,-0.322242811813613,-0.310751272000897,-0.303999848558903,
-0.297907870823549,-0.289951107422307,-0.271749399225708,-0.244199026294971,
-0.19902214586421,-0.190474022986768,-0.186282516667828,-0.182891977094015,
-0.178383628957853,-0.168052989178377,-0.152591079151827,-0.0961144860805975,
-0.079151616139969,-0.0713849303718217,-0.065307044284041,-0.0584348018970584,
-0.0512357942656692,-0.0366507069838287,-0.0182409621825525),
 .UNSPECIFIED.);
#505=B_SPLINE_CURVE_WITH_KNOTS('',3,(#45056,#45057,#45058,#45059,#45060,
#45061),.UNSPECIFIED.,.F.,.F.,(4,1,1,4),(-4.09293042013066,-3.9493215972006,
-2.96199119790045,-2.06910254442638),.UNSPECIFIED.);
#506=B_SPLINE_CURVE_WITH_KNOTS('',3,(#45065,#45066,#45067,#45068,#45069),
 .UNSPECIFIED.,.F.,.F.,(4,1,4),(0.,0.988566943725272,1.11730040836823),
 .UNSPECIFIED.);
#507=B_SPLINE_CURVE_WITH_KNOTS('',3,(#45071,#45072,#45073,#45074,#45075,
#45076,#45077,#45078,#45079,#45080,#45081,#45082,#45083,#45084,#45085,#45086,
#45087,#45088,#45089,#45090,#45091,#45092,#45093,#45094,#45095,#45096,#45097,
#45098,#45099,#45100,#45101,#45102,#45103,#45104,#45105,#45106,#45107,#45108,
#45109,#45110,#45111,#45112,#45113,#45114,#45115,#45116,#45117,#45118,#45119,
#45120,#45121,#45122,#45123,#45124,#45125,#45126,#45127,#45128,#45129,#45130,
#45131,#45132,#45133,#45134,#45135,#45136,#45137,#45138,#45139,#45140,#45141,
#45142,#45143,#45144,#45145,#45146,#45147,#45148,#45149,#45150,#45151,#45152,
#45153,#45154,#45155,#45156,#45157,#45158,#45159,#45160,#45161,#45162,#45163,
#45164,#45165,#45166,#45167,#45168,#45169,#45170,#45171,#45172,#45173,#45174,
#45175,#45176,#45177,#45178,#45179,#45180,#45181,#45182,#45183,#45184,#45185,
#45186,#45187,#45188,#45189,#45190,#45191,#45192,#45193,#45194,#45195,#45196,
#45197,#45198,#45199,#45200,#45201,#45202,#45203,#45204,#45205,#45206,#45207,
#45208,#45209,#45210,#45211,#45212,#45213,#45214,#45215,#45216,#45217,#45218,
#45219,#45220,#45221,#45222,#45223,#45224,#45225,#45226,#45227,#45228,#45229,
#45230,#45231,#45232,#45233,#45234,#45235,#45236,#45237,#45238,#45239,#45240,
#45241,#45242,#45243,#45244,#45245,#45246,#45247,#45248,#45249,#45250,#45251,
#45252,#45253,#45254,#45255,#45256,#45257,#45258,#45259,#45260,#45261,#45262,
#45263,#45264,#45265,#45266,#45267,#45268,#45269,#45270,#45271,#45272,#45273,
#45274,#45275,#45276,#45277,#45278,#45279,#45280,#45281),.UNSPECIFIED.,
 .F.,.F.,(4,3,3,3,3,3,3,3,3,3,3,3,3,3,3,3,3,3,3,3,3,3,3,3,3,3,3,3,3,3,3,
3,3,3,3,3,3,3,3,3,3,3,3,3,3,3,3,3,3,3,3,3,3,3,3,3,3,3,3,3,3,3,3,3,3,3,3,
3,3,3,4),(1.11730040836823,1.21037388007188,1.30621888099421,1.39909202481253,
1.49192328569137,1.58474107162718,1.67757377046851,1.77050322392294,1.86349120514412,
1.95661989431377,1.97713388745054,2.07263487628453,2.16800729129127,2.26771898377683,
2.36292314190516,2.45809521423212,2.55326139142238,2.64844785131489,2.74373567178762,
2.83908288421244,2.9345736252384,2.9657008311758,3.0612101519017,3.15659374321842,
3.25630299717875,3.35152542041667,3.44671833584018,3.54190791950783,3.63712033682998,
3.7324378035997,3.82781683687417,3.92334239041227,3.95426777490106,4.04949425818523,
4.14459011568218,4.2443706910502,4.33929523863208,4.43418719540974,4.52907312140792,
4.62397956378642,4.71898930590132,4.81405924567905,4.90927623089053,4.94283471862632,
5.03821711679297,5.13347079444595,5.23321215293416,5.32829814620465,5.42335253563372,
5.51840167611464,5.61347191028934,5.70864539355769,5.80387923767303,5.89925900834736,
5.93140166235159,6.02677164553458,6.12201312336192,6.22175755870129,6.31683198767932,
6.41187507260355,6.50691318440943,6.60197268202006,6.6971359286251,6.79235981409918,
6.88773012583267,6.91996860607685,7.02073121797426,7.12120864243437,7.22151462151028,
7.32158735870522,7.40048571527184),.UNSPECIFIED.);
#508=B_SPLINE_CURVE_WITH_KNOTS('',3,(#45283,#45284,#45285,#45286,#45287,
#45288,#45289,#45290,#45291,#45292,#45293,#45294,#45295,#45296,#45297,#45298,
#45299,#45300,#45301,#45302,#45303,#45304,#45305,#45306,#45307,#45308,#45309,
#45310,#45311,#45312,#45313,#45314,#45315,#45316,#45317,#45318,#45319,#45320,
#45321,#45322,#45323,#45324,#45325,#45326,#45327,#45328,#45329,#45330,#45331,
#45332,#45333,#45334,#45335,#45336,#45337,#45338,#45339,#45340,#45341,#45342,
#45343,#45344,#45345,#45346,#45347,#45348,#45349,#45350,#45351,#45352,#45353,
#45354,#45355,#45356,#45357,#45358,#45359,#45360,#45361,#45362,#45363,#45364,
#45365,#45366,#45367,#45368,#45369,#45370,#45371,#45372,#45373,#45374,#45375,
#45376,#45377,#45378,#45379,#45380,#45381,#45382,#45383,#45384,#45385,#45386,
#45387,#45388,#45389,#45390,#45391,#45392,#45393,#45394,#45395,#45396,#45397,
#45398,#45399,#45400,#45401,#45402,#45403,#45404,#45405,#45406,#45407,#45408,
#45409,#45410,#45411,#45412,#45413,#45414,#45415,#45416,#45417,#45418,#45419,
#45420,#45421,#45422,#45423,#45424,#45425,#45426,#45427,#45428,#45429,#45430,
#45431,#45432,#45433,#45434,#45435,#45436,#45437,#45438,#45439,#45440,#45441,
#45442,#45443,#45444,#45445,#45446,#45447,#45448,#45449,#45450,#45451,#45452,
#45453,#45454,#45455,#45456,#45457,#45458,#45459,#45460,#45461,#45462,#45463,
#45464,#45465,#45466,#45467,#45468,#45469,#45470,#45471,#45472,#45473,#45474,
#45475,#45476,#45477,#45478,#45479,#45480,#45481,#45482,#45483,#45484,#45485,
#45486,#45487,#45488,#45489,#45490),.UNSPECIFIED.,.F.,.F.,(4,3,3,3,3,3,
3,3,3,3,3,3,3,3,3,3,3,3,3,3,3,3,3,3,3,3,3,3,3,3,3,3,3,3,3,3,3,3,3,3,3,3,
3,3,3,3,3,3,3,3,3,3,3,3,3,3,3,3,3,3,3,3,3,3,3,3,3,3,3,4),(7.40048571554782,
7.49937034306215,7.60166164474714,7.70089351874772,7.80471453427491,7.90853554980211,
8.00389380426277,8.09912321670652,8.19887062630912,8.29393223320934,8.38896224533412,
8.48398704975616,8.57903302133985,8.67418248971306,8.76939243491052,8.86474867946115,
8.89710249352738,8.99245676209535,9.08768218520464,9.18743059171064,9.28248823090432,
9.3775142919929,9.47253516730274,9.56757723697213,9.66272286636021,9.75792900460433,
9.85328152193589,9.88566943725264,9.98101947654195,10.0762405859611,10.1759900603382,
10.2710432057759,10.3660647165878,10.4610809908222,10.5561184142973,10.651259355886,
10.7464607767975,10.841808571773,10.8742363809779,10.9695899428316,11.064814624289,
11.1645632118408,11.2596200269402,11.3546452353564,11.4496652304129,11.5447063932207,
11.6398510808652,11.735056256063,11.8304077864152,11.8628033247032,11.9581560172067,
12.0533798239388,12.1531286295,12.2481845629618,12.3432088891243,12.4382280024644,
12.5332682852472,12.6284121003789,12.7236164064074,12.8189670798418,12.8513702684284,
12.9453321463137,13.039144360993,13.1328721337901,13.2265434258128,13.3201861320926,
13.4138735216964,13.5075805203644,13.60140729215,13.6836710227274),
 .UNSPECIFIED.);
#509=B_SPLINE_CURVE_WITH_KNOTS('',3,(#45492,#45493,#45494,#45495,#45496,
#45497,#45498,#45499,#45500,#45501,#45502),.UNSPECIFIED.,.F.,.F.,(4,1,1,
1,1,1,1,1,4),(13.6836710227274,13.8399372121537,14.828504155879,15.8170710996042,
16.8056380433295,17.7942049870548,18.78277193078,19.7713388745053,19.966856329907),
 .UNSPECIFIED.);
#510=B_SPLINE_CURVE_WITH_KNOTS('',3,(#45504,#45505,#45506,#45507,#45508,
#45509,#45510,#45511,#45512,#45513,#45514,#45515,#45516,#45517,#45518,#45519,
#45520,#45521,#45522,#45523,#45524,#45525,#45526,#45527,#45528,#45529,#45530,
#45531,#45532,#45533,#45534,#45535,#45536,#45537,#45538,#45539,#45540,#45541,
#45542,#45543,#45544,#45545,#45546,#45547,#45548,#45549,#45550,#45551,#45552,
#45553,#45554,#45555,#45556,#45557,#45558,#45559,#45560,#45561,#45562,#45563,
#45564,#45565,#45566,#45567,#45568,#45569,#45570,#45571,#45572,#45573,#45574,
#45575,#45576,#45577,#45578,#45579,#45580,#45581,#45582,#45583,#45584,#45585,
#45586,#45587,#45588,#45589,#45590,#45591,#45592,#45593,#45594,#45595,#45596,
#45597,#45598,#45599,#45600,#45601,#45602,#45603,#45604,#45605,#45606,#45607,
#45608,#45609,#45610,#45611,#45612,#45613,#45614,#45615,#45616,#45617,#45618,
#45619,#45620,#45621,#45622,#45623,#45624,#45625,#45626,#45627,#45628,#45629,
#45630,#45631,#45632,#45633,#45634,#45635,#45636,#45637,#45638,#45639,#45640,
#45641,#45642,#45643,#45644,#45645,#45646,#45647,#45648,#45649,#45650,#45651,
#45652,#45653,#45654,#45655,#45656,#45657,#45658,#45659,#45660,#45661,#45662,
#45663,#45664,#45665,#45666,#45667,#45668,#45669,#45670,#45671,#45672,#45673,
#45674,#45675,#45676,#45677,#45678,#45679,#45680,#45681,#45682,#45683,#45684,
#45685,#45686,#45687,#45688,#45689,#45690,#45691,#45692,#45693,#45694,#45695,
#45696,#45697,#45698,#45699,#45700,#45701,#45702,#45703,#45704,#45705,#45706,
#45707,#45708,#45709,#45710,#45711,#45712,#45713,#45714),.UNSPECIFIED.,
 .F.,.F.,(4,3,3,3,3,3,3,3,3,3,3,3,3,3,3,3,3,3,3,3,3,3,3,3,3,3,3,3,3,3,3,
3,3,3,3,3,3,3,3,3,3,3,3,3,3,3,3,3,3,3,3,3,3,3,3,3,3,3,3,3,3,3,3,3,3,3,3,
3,3,3,4),(19.966856329907,20.0606883778646,20.1544324765222,20.2481305658949,
20.3418104960079,20.4355000925652,20.5292828743492,20.6231185270144,20.7170997179296,
20.7599058182306,20.8552583879036,20.9504820669485,21.0502309038244,21.145286698325,
21.2403108816755,21.3353298485237,21.4303699813028,21.5255136419971,21.6207177908408,
21.7160683042774,21.7484727619558,21.8438253317088,21.9390490108222,22.0387978476796,
22.1338536422197,22.2288778255989,22.3238967924648,22.4189369252509,22.5140805859356,
22.60928473476,22.7046352481631,22.7370397056811,22.8323922766482,22.9276159569972,
23.0273647935483,23.1224205893681,23.2174447740405,23.3124637422117,23.4075038763132,
23.5026475383213,23.5978516884751,23.6932022032059,23.7256066494064,23.8209592196533,
23.9161828992727,24.0159317360051,24.110987531078,24.2060117149986,24.3010306824142,
24.3960708157573,24.4912144770068,24.5864186264011,24.6817691403775,24.7141735931316,
24.8095261634606,24.9047498431618,25.0044986798737,25.0995544750262,25.1945786590253,
25.2895976265183,25.3846377599378,25.4797814212618,25.5749855707292,25.6703360847763,
25.7027405368569,25.8008404154051,25.8987825103485,25.9965488931931,26.0942114708792,
26.1917715987827,26.2500416370866),.UNSPECIFIED.);
#511=B_SPLINE_CURVE_WITH_KNOTS('',3,(#45716,#45717,#45718,#45719,#45720,
#45721,#45722,#45723,#45724,#45725,#45726,#45727,#45728,#45729,#45730,#45731,
#45732,#45733,#45734,#45735,#45736,#45737,#45738,#45739,#45740,#45741,#45742,
#45743,#45744,#45745,#45746,#45747,#45748,#45749,#45750,#45751,#45752,#45753,
#45754,#45755,#45756,#45757,#45758,#45759,#45760,#45761,#45762,#45763,#45764,
#45765,#45766,#45767,#45768,#45769,#45770,#45771,#45772,#45773,#45774,#45775,
#45776,#45777,#45778,#45779,#45780,#45781,#45782,#45783,#45784,#45785,#45786,
#45787,#45788,#45789,#45790,#45791,#45792,#45793,#45794,#45795,#45796,#45797,
#45798,#45799,#45800,#45801,#45802,#45803,#45804,#45805,#45806,#45807,#45808,
#45809,#45810,#45811,#45812,#45813,#45814,#45815,#45816,#45817,#45818,#45819,
#45820,#45821,#45822,#45823,#45824,#45825,#45826,#45827,#45828,#45829,#45830,
#45831,#45832,#45833,#45834,#45835,#45836,#45837,#45838,#45839,#45840,#45841,
#45842,#45843,#45844,#45845,#45846,#45847,#45848,#45849,#45850,#45851,#45852,
#45853,#45854,#45855,#45856,#45857,#45858,#45859,#45860,#45861,#45862,#45863,
#45864,#45865,#45866,#45867,#45868,#45869,#45870,#45871,#45872,#45873,#45874,
#45875,#45876,#45877,#45878,#45879,#45880,#45881,#45882,#45883,#45884,#45885,
#45886,#45887,#45888,#45889,#45890,#45891,#45892,#45893,#45894,#45895,#45896,
#45897,#45898,#45899,#45900,#45901,#45902,#45903,#45904,#45905,#45906,#45907,
#45908,#45909,#45910,#45911,#45912,#45913,#45914,#45915,#45916,#45917,#45918,
#45919,#45920,#45921,#45922,#45923,#45924,#45925,#45926),.UNSPECIFIED.,
 .F.,.F.,(4,3,3,3,3,3,3,3,3,3,3,3,3,3,3,3,3,3,3,3,3,3,3,3,3,3,3,3,3,3,3,
3,3,3,3,3,3,3,3,3,3,3,3,3,3,3,3,3,3,3,3,3,3,3,3,3,3,3,3,3,3,3,3,3,3,3,3,
3,3,3,4),(26.2500416373359,26.3519613122933,26.4542712901962,26.5567882928527,
26.6596074482971,26.6913074805822,26.7866600509523,26.8818837306959,26.9816325673974,
27.0766883625954,27.1717125466414,27.2667315141822,27.3617716476502,27.4569153090236,
27.5521194585415,27.6474699726396,27.6798744243074,27.7752269946991,27.8704506744644,
27.9701995111604,28.0652553063801,28.1602794904476,28.25529845801,28.3503385914995,
28.4454822528942,28.5406864024331,28.6360369165519,28.6684413680327,28.7637939384417,
28.8590176182246,28.9587664549163,29.0538222501544,29.1488464342407,29.2438654018219,
29.3389055353305,29.4340491967444,29.5292533463028,29.624603860441,29.6570083117579,
29.752360882151,29.8475845619179,29.9473333986136,30.0423891938351,30.1374133779048,
30.2324323454692,30.3274724789609,30.422616140358,30.5178202898994,30.6131708040208,
30.6455752554832,30.7409278258807,30.8361515056521,30.9359003423466,31.0309561375726,
31.1259803216467,31.2209992892157,31.3160394227119,31.4111830841135,31.5063872336593,
31.6017377477851,31.6341421992085,31.7283920093595,31.822513801464,31.9165313934101,
32.0104926734926,32.1044252862533,32.1983568418308,32.2923673015784,32.386420948748,
32.4806113479254,32.5332269440593),.UNSPECIFIED.);
#512=B_SPLINE_CURVE_WITH_KNOTS('',3,(#45928,#45929,#45930,#45931,#45932,
#45933,#45934,#45935,#45936,#45937,#45938,#45939,#45940,#45941,#45942,#45943,
#45944,#45945,#45946,#45947,#45948,#45949,#45950,#45951,#45952,#45953,#45954,
#45955,#45956,#45957,#45958,#45959,#45960,#45961,#45962,#45963,#45964,#45965,
#45966,#45967,#45968,#45969,#45970,#45971,#45972,#45973,#45974,#45975,#45976,
#45977,#45978,#45979,#45980,#45981,#45982,#45983,#45984,#45985,#45986,#45987,
#45988,#45989,#45990,#45991,#45992,#45993,#45994,#45995,#45996,#45997,#45998,
#45999,#46000,#46001,#46002,#46003,#46004,#46005,#46006,#46007,#46008,#46009,
#46010,#46011,#46012,#46013,#46014,#46015,#46016,#46017,#46018,#46019,#46020,
#46021,#46022,#46023,#46024,#46025,#46026,#46027,#46028,#46029,#46030,#46031,
#46032,#46033,#46034,#46035,#46036,#46037,#46038,#46039,#46040,#46041,#46042,
#46043,#46044,#46045,#46046,#46047,#46048,#46049,#46050,#46051,#46052,#46053,
#46054,#46055,#46056,#46057,#46058,#46059,#46060,#46061,#46062,#46063,#46064,
#46065,#46066,#46067,#46068,#46069,#46070,#46071,#46072,#46073,#46074,#46075,
#46076,#46077,#46078,#46079,#46080,#46081,#46082,#46083,#46084,#46085,#46086,
#46087,#46088,#46089,#46090,#46091,#46092,#46093,#46094,#46095,#46096,#46097,
#46098,#46099,#46100,#46101,#46102,#46103,#46104,#46105,#46106,#46107,#46108,
#46109,#46110,#46111,#46112,#46113,#46114,#46115,#46116,#46117,#46118,#46119,
#46120,#46121,#46122,#46123,#46124,#46125,#46126,#46127,#46128,#46129,#46130,
#46131,#46132,#46133,#46134,#46135,#46136,#46137,#46138),.UNSPECIFIED.,
 .F.,.F.,(4,3,3,3,3,3,3,3,3,3,3,3,3,3,3,3,3,3,3,3,3,3,3,3,3,3,3,3,3,3,3,
3,3,3,3,3,3,3,3,3,3,3,3,3,3,3,3,3,3,3,3,3,3,3,3,3,3,3,3,3,3,3,3,3,3,3,3,
3,3,3,4),(32.5332269442662,32.6227091429337,32.7180617133311,32.8132853931022,
32.9130342297968,33.0080900250228,33.1031142090968,33.1981331766657,33.2931733101617,
33.3883169715633,33.4835211211092,33.578871635235,33.611276086659,33.7066286570568,
33.8018523368284,33.9016011735229,33.9966569687493,34.0916811528238,34.1867001203931,
34.2817402538897,34.3768839152916,34.4720880648378,34.567438578964,34.5998430303843,
34.6951956007822,34.790419280554,34.8901681172485,34.985223912475,35.0802480965497,
35.1752670641192,35.270307197616,35.3654508590182,35.4606550085646,35.556005522691,
35.5884099741095,35.6837625445072,35.7789862242788,35.8787350609733,35.9737908561996,
36.068815040274,36.1638340078432,36.2588741413398,36.3540178027417,36.4492219522878,
36.544572466414,36.5769769178348,36.6723294882327,36.7675531680045,36.8673020046989,
36.9623577999254,37.057381984,37.1524009515694,37.247441085066,37.3425847464681,
37.4377888960145,37.5331394101408,37.5655438615601,37.660896431958,37.7561201117295,
37.855868948424,37.9509247436504,38.0459489277249,38.1409678952943,38.2360080287909,
38.3311516901928,38.4263558397392,38.5217063538654,38.5541108052853,38.6750958169878,
38.7939679214662,38.8164120719258),.UNSPECIFIED.);
#513=B_SPLINE_CURVE_WITH_KNOTS('',3,(#46140,#46141,#46142,#46143,#46144,
#46145,#46146,#46147,#46148,#46149),.UNSPECIFIED.,.F.,.F.,(4,1,1,1,1,1,
1,4),(38.8164122514458,39.5426777490106,40.5312446927359,41.5198116364611,
42.5083785801864,43.4969455239117,44.4855124676369,45.0995975586253),
 .UNSPECIFIED.);
#514=B_SPLINE_CURVE_WITH_KNOTS('',3,(#46151,#46152,#46153,#46154,#46155,
#46156,#46157,#46158,#46159,#46160),.UNSPECIFIED.,.F.,.F.,(4,1,1,1,1,1,
1,4),(45.0995975586253,45.4740794113622,46.4626463550875,47.4512132988127,
48.439780242538,49.4283471862633,50.4169141299885,51.3827800491886),
 .UNSPECIFIED.);
#515=B_SPLINE_CURVE_WITH_KNOTS('',3,(#46162,#46163,#46164,#46165,#46166,
#46167,#46168,#46169,#46170,#46171,#46172,#46173,#46174,#46175,#46176,#46177,
#46178,#46179,#46180,#46181,#46182,#46183,#46184,#46185,#46186,#46187,#46188,
#46189,#46190,#46191,#46192,#46193,#46194,#46195,#46196,#46197,#46198,#46199,
#46200,#46201,#46202,#46203,#46204,#46205,#46206,#46207,#46208,#46209,#46210,
#46211,#46212,#46213,#46214,#46215,#46216,#46217,#46218,#46219,#46220,#46221,
#46222,#46223,#46224,#46225,#46226,#46227,#46228,#46229,#46230,#46231,#46232,
#46233,#46234,#46235,#46236,#46237,#46238,#46239,#46240,#46241,#46242,#46243,
#46244,#46245,#46246,#46247,#46248,#46249,#46250,#46251,#46252,#46253,#46254,
#46255,#46256,#46257,#46258,#46259,#46260,#46261,#46262,#46263,#46264,#46265,
#46266,#46267,#46268,#46269,#46270,#46271,#46272,#46273,#46274,#46275,#46276,
#46277,#46278,#46279,#46280,#46281,#46282,#46283,#46284,#46285,#46286,#46287,
#46288,#46289,#46290,#46291,#46292,#46293,#46294,#46295,#46296,#46297,#46298,
#46299,#46300,#46301,#46302,#46303,#46304,#46305,#46306,#46307,#46308,#46309,
#46310,#46311,#46312,#46313,#46314,#46315,#46316,#46317,#46318,#46319,#46320,
#46321,#46322,#46323,#46324,#46325,#46326,#46327,#46328,#46329,#46330,#46331,
#46332,#46333,#46334,#46335,#46336,#46337,#46338,#46339,#46340,#46341,#46342,
#46343,#46344,#46345,#46346,#46347,#46348,#46349,#46350,#46351,#46352,#46353,
#46354,#46355,#46356,#46357,#46358,#46359,#46360,#46361,#46362,#46363,#46364,
#46365,#46366,#46367,#46368,#46369,#46370,#46371,#46372),.UNSPECIFIED.,
 .F.,.F.,(4,3,3,3,3,3,3,3,3,3,3,3,3,3,3,3,3,3,3,3,3,3,3,3,3,3,3,3,3,3,3,
3,3,3,3,3,3,3,3,3,3,3,3,3,3,3,3,3,3,3,3,3,3,3,3,3,3,3,3,3,3,3,3,3,3,3,3,
3,3,3,4),(51.3827828658049,51.4054810737138,51.5008336447139,51.5960573250891,
51.6958061616329,51.7908619574615,51.8858861421364,51.9809051103038,52.075945244395,
52.1710889063835,52.2662930565123,52.36164357121,52.394048017439,52.4894005871162,
52.5846242661698,52.6843731030441,52.7794288975638,52.8744530809372,52.969472047812,
53.0645121806213,53.1596558413507,53.2548599902323,53.3502105037107,53.3826149611643,
53.4779675308754,53.5731912099506,53.672940046818,53.7679958413289,53.8630200246824,
53.9580389915263,54.053079124294,54.148222784966,54.2434269337809,54.3387774471797,
54.3711819048896,54.4665344793659,54.5617581632274,54.6615069989008,54.7565627982158,
54.8515869863696,54.946605958004,55.0416460955462,55.136789760942,55.2319939144568,
55.327344432481,55.3597488486148,55.4551014129466,55.5503250866643,55.6500739248737,
55.7451297141187,55.8401538922509,55.9351728539245,56.0302129815792,56.1253566372516,
56.2205607811269,56.3159112897158,56.3483157923401,56.4436683605826,56.5388920381325,
56.6386408753741,56.7336966682308,56.828720849887,56.9237398149926,57.0187799459837,
57.1139236048325,57.2091277517951,57.3044782633144,57.3368827360654,57.4485132464071,
57.5591246734767,57.6659679604612),.UNSPECIFIED.);
#516=B_SPLINE_CURVE_WITH_KNOTS('',3,(#46374,#46375,#46376,#46377,#46378,
#46379,#46380,#46381,#46382,#46383),.UNSPECIFIED.,.F.,.F.,(4,1,1,1,1,1,
1,4),(57.6659681729845,58.3254496797906,59.3140166235159,60.3025835672412,
61.2911505109664,62.2797174546917,63.268284398417,63.9491534801641),
 .UNSPECIFIED.);
#517=B_SPLINE_CURVE_WITH_KNOTS('',3,(#46385,#46386,#46387,#46388,#46389,
#46390,#46391,#46392,#46393,#46394),.UNSPECIFIED.,.F.,.F.,(4,1,1,1,1,1,
1,4),(63.9491534801641,64.2568513421422,65.2454182858675,66.2339852295928,
67.222552173318,68.2111191170433,69.1996860607685,69.4794631267919),
 .UNSPECIFIED.);
#518=B_SPLINE_CURVE_WITH_KNOTS('',3,(#46398,#46399,#46400,#46401,#46402,
#46403,#46404,#46405,#46406,#46407,#46408,#46409,#46410,#46411,#46412,#46413,
#46414,#46415,#46416,#46417,#46418,#46419,#46420,#46421,#46422,#46423,#46424,
#46425,#46426,#46427,#46428,#46429,#46430,#46431,#46432,#46433,#46434,#46435,
#46436,#46437,#46438,#46439,#46440,#46441,#46442,#46443,#46444,#46445,#46446,
#46447,#46448,#46449,#46450,#46451,#46452,#46453,#46454,#46455,#46456,#46457,
#46458,#46459,#46460,#46461,#46462,#46463,#46464,#46465,#46466,#46467,#46468,
#46469,#46470,#46471,#46472,#46473,#46474,#46475,#46476,#46477,#46478,#46479,
#46480,#46481,#46482,#46483,#46484,#46485,#46486,#46487,#46488,#46489,#46490,
#46491,#46492,#46493,#46494,#46495,#46496,#46497,#46498,#46499,#46500,#46501,
#46502,#46503,#46504,#46505,#46506,#46507,#46508,#46509,#46510,#46511,#46512,
#46513,#46514,#46515,#46516,#46517,#46518,#46519,#46520,#46521,#46522,#46523,
#46524,#46525,#46526,#46527,#46528,#46529,#46530,#46531,#46532,#46533,#46534,
#46535,#46536,#46537,#46538,#46539,#46540,#46541,#46542,#46543,#46544,#46545,
#46546,#46547,#46548,#46549,#46550,#46551),.UNSPECIFIED.,.F.,.F.,(4,3,3,
3,3,3,3,3,3,3,3,3,3,3,3,3,3,3,3,3,3,3,3,3,3,3,3,3,3,3,3,3,3,3,3,3,3,3,3,
3,3,3,3,3,3,3,3,3,3,3,3,4),(-71.5480958397728,-71.4478687915014,-71.3473161830486,
-71.2465915735931,-71.1455739445365,-71.0877887496107,-70.9922715804326,
-70.8968826481691,-70.7973296109368,-70.702108211632,-70.6069187283835,
-70.5117349944208,-70.4165308556829,-70.3212255530631,-70.2258607810251,
-70.1303531882947,-70.1004583503106,-70.004935306632,-69.9095376969293,
-69.8099864786894,-69.7147494053626,-69.6195416955273,-69.5243371935969,
-69.4291097545351,-69.3337774799512,-69.2383835718144,-69.142843853146,
-69.1131279510104,-69.0178865528629,-68.922775479434,-68.8231532384685,
-68.7282128188874,-68.633304840629,-68.5384027636419,-68.4434800606417,
-68.3484542673785,-68.2533682026849,-68.1581358107866,-68.1257975517103,
-68.0303999276791,-67.9351307097886,-67.8355477651162,-67.7404455532529,
-67.6453747884525,-67.5503091374064,-67.4552222789518,-67.360032376824,
-67.2647820395354,-67.1693864892511,-67.1384671524101,-67.0084331297282,
-66.9247834919266),.UNSPECIFIED.);
#519=B_SPLINE_CURVE_WITH_KNOTS('',3,(#46553,#46554,#46555,#46556,#46557,
#46558,#46559,#46560,#46561,#46562),.UNSPECIFIED.,.F.,.F.,(4,1,1,1,1,1,
1,4),(-66.9247821671427,-66.15113675311,-65.1638063538098,-64.1764759545097,
-63.1891455552095,-62.2018151559094,-61.2144847566092,-60.641598184747),
 .UNSPECIFIED.);
#520=B_SPLINE_CURVE_WITH_KNOTS('',3,(#46564,#46565,#46566,#46567,#46568,
#46569,#46570,#46571,#46572,#46573),.UNSPECIFIED.,.F.,.F.,(4,1,1,1,1,1,
1,4),(-60.641598184747,-60.2271543573091,-59.2398239580089,-58.2524935587088,
-57.2651631594086,-56.2778327601085,-55.2905023608083,-54.3584128775674),
 .UNSPECIFIED.);
#521=B_SPLINE_CURVE_WITH_KNOTS('',3,(#46575,#46576,#46577,#46578,#46579,
#46580,#46581,#46582,#46583,#46584,#46585),.UNSPECIFIED.,.F.,.F.,(4,1,1,
1,1,1,1,1,4),(-54.3584128775674,-54.3031719615082,-53.315841562208,-52.3285111629079,
-51.3411807636077,-50.3538503643076,-49.3665199650074,-48.3791895657073,
-48.0752275703878),.UNSPECIFIED.);
#522=B_SPLINE_CURVE_WITH_KNOTS('',3,(#46587,#46588,#46589,#46590,#46591,
#46592,#46593,#46594,#46595,#46596),.UNSPECIFIED.,.F.,.F.,(4,1,1,1,1,1,
1,4),(-48.0752275703878,-47.3918591664071,-46.404528767107,-45.4171983678069,
-44.4298679685067,-43.4425375692066,-42.4552071699064,-41.7920422632082),
 .UNSPECIFIED.);
#523=B_SPLINE_CURVE_WITH_KNOTS('',3,(#46598,#46599,#46600,#46601,#46602,
#46603,#46604,#46605,#46606,#46607,#46608),.UNSPECIFIED.,.F.,.F.,(4,1,1,
1,1,1,1,1,4),(-41.7920422632082,-41.4678767706063,-40.4805463713061,-39.4932159720059,
-38.5058855727058,-37.5185551734057,-36.5312247741055,-35.5438943748054,
-35.5088569560286),.UNSPECIFIED.);
#524=B_SPLINE_CURVE_WITH_KNOTS('',3,(#46610,#46611,#46612,#46613,#46614,
#46615,#46616,#46617,#46618,#46619),.UNSPECIFIED.,.F.,.F.,(4,1,1,1,1,1,
1,4),(-35.5088569560286,-34.5565639755052,-33.5692335762051,-32.5819031769049,
-31.5945727776048,-30.6072423783046,-29.6199119790045,-29.225671648849),
 .UNSPECIFIED.);
#525=B_SPLINE_CURVE_WITH_KNOTS('',3,(#46621,#46622,#46623,#46624,#46625,
#46626,#46627,#46628,#46629,#46630),.UNSPECIFIED.,.F.,.F.,(4,1,1,1,1,1,
1,4),(-29.225671648849,-28.6325815797043,-27.6452511804042,-26.657920781104,
-25.6705903818039,-24.6832599825037,-23.6959295832036,-22.9424863416694),
 .UNSPECIFIED.);
#526=B_SPLINE_CURVE_WITH_KNOTS('',3,(#46632,#46633,#46634,#46635,#46636,
#46637,#46638,#46639,#46640,#46641,#46642),.UNSPECIFIED.,.F.,.F.,(4,1,1,
1,1,1,1,1,4),(-22.9424863416694,-22.7085991839034,-21.7212687846033,-20.7339383853031,
-19.746607986003,-18.7592775867028,-17.7719471874027,-16.7846167881025,
-16.6593010344898),.UNSPECIFIED.);
#527=B_SPLINE_CURVE_WITH_KNOTS('',3,(#46644,#46645,#46646,#46647,#46648,
#46649,#46650,#46651,#46652,#46653,#46654,#46655,#46656,#46657,#46658,#46659,
#46660,#46661,#46662,#46663,#46664,#46665,#46666,#46667,#46668,#46669,#46670,
#46671,#46672,#46673,#46674,#46675,#46676,#46677,#46678,#46679,#46680,#46681,
#46682,#46683,#46684,#46685,#46686,#46687,#46688,#46689,#46690,#46691,#46692,
#46693,#46694,#46695,#46696,#46697,#46698,#46699,#46700,#46701,#46702,#46703,
#46704,#46705,#46706,#46707,#46708,#46709,#46710,#46711,#46712,#46713,#46714,
#46715,#46716,#46717,#46718,#46719,#46720,#46721,#46722,#46723,#46724,#46725,
#46726,#46727,#46728,#46729,#46730,#46731,#46732,#46733,#46734,#46735,#46736,
#46737,#46738,#46739,#46740,#46741,#46742,#46743,#46744,#46745,#46746,#46747,
#46748,#46749,#46750,#46751,#46752,#46753,#46754,#46755,#46756,#46757,#46758,
#46759,#46760,#46761,#46762,#46763,#46764,#46765,#46766,#46767,#46768,#46769,
#46770,#46771,#46772,#46773,#46774,#46775,#46776,#46777,#46778,#46779,#46780,
#46781,#46782,#46783,#46784,#46785,#46786,#46787,#46788,#46789,#46790,#46791,
#46792,#46793,#46794,#46795,#46796,#46797,#46798,#46799,#46800,#46801,#46802,
#46803,#46804,#46805,#46806,#46807,#46808,#46809,#46810,#46811,#46812,#46813,
#46814,#46815,#46816,#46817,#46818,#46819,#46820,#46821,#46822,#46823,#46824,
#46825,#46826,#46827,#46828,#46829,#46830,#46831,#46832,#46833,#46834,#46835,
#46836,#46837,#46838,#46839,#46840,#46841,#46842,#46843,#46844,#46845,#46846,
#46847,#46848,#46849,#46850,#46851,#46852,#46853,#46854),.UNSPECIFIED.,
 .F.,.F.,(4,3,3,3,3,3,3,3,3,3,3,3,3,3,3,3,3,3,3,3,3,3,3,3,3,3,3,3,3,3,3,
3,3,3,3,3,3,3,3,3,3,3,3,3,3,3,3,3,3,3,3,3,3,3,3,3,3,3,3,3,3,3,3,3,3,3,3,
3,3,3,4),(-16.6593010344898,-16.5653248924565,-16.4693200794998,-16.3755301668361,
-16.281777908926,-16.1880355175729,-16.0903482353803,-15.9964879999612,
-15.9025665271193,-15.8085079323049,-15.7972863888024,-15.7019189811482,
-15.6066801580444,-15.5070896369767,-15.4120180367218,-15.316977895839,
-15.2219428405017,-15.1268865089978,-15.0317268581315,-14.9365066464886,
-14.8411407847332,-14.8099559895022,-14.7145884131069,-14.6193494200575,
-14.5197589413256,-14.4246871693757,-14.3296468565278,-14.2346116291798,
-14.1395551258434,-14.0443953043764,-13.9491749226522,-13.8538088929973,
-13.8226255902021,-13.727258549964,-13.6320200938329,-13.5324294809666,
-13.4373582439689,-13.3423184642153,-13.2472837674279,-13.1522277914397,
-13.0570684896125,-12.9618486236562,-12.8664830997774,-12.8352951909019,
-12.7399276379914,-12.6446886719872,-12.5450981869391,-12.4500264506047,
-12.3549861764143,-12.2599509906954,-12.1648945318917,-12.0697347589848,
-11.9745144282059,-11.8791484525789,-11.8479647916018,-11.7525963589307,
-11.6573565044856,-11.5577662404626,-11.4626936006782,-11.3676524195072,
-11.2726163244718,-11.1775589552082,-11.0823982752983,-10.9871770384881,
-10.8918101658113,-10.8606343923016,-10.7600650610283,-10.6597728389421,
-10.5596465466219,-10.4597437159183,-10.3761157274923),.UNSPECIFIED.);
#528=B_SPLINE_CURVE_WITH_KNOTS('',3,(#46855,#46856,#46857,#46858,#46859,
#46860,#46861,#46862,#46863,#46864,#46865,#46866,#46867,#46868,#46869,#46870,
#46871,#46872,#46873,#46874,#46875,#46876,#46877,#46878,#46879,#46880,#46881,
#46882,#46883,#46884,#46885,#46886,#46887,#46888,#46889,#46890,#46891,#46892,
#46893,#46894,#46895,#46896,#46897,#46898,#46899,#46900,#46901,#46902,#46903,
#46904,#46905,#46906,#46907,#46908,#46909,#46910,#46911,#46912,#46913,#46914,
#46915,#46916,#46917,#46918,#46919,#46920,#46921,#46922,#46923,#46924,#46925,
#46926,#46927,#46928,#46929,#46930,#46931,#46932,#46933,#46934,#46935,#46936,
#46937,#46938,#46939,#46940,#46941,#46942,#46943,#46944,#46945,#46946,#46947,
#46948,#46949,#46950,#46951,#46952,#46953,#46954,#46955,#46956,#46957,#46958,
#46959,#46960,#46961,#46962,#46963,#46964,#46965,#46966,#46967,#46968,#46969,
#46970,#46971,#46972,#46973,#46974,#46975,#46976,#46977,#46978,#46979,#46980,
#46981,#46982,#46983,#46984,#46985,#46986,#46987,#46988,#46989,#46990,#46991,
#46992,#46993,#46994,#46995,#46996,#46997,#46998,#46999,#47000,#47001,#47002,
#47003,#47004,#47005,#47006,#47007,#47008,#47009,#47010,#47011,#47012,#47013,
#47014,#47015,#47016,#47017,#47018,#47019,#47020,#47021,#47022,#47023,#47024,
#47025,#47026,#47027,#47028,#47029,#47030,#47031,#47032,#47033,#47034,#47035,
#47036,#47037,#47038,#47039,#47040,#47041,#47042,#47043,#47044,#47045,#47046,
#47047,#47048,#47049,#47050,#47051,#47052,#47053,#47054,#47055,#47056,#47057,
#47058,#47059,#47060,#47061,#47062),.UNSPECIFIED.,.F.,.F.,(4,3,3,3,3,3,
3,3,3,3,3,3,3,3,3,3,3,3,3,3,3,3,3,3,3,3,3,3,3,3,3,3,3,3,3,3,3,3,3,3,3,3,
3,3,3,3,3,3,3,3,3,3,3,3,3,3,3,3,3,3,3,3,3,3,3,3,3,3,3,4),(-10.3761157273102,
-10.277030159422,-10.1760986178168,-10.0766550971632,-9.97497954508236,
-9.87330399300149,-9.77793465170269,-9.68269391144577,-9.58310387172771,
-9.48803040862856,-9.39298842864118,-9.29795156015412,-9.20289344369246,
-9.10773205948534,-9.01251014240612,-8.91714263045597,-8.88597359370134,
-8.7906003941096,-8.69535573499435,-8.5957666674202,-8.50068916445218,-8.40564310920763,
-8.31060213558218,-8.21553988958314,-8.12037436320737,-8.02514829195954,
-7.92977664283056,-7.89864319440119,-7.80329505616397,-7.70807553182495,
-7.60848018973446,-7.51342782279223,-7.41840685045479,-7.32339087466709,
-7.22835350940553,-7.13321255084905,-7.03801089429927,-6.94266323112823,
-6.91131279510104,-6.81592594731719,-6.7206677800099,-6.62108210698378,
-6.52599153730943,-6.43093260402686,-6.33587895645016,-6.24080425618366,
-6.14562666958989,-6.05038875257428,-5.9550056715846,-5.92398239580089,
-5.82858542316081,-5.73331672119191,-5.63373363060551,-5.5386315937293,
-5.44356087860388,-5.34849515201683,-5.25340809279504,-5.15821780479437,
-5.06296697390101,-4.96757077445709,-4.93665199650074,-4.84277093189022,
-4.7490388889567,-4.65539094679393,-4.56179908829439,-4.46823536276442,
-4.37440912710598,-4.28077696275078,-4.18685369144072,-4.09293042013066),
 .UNSPECIFIED.);
#529=B_SPLINE_CURVE_WITH_KNOTS('',3,(#47065,#47066,#47067,#47068),
 .UNSPECIFIED.,.F.,.F.,(4,4),(-0.0182409621825525,-0.000698701667614549),
 .UNSPECIFIED.);
#530=B_SPLINE_CURVE_WITH_KNOTS('',3,(#47070,#47071,#47072,#47073,#47074,
#47075,#47076,#47077,#47078,#47079,#47080,#47081,#47082,#47083,#47084,#47085,
#47086,#47087,#47088,#47089,#47090,#47091,#47092,#47093,#47094,#47095,#47096,
#47097,#47098,#47099,#47100,#47101,#47102,#47103,#47104,#47105,#47106,#47107,
#47108,#47109,#47110,#47111,#47112,#47113,#47114,#47115,#47116,#47117,#47118,
#47119,#47120,#47121,#47122,#47123,#47124,#47125,#47126,#47127,#47128,#47129,
#47130,#47131,#47132,#47133,#47134,#47135,#47136,#47137,#47138,#47139,#47140,
#47141,#47142,#47143,#47144,#47145,#47146,#47147,#47148,#47149,#47150,#47151,
#47152,#47153,#47154,#47155,#47156,#47157,#47158,#47159,#47160,#47161,#47162,
#47163,#47164,#47165,#47166,#47167,#47168,#47169,#47170,#47171,#47172,#47173,
#47174,#47175,#47176,#47177,#47178,#47179,#47180,#47181,#47182,#47183,#47184,
#47185,#47186,#47187,#47188,#47189,#47190,#47191,#47192,#47193,#47194,#47195,
#47196,#47197,#47198,#47199,#47200,#47201,#47202,#47203,#47204,#47205,#47206,
#47207,#47208,#47209,#47210,#47211,#47212,#47213,#47214,#47215,#47216,#47217,
#47218,#47219,#47220,#47221,#47222,#47223,#47224,#47225,#47226,#47227,#47228,
#47229,#47230,#47231,#47232,#47233,#47234,#47235,#47236,#47237,#47238,#47239,
#47240,#47241,#47242,#47243,#47244,#47245,#47246,#47247,#47248,#47249,#47250,
#47251,#47252,#47253,#47254,#47255,#47256),.UNSPECIFIED.,.F.,.F.,(4,3,3,
3,3,3,3,3,3,3,3,3,3,3,3,3,3,3,3,3,3,3,3,3,3,3,3,3,3,3,3,3,3,3,3,3,3,3,3,
3,3,3,3,3,3,3,3,3,3,3,3,3,3,3,3,3,3,3,3,3,3,3,4),(78.5398163397448,78.677046774016,
78.7535000002284,78.8541764825381,78.9547110029923,79.0551323551228,79.1554921585444,
79.2558214002717,79.3561510284159,79.4565790619252,79.5570564320356,79.6577081753727,
79.7408303995285,79.8413353461935,79.9416976613493,80.0419466171441,80.1421339931493,
80.2422910182837,80.342448882667,80.4427070395265,80.5430153144406,80.6435011743321,
80.7281607988287,80.8289888931789,80.9296740991317,81.0302440428158,81.1307510764058,
81.2312259823438,81.3316995027274,81.4322676917544,81.5328833565173,81.6336687762747,
81.7154911981288,81.8162854342717,81.9169397387056,82.0174832941154,82.1179667039081,
82.2184207568815,82.318876204121,82.4194307102225,82.5200350970089,82.6208132889057,
82.702821597429,82.8023943022322,82.9018239519552,83.0011436471454,83.1004040721794,
83.1996375603753,83.2988764084443,83.3982287259881,83.4976367746819,83.5972422198623,
83.6901519967291,83.7935465522308,83.8967794207781,83.9998522816575,84.1028308874541,
84.2057403662952,84.3086057649522,84.4114805456595,84.5143560839271,84.6173011712591,
84.6774823960293),.UNSPECIFIED.);
#531=B_SPLINE_CURVE_WITH_KNOTS('',3,(#47260,#47261,#47262,#47263,#47264,
#47265,#47266,#47267,#47268,#47269,#47270,#47271,#47272,#47273,#47274,#47275,
#47276,#47277,#47278,#47279,#47280,#47281,#47282,#47283,#47284,#47285,#47286,
#47287,#47288,#47289,#47290,#47291,#47292,#47293,#47294,#47295,#47296,#47297,
#47298,#47299,#47300,#47301,#47302,#47303,#47304,#47305,#47306,#47307,#47308,
#47309,#47310,#47311,#47312,#47313,#47314,#47315,#47316,#47317,#47318,#47319,
#47320,#47321,#47322,#47323,#47324,#47325,#47326,#47327,#47328,#47329,#47330,
#47331,#47332,#47333,#47334,#47335,#47336,#47337,#47338,#47339,#47340,#47341,
#47342,#47343,#47344,#47345,#47346,#47347,#47348,#47349,#47350,#47351,#47352,
#47353,#47354,#47355,#47356,#47357,#47358,#47359,#47360,#47361,#47362,#47363,
#47364,#47365,#47366,#47367,#47368,#47369,#47370,#47371,#47372,#47373,#47374,
#47375,#47376,#47377,#47378,#47379,#47380,#47381,#47382,#47383,#47384,#47385,
#47386,#47387,#47388,#47389,#47390,#47391,#47392,#47393,#47394,#47395,#47396,
#47397,#47398,#47399,#47400,#47401,#47402,#47403,#47404,#47405,#47406,#47407,
#47408,#47409,#47410),.UNSPECIFIED.,.F.,.F.,(4,3,3,3,3,3,3,3,3,3,3,3,3,
3,3,3,3,3,3,3,3,3,3,3,3,3,3,3,3,3,3,3,3,3,3,3,3,3,3,3,3,3,3,3,3,3,3,3,3,
3,4),(78.5398163400955,78.6396051546265,78.7392548410145,78.8387975186506,
78.9382836159524,79.0377452469571,79.1372144915425,79.2367866223946,79.3364166299699,
79.4362117134907,79.4842975006201,79.5851111912929,79.6857816535804,79.7863364727349,
79.8868281365189,79.9872874516924,80.0877451844647,80.1882977346122,80.2888976157929,
80.3896681150517,80.4728644443454,80.5736414351339,80.6742781542139,80.7748037594743,
80.8752689834692,80.9757046432654,81.0761415180248,81.1766776525678,81.277263544666,
81.3780241833049,81.4614313880706,81.5609873162485,81.6603998580491,81.7597020774321,
81.8589447763137,81.9581603063024,82.0573809821283,82.1567152897885,82.2561051556921,
82.3556933778849,82.4499983317959,82.5533841966888,82.6566079229631,82.7596710669683,
82.8626396280425,82.9655387682385,83.0683935679595,83.1712576539379,83.2741223179695,
83.3770569248603,83.4385652755212),.UNSPECIFIED.);
#532=B_SPLINE_CURVE_WITH_KNOTS('',3,(#47411,#47412,#47413,#47414,#47415,
#47416,#47417,#47418,#47419,#47420,#47421,#47422),.UNSPECIFIED.,.F.,.F.,
(4,2,2,2,2,4),(-2.98855656026776,-2.98466939185962,-2.98096825215168,-2.9778891399808,
-2.97434988120648,-2.97128357771462),.UNSPECIFIED.);
#533=B_SPLINE_CURVE_WITH_KNOTS('',3,(#47425,#47426,#47427,#47428,#47429,
#47430,#47431,#47432,#47433,#47434,#47435,#47436,#47437,#47438,#47439,#47440,
#47441,#47442,#47443,#47444,#47445,#47446,#47447,#47448,#47449,#47450,#47451,
#47452,#47453,#47454,#47455,#47456),.UNSPECIFIED.,.F.,.F.,(4,2,2,2,2,2,
2,2,2,2,2,2,2,2,2,4),(-2.19429233995567,-2.08491574472027,-1.96884002433686,
-1.79513299643777,-1.58607354155283,-1.34152662368927,-1.12750671314745,
-1.05017184774955,-0.892675460524429,-0.709583783276434,-0.553226716657333,
-0.367073680837577,-0.242877737203899,-0.136980729082507,-0.0715905781283026,
-7.46082012014841E-5),.UNSPECIFIED.);
#534=B_SPLINE_CURVE_WITH_KNOTS('',3,(#47457,#47458,#47459,#47460,#47461,
#47462,#47463,#47464,#47465,#47466,#47467,#47468,#47469,#47470,#47471,#47472,
#47473,#47474,#47475,#47476,#47477,#47478,#47479,#47480,#47481,#47482,#47483,
#47484,#47485,#47486,#47487,#47488,#47489,#47490,#47491,#47492,#47493,#47494,
#47495,#47496,#47497,#47498,#47499,#47500,#47501,#47502,#47503,#47504,#47505,
#47506,#47507,#47508,#47509,#47510,#47511,#47512,#47513,#47514,#47515,#47516,
#47517),.UNSPECIFIED.,.F.,.F.,(4,3,3,3,3,3,3,3,3,3,3,3,3,3,3,3,3,3,3,3,
4),(-0.410648750432938,-0.381294613665594,-0.352267124576947,-0.328792823836752,
-0.311187098281605,-0.306018425011984,-0.301691296836585,-0.274143229574461,
-0.258369921616165,-0.230117472373342,-0.201352788326674,-0.195525900786732,
-0.16833922287309,-0.141249160586392,-0.114615533759621,-0.100282139063474,
-0.0960342097686789,-0.0702554174629941,-0.0448546715641945,-0.0201984500449382,
0.),.UNSPECIFIED.);
#535=B_SPLINE_CURVE_WITH_KNOTS('',3,(#47518,#47519,#47520,#47521,#47522,
#47523,#47524,#47525,#47526,#47527,#47528,#47529,#47530,#47531,#47532,#47533,
#47534,#47535,#47536,#47537,#47538,#47539,#47540,#47541,#47542,#47543,#47544,
#47545,#47546,#47547,#47548,#47549,#47550,#47551),.UNSPECIFIED.,.F.,.F.,
(4,3,3,3,3,3,3,3,3,3,3,4),(-0.219677966288006,-0.206985183547511,-0.179985476037348,
-0.178213580556878,-0.148819200354015,-0.130216800309763,-0.118450459252591,
-0.113866160083042,-0.0841488051349767,-0.0540951018364117,-0.0242019686830237,
0.),.UNSPECIFIED.);
#536=B_SPLINE_CURVE_WITH_KNOTS('',3,(#47863,#47864,#47865,#47866,#47867,
#47868,#47869,#47870,#47871,#47872,#47873,#47874,#47875,#47876,#47877,#47878,
#47879,#47880,#47881,#47882,#47883,#47884,#47885,#47886,#47887,#47888,#47889,
#47890,#47891,#47892,#47893,#47894,#47895,#47896,#47897,#47898,#47899,#47900,
#47901,#47902,#47903,#47904,#47905,#47906,#47907,#47908,#47909,#47910,#47911,
#47912,#47913,#47914,#47915,#47916,#47917,#47918,#47919,#47920,#47921,#47922,
#47923,#47924,#47925,#47926,#47927,#47928,#47929,#47930,#47931,#47932,#47933,
#47934,#47935,#47936,#47937,#47938,#47939,#47940,#47941,#47942,#47943,#47944,
#47945,#47946,#47947,#47948,#47949,#47950),.UNSPECIFIED.,.F.,.F.,(4,3,3,
3,3,3,3,3,3,3,3,3,3,3,3,3,3,3,3,3,3,3,3,3,3,3,3,3,3,4),(-0.55274537837504,
-0.525174630400016,-0.495956305234574,-0.483208430614118,-0.476222765985277,
-0.469631349081844,-0.440661555816212,-0.411705679997849,-0.408301329738247,
-0.401969450637142,-0.397429868442983,-0.369148459214845,-0.341142139849232,
-0.313940382864803,-0.29772704364586,-0.291366968188088,-0.26455959815265,
-0.249599392264211,-0.222018910858968,-0.194438429453726,-0.189292991414398,
-0.162671573252089,-0.136033750846249,-0.109916719326503,-0.0950850259724172,
-0.09115324392662,-0.0655931049064447,-0.0404250325731723,-0.0160423336426468,
0.),.UNSPECIFIED.);
#537=B_SPLINE_CURVE_WITH_KNOTS('',3,(#48267,#48268,#48269,#48270,#48271,
#48272,#48273,#48274,#48275,#48276,#48277,#48278,#48279,#48280,#48281,#48282,
#48283,#48284,#48285,#48286,#48287,#48288,#48289,#48290,#48291,#48292,#48293,
#48294,#48295,#48296,#48297,#48298,#48299,#48300,#48301,#48302,#48303,#48304,
#48305,#48306,#48307,#48308,#48309,#48310,#48311,#48312,#48313,#48314,#48315,
#48316,#48317,#48318,#48319,#48320,#48321,#48322,#48323,#48324,#48325,#48326,
#48327,#48328,#48329,#48330,#48331,#48332,#48333,#48334,#48335,#48336,#48337,
#48338,#48339,#48340,#48341,#48342,#48343,#48344,#48345,#48346,#48347,#48348,
#48349,#48350,#48351),.UNSPECIFIED.,.F.,.F.,(4,3,3,3,3,3,3,3,3,3,3,3,3,
3,3,3,3,3,3,3,3,3,3,3,3,3,3,3,4),(-0.555272788399385,-0.533197712400843,
-0.50828572908666,-0.492097097422296,-0.487698425831477,-0.462241873724153,
-0.43610473287827,-0.427671428401512,-0.42202191869945,-0.395298681472729,
-0.368236505229611,-0.341280288641109,-0.32517826205158,-0.321068892319616,
-0.293156561265571,-0.279892116585652,-0.252647806442289,-0.225403496298925,
-0.220542492202756,-0.216708298034074,-0.188804183704433,-0.160414457473374,
-0.131690244065431,-0.114355289595352,-0.109564750157472,-0.0800994390250807,
-0.0505572378463981,-0.021577624140468,-4.47678306657353E-15),
 .UNSPECIFIED.);
#941=SHAPE_REPRESENTATION_RELATIONSHIP('SRR','None',#94493,#956);
#956=ADVANCED_BREP_SHAPE_REPRESENTATION('',(#986),#94402);
#971=STYLED_ITEM('',(#94578),#986);
#986=MANIFOLD_SOLID_BREP('Body1',#8256);
#1014=FACE_BOUND('',#1693,.T.);
#1015=FACE_BOUND('',#1696,.T.);
#1096=PLANE('',#8634);
#1097=PLANE('',#8635);
#1098=PLANE('',#8636);
#1099=PLANE('',#8637);
#1100=PLANE('',#8638);
#1101=PLANE('',#8639);
#1102=PLANE('',#8640);
#1103=PLANE('',#8641);
#1104=PLANE('',#8645);
#1105=PLANE('',#8646);
#1295=FACE_OUTER_BOUND('',#1669,.T.);
#1296=FACE_OUTER_BOUND('',#1670,.T.);
#1297=FACE_OUTER_BOUND('',#1671,.T.);
#1298=FACE_OUTER_BOUND('',#1672,.T.);
#1299=FACE_OUTER_BOUND('',#1673,.T.);
#1300=FACE_OUTER_BOUND('',#1674,.T.);
#1301=FACE_OUTER_BOUND('',#1675,.T.);
#1302=FACE_OUTER_BOUND('',#1676,.T.);
#1303=FACE_OUTER_BOUND('',#1677,.T.);
#1304=FACE_OUTER_BOUND('',#1678,.T.);
#1305=FACE_OUTER_BOUND('',#1679,.T.);
#1306=FACE_OUTER_BOUND('',#1680,.T.);
#1307=FACE_OUTER_BOUND('',#1681,.T.);
#1308=FACE_OUTER_BOUND('',#1682,.T.);
#1309=FACE_OUTER_BOUND('',#1683,.T.);
#1310=FACE_OUTER_BOUND('',#1684,.T.);
#1311=FACE_OUTER_BOUND('',#1685,.T.);
#1312=FACE_OUTER_BOUND('',#1686,.T.);
#1313=FACE_OUTER_BOUND('',#1687,.T.);
#1314=FACE_OUTER_BOUND('',#1688,.T.);
#1315=FACE_OUTER_BOUND('',#1689,.T.);
#1316=FACE_OUTER_BOUND('',#1690,.T.);
#1317=FACE_OUTER_BOUND('',#1691,.T.);
#1318=FACE_OUTER_BOUND('',#1692,.T.);
#1319=FACE_OUTER_BOUND('',#1694,.T.);
#1320=FACE_OUTER_BOUND('',#1695,.T.);
#1321=FACE_OUTER_BOUND('',#1697,.T.);
#1669=EDGE_LOOP('',(#6114,#6115,#6116,#6117));
#1670=EDGE_LOOP('',(#6118,#6119,#6120,#6121,#6122,#6123));
#1671=EDGE_LOOP('',(#6124,#6125,#6126,#6127));
#1672=EDGE_LOOP('',(#6128,#6129,#6130,#6131,#6132,#6133));
#1673=EDGE_LOOP('',(#6134,#6135,#6136,#6137));
#1674=EDGE_LOOP('',(#6138,#6139,#6140,#6141,#6142,#6143));
#1675=EDGE_LOOP('',(#6144,#6145,#6146,#6147));
#1676=EDGE_LOOP('',(#6148,#6149,#6150,#6151,#6152,#6153));
#1677=EDGE_LOOP('',(#6154,#6155,#6156,#6157));
#1678=EDGE_LOOP('',(#6158,#6159,#6160,#6161,#6162,#6163));
#1679=EDGE_LOOP('',(#6164,#6165,#6166,#6167));
#1680=EDGE_LOOP('',(#6168,#6169,#6170,#6171,#6172,#6173,#6174,#6175,#6176,
#6177,#6178,#6179,#6180,#6181,#6182,#6183,#6184,#6185,#6186,#6187,#6188,
#6189,#6190,#6191,#6192,#6193));
#1681=EDGE_LOOP('',(#6194,#6195,#6196,#6197,#6198,#6199));
#1682=EDGE_LOOP('',(#6200,#6201,#6202,#6203,#6204,#6205,#6206,#6207));
#1683=EDGE_LOOP('',(#6208,#6209,#6210,#6211,#6212,#6213,#6214,#6215,#6216,
#6217,#6218,#6219,#6220,#6221,#6222,#6223,#6224,#6225,#6226,#6227,#6228,
#6229,#6230,#6231,#6232,#6233,#6234,#6235,#6236,#6237,#6238,#6239));
#1684=EDGE_LOOP('',(#6240,#6241,#6242,#6243,#6244,#6245,#6246,#6247,#6248,
#6249,#6250,#6251,#6252,#6253,#6254,#6255,#6256,#6257,#6258,#6259,#6260,
#6261,#6262,#6263,#6264,#6265,#6266,#6267,#6268,#6269,#6270,#6271,#6272));
#1685=EDGE_LOOP('',(#6273,#6274,#6275,#6276));
#1686=EDGE_LOOP('',(#6277,#6278,#6279,#6280));
#1687=EDGE_LOOP('',(#6281,#6282,#6283,#6284));
#1688=EDGE_LOOP('',(#6285,#6286,#6287,#6288));
#1689=EDGE_LOOP('',(#6289,#6290,#6291,#6292));
#1690=EDGE_LOOP('',(#6293,#6294,#6295,#6296));
#1691=EDGE_LOOP('',(#6297,#6298,#6299,#6300,#6301,#6302));
#1692=EDGE_LOOP('',(#6303));
#1693=EDGE_LOOP('',(#6304,#6305,#6306,#6307));
#1694=EDGE_LOOP('',(#6308,#6309,#6310,#6311));
#1695=EDGE_LOOP('',(#6312));
#1696=EDGE_LOOP('',(#6313,#6314,#6315,#6316,#6317,#6318));
#1697=EDGE_LOOP('',(#6319));
#2097=LINE('',#40985,#2495);
#2098=LINE('',#41276,#2496);
#2099=LINE('',#41650,#2497);
#2100=LINE('',#42030,#2498);
#2101=LINE('',#42408,#2499);
#2102=LINE('',#42780,#2500);
#2103=LINE('',#43170,#2501);
#2104=LINE('',#43546,#2502);
#2105=LINE('',#43922,#2503);
#2106=LINE('',#44294,#2504);
#2107=LINE('',#44680,#2505);
#2108=LINE('',#47553,#2506);
#2109=LINE('',#48355,#2507);
#2110=LINE('',#48357,#2508);
#2111=LINE('',#48359,#2509);
#2112=LINE('',#48360,#2510);
#2113=LINE('',#48363,#2511);
#2114=LINE('',#48365,#2512);
#2115=LINE('',#48366,#2513);
#2116=LINE('',#48369,#2514);
#2117=LINE('',#48371,#2515);
#2118=LINE('',#48372,#2516);
#2119=LINE('',#48375,#2517);
#2120=LINE('',#48377,#2518);
#2121=LINE('',#48378,#2519);
#2122=LINE('',#48381,#2520);
#2123=LINE('',#48383,#2521);
#2124=LINE('',#48384,#2522);
#2125=LINE('',#48386,#2523);
#2126=LINE('',#48387,#2524);
#2127=LINE('',#48394,#2525);
#2495=VECTOR('',#9475,2.37175);
#2496=VECTOR('',#9480,2.37175);
#2497=VECTOR('',#9483,2.37175);
#2498=VECTOR('',#9486,2.37175);
#2499=VECTOR('',#9489,2.37175);
#2500=VECTOR('',#9492,2.37175);
#2501=VECTOR('',#9495,2.37175);
#2502=VECTOR('',#9498,2.37175);
#2503=VECTOR('',#9501,2.37175);
#2504=VECTOR('',#9504,2.37175);
#2505=VECTOR('',#9507,2.37175);
#2506=VECTOR('',#9520,2.5);
#2507=VECTOR('',#9525,10.);
#2508=VECTOR('',#9526,10.);
#2509=VECTOR('',#9527,10.);
#2510=VECTOR('',#9528,10.);
#2511=VECTOR('',#9531,10.);
#2512=VECTOR('',#9532,10.);
#2513=VECTOR('',#9533,10.);
#2514=VECTOR('',#9536,9.99999999999999);
#2515=VECTOR('',#9537,10.);
#2516=VECTOR('',#9538,10.);
#2517=VECTOR('',#9541,10.);
#2518=VECTOR('',#9542,10.);
#2519=VECTOR('',#9543,10.);
#2520=VECTOR('',#9546,10.);
#2521=VECTOR('',#9547,10.);
#2522=VECTOR('',#9548,10.);
#2523=VECTOR('',#9551,10.);
#2524=VECTOR('',#9552,10.);
#2525=VECTOR('',#9561,5.);
#2770=CIRCLE('',#8616,2.37175);
#2771=CIRCLE('',#8628,2.942);
#2772=CIRCLE('',#8629,2.942);
#2773=CIRCLE('',#8631,2.37175);
#2774=CIRCLE('',#8633,2.);
#2775=CIRCLE('',#8642,5.);
#2776=CIRCLE('',#8644,5.);
#3231=VERTEX_POINT('',#40983);
#3232=VERTEX_POINT('',#40984);
#3233=VERTEX_POINT('',#40986);
#3234=VERTEX_POINT('',#41147);
#3235=VERTEX_POINT('',#41274);
#3236=VERTEX_POINT('',#41275);
#3237=VERTEX_POINT('',#41277);
#3238=VERTEX_POINT('',#41466);
#3239=VERTEX_POINT('',#41648);
#3240=VERTEX_POINT('',#41649);
#3241=VERTEX_POINT('',#42028);
#3242=VERTEX_POINT('',#42029);
#3243=VERTEX_POINT('',#42031);
#3244=VERTEX_POINT('',#42214);
#3245=VERTEX_POINT('',#42406);
#3246=VERTEX_POINT('',#42407);
#3247=VERTEX_POINT('',#42778);
#3248=VERTEX_POINT('',#42779);
#3249=VERTEX_POINT('',#42781);
#3250=VERTEX_POINT('',#42980);
#3251=VERTEX_POINT('',#43168);
#3252=VERTEX_POINT('',#43169);
#3253=VERTEX_POINT('',#43544);
#3254=VERTEX_POINT('',#43545);
#3255=VERTEX_POINT('',#43547);
#3256=VERTEX_POINT('',#43732);
#3257=VERTEX_POINT('',#43920);
#3258=VERTEX_POINT('',#43921);
#3259=VERTEX_POINT('',#44292);
#3260=VERTEX_POINT('',#44293);
#3261=VERTEX_POINT('',#44295);
#3262=VERTEX_POINT('',#44488);
#3263=VERTEX_POINT('',#44678);
#3264=VERTEX_POINT('',#44679);
#3265=VERTEX_POINT('',#45054);
#3266=VERTEX_POINT('',#45055);
#3267=VERTEX_POINT('',#45062);
#3268=VERTEX_POINT('',#45064);
#3269=VERTEX_POINT('',#45070);
#3270=VERTEX_POINT('',#45282);
#3271=VERTEX_POINT('',#45491);
#3272=VERTEX_POINT('',#45503);
#3273=VERTEX_POINT('',#45715);
#3274=VERTEX_POINT('',#45927);
#3275=VERTEX_POINT('',#46139);
#3276=VERTEX_POINT('',#46150);
#3277=VERTEX_POINT('',#46161);
#3278=VERTEX_POINT('',#46373);
#3279=VERTEX_POINT('',#46384);
#3280=VERTEX_POINT('',#46395);
#3281=VERTEX_POINT('',#46397);
#3282=VERTEX_POINT('',#46552);
#3283=VERTEX_POINT('',#46563);
#3284=VERTEX_POINT('',#46574);
#3285=VERTEX_POINT('',#46586);
#3286=VERTEX_POINT('',#46597);
#3287=VERTEX_POINT('',#46609);
#3288=VERTEX_POINT('',#46620);
#3289=VERTEX_POINT('',#46631);
#3290=VERTEX_POINT('',#46643);
#3291=VERTEX_POINT('',#47064);
#3292=VERTEX_POINT('',#47069);
#3293=VERTEX_POINT('',#47257);
#3294=VERTEX_POINT('',#47259);
#3295=VERTEX_POINT('',#47424);
#3296=VERTEX_POINT('',#47552);
#3297=VERTEX_POINT('',#48353);
#3298=VERTEX_POINT('',#48354);
#3299=VERTEX_POINT('',#48356);
#3300=VERTEX_POINT('',#48358);
#3301=VERTEX_POINT('',#48362);
#3302=VERTEX_POINT('',#48364);
#3303=VERTEX_POINT('',#48368);
#3304=VERTEX_POINT('',#48370);
#3305=VERTEX_POINT('',#48374);
#3306=VERTEX_POINT('',#48376);
#3307=VERTEX_POINT('',#48380);
#3308=VERTEX_POINT('',#48382);
#3309=VERTEX_POINT('',#48390);
#3310=VERTEX_POINT('',#48393);
#4322=EDGE_CURVE('',#3231,#3232,#2097,.T.);
#4323=EDGE_CURVE('',#3233,#3231,#473,.T.);
#4324=EDGE_CURVE('',#3234,#3233,#2770,.T.);
#4325=EDGE_CURVE('',#3234,#3232,#474,.T.);
#4326=EDGE_CURVE('',#3235,#3236,#2098,.T.);
#4327=EDGE_CURVE('',#3237,#3235,#475,.F.);
#4328=EDGE_CURVE('',#3231,#3237,#476,.T.);
#4329=EDGE_CURVE('',#3232,#3238,#477,.T.);
#4330=EDGE_CURVE('',#3238,#3236,#478,.T.);
#4331=EDGE_CURVE('',#3239,#3240,#2099,.T.);
#4332=EDGE_CURVE('',#3235,#3239,#479,.F.);
#4333=EDGE_CURVE('',#3236,#3240,#480,.T.);
#4334=EDGE_CURVE('',#3241,#3242,#2100,.T.);
#4335=EDGE_CURVE('',#3243,#3241,#481,.F.);
#4336=EDGE_CURVE('',#3239,#3243,#482,.F.);
#4337=EDGE_CURVE('',#3240,#3244,#483,.T.);
#4338=EDGE_CURVE('',#3244,#3242,#484,.T.);
#4339=EDGE_CURVE('',#3245,#3246,#2101,.T.);
#4340=EDGE_CURVE('',#3241,#3245,#485,.F.);
#4341=EDGE_CURVE('',#3242,#3246,#486,.T.);
#4342=EDGE_CURVE('',#3247,#3248,#2102,.T.);
#4343=EDGE_CURVE('',#3249,#3247,#487,.F.);
#4344=EDGE_CURVE('',#3245,#3249,#488,.F.);
#4345=EDGE_CURVE('',#3246,#3250,#489,.T.);
#4346=EDGE_CURVE('',#3250,#3248,#490,.T.);
#4347=EDGE_CURVE('',#3251,#3252,#2103,.T.);
#4348=EDGE_CURVE('',#3247,#3251,#491,.F.);
#4349=EDGE_CURVE('',#3248,#3252,#492,.T.);
#4350=EDGE_CURVE('',#3253,#3254,#2104,.T.);
#4351=EDGE_CURVE('',#3255,#3253,#493,.F.);
#4352=EDGE_CURVE('',#3251,#3255,#494,.F.);
#4353=EDGE_CURVE('',#3252,#3256,#495,.T.);
#4354=EDGE_CURVE('',#3256,#3254,#496,.T.);
#4355=EDGE_CURVE('',#3257,#3258,#2105,.T.);
#4356=EDGE_CURVE('',#3253,#3257,#497,.F.);
#4357=EDGE_CURVE('',#3254,#3258,#498,.T.);
#4358=EDGE_CURVE('',#3259,#3260,#2106,.T.);
#4359=EDGE_CURVE('',#3261,#3259,#499,.F.);
#4360=EDGE_CURVE('',#3257,#3261,#500,.F.);
#4361=EDGE_CURVE('',#3258,#3262,#501,.T.);
#4362=EDGE_CURVE('',#3262,#3260,#502,.T.);
#4363=EDGE_CURVE('',#3263,#3264,#2107,.T.);
#4364=EDGE_CURVE('',#3259,#3263,#503,.F.);
#4365=EDGE_CURVE('',#3260,#3264,#504,.T.);
#4366=EDGE_CURVE('',#3265,#3266,#505,.T.);
#4367=EDGE_CURVE('',#3266,#3267,#2771,.F.);
#4368=EDGE_CURVE('',#3267,#3268,#506,.T.);
#4369=EDGE_CURVE('',#3268,#3269,#507,.T.);
#4370=EDGE_CURVE('',#3269,#3270,#508,.T.);
#4371=EDGE_CURVE('',#3270,#3271,#509,.T.);
#4372=EDGE_CURVE('',#3271,#3272,#510,.T.);
#4373=EDGE_CURVE('',#3272,#3273,#511,.T.);
#4374=EDGE_CURVE('',#3273,#3274,#512,.T.);
#4375=EDGE_CURVE('',#3274,#3275,#513,.T.);
#4376=EDGE_CURVE('',#3275,#3276,#514,.T.);
#4377=EDGE_CURVE('',#3276,#3277,#515,.T.);
#4378=EDGE_CURVE('',#3277,#3278,#516,.T.);
#4379=EDGE_CURVE('',#3278,#3279,#517,.T.);
#4380=EDGE_CURVE('',#3279,#3280,#2772,.T.);
#4381=EDGE_CURVE('',#3280,#3281,#518,.T.);
#4382=EDGE_CURVE('',#3281,#3282,#519,.T.);
#4383=EDGE_CURVE('',#3282,#3283,#520,.T.);
#4384=EDGE_CURVE('',#3283,#3284,#521,.T.);
#4385=EDGE_CURVE('',#3284,#3285,#522,.T.);
#4386=EDGE_CURVE('',#3285,#3286,#523,.T.);
#4387=EDGE_CURVE('',#3286,#3287,#524,.T.);
#4388=EDGE_CURVE('',#3287,#3288,#525,.T.);
#4389=EDGE_CURVE('',#3288,#3289,#526,.T.);
#4390=EDGE_CURVE('',#3289,#3290,#527,.T.);
#4391=EDGE_CURVE('',#3290,#3265,#528,.T.);
#4392=EDGE_CURVE('',#3264,#3291,#529,.T.);
#4393=EDGE_CURVE('',#3291,#3292,#530,.T.);
#4394=EDGE_CURVE('',#3292,#3293,#2773,.T.);
#4395=EDGE_CURVE('',#3294,#3293,#531,.T.);
#4396=EDGE_CURVE('',#3263,#3294,#532,.F.);
#4397=EDGE_CURVE('',#3293,#3295,#533,.T.);
#4398=EDGE_CURVE('',#3280,#3292,#534,.T.);
#4399=EDGE_CURVE('',#3295,#3279,#535,.T.);
#4400=EDGE_CURVE('',#3295,#3296,#2108,.T.);
#4401=EDGE_CURVE('',#3296,#3296,#2774,.T.);
#4402=EDGE_CURVE('',#3266,#3234,#536,.T.);
#4403=EDGE_CURVE('',#3233,#3267,#537,.T.);
#4404=EDGE_CURVE('',#3297,#3298,#2109,.T.);
#4405=EDGE_CURVE('',#3297,#3299,#2110,.T.);
#4406=EDGE_CURVE('',#3299,#3300,#2111,.T.);
#4407=EDGE_CURVE('',#3298,#3300,#2112,.T.);
#4408=EDGE_CURVE('',#3301,#3297,#2113,.T.);
#4409=EDGE_CURVE('',#3301,#3302,#2114,.T.);
#4410=EDGE_CURVE('',#3302,#3299,#2115,.T.);
#4411=EDGE_CURVE('',#3303,#3301,#2116,.T.);
#4412=EDGE_CURVE('',#3303,#3304,#2117,.T.);
#4413=EDGE_CURVE('',#3304,#3302,#2118,.T.);
#4414=EDGE_CURVE('',#3305,#3303,#2119,.T.);
#4415=EDGE_CURVE('',#3305,#3306,#2120,.T.);
#4416=EDGE_CURVE('',#3306,#3304,#2121,.T.);
#4417=EDGE_CURVE('',#3307,#3305,#2122,.T.);
#4418=EDGE_CURVE('',#3307,#3308,#2123,.T.);
#4419=EDGE_CURVE('',#3308,#3306,#2124,.T.);
#4420=EDGE_CURVE('',#3298,#3307,#2125,.T.);
#4421=EDGE_CURVE('',#3300,#3308,#2126,.T.);
#4422=EDGE_CURVE('',#3309,#3309,#2775,.T.);
#4423=EDGE_CURVE('',#3309,#3310,#2127,.T.);
#4424=EDGE_CURVE('',#3310,#3310,#2776,.T.);
#6114=ORIENTED_EDGE('',*,*,#4322,.F.);
#6115=ORIENTED_EDGE('',*,*,#4323,.F.);
#6116=ORIENTED_EDGE('',*,*,#4324,.F.);
#6117=ORIENTED_EDGE('',*,*,#4325,.T.);
#6118=ORIENTED_EDGE('',*,*,#4326,.F.);
#6119=ORIENTED_EDGE('',*,*,#4327,.F.);
#6120=ORIENTED_EDGE('',*,*,#4328,.F.);
#6121=ORIENTED_EDGE('',*,*,#4322,.T.);
#6122=ORIENTED_EDGE('',*,*,#4329,.T.);
#6123=ORIENTED_EDGE('',*,*,#4330,.T.);
#6124=ORIENTED_EDGE('',*,*,#4331,.F.);
#6125=ORIENTED_EDGE('',*,*,#4332,.F.);
#6126=ORIENTED_EDGE('',*,*,#4326,.T.);
#6127=ORIENTED_EDGE('',*,*,#4333,.T.);
#6128=ORIENTED_EDGE('',*,*,#4334,.F.);
#6129=ORIENTED_EDGE('',*,*,#4335,.F.);
#6130=ORIENTED_EDGE('',*,*,#4336,.F.);
#6131=ORIENTED_EDGE('',*,*,#4331,.T.);
#6132=ORIENTED_EDGE('',*,*,#4337,.T.);
#6133=ORIENTED_EDGE('',*,*,#4338,.T.);
#6134=ORIENTED_EDGE('',*,*,#4339,.F.);
#6135=ORIENTED_EDGE('',*,*,#4340,.F.);
#6136=ORIENTED_EDGE('',*,*,#4334,.T.);
#6137=ORIENTED_EDGE('',*,*,#4341,.T.);
#6138=ORIENTED_EDGE('',*,*,#4342,.F.);
#6139=ORIENTED_EDGE('',*,*,#4343,.F.);
#6140=ORIENTED_EDGE('',*,*,#4344,.F.);
#6141=ORIENTED_EDGE('',*,*,#4339,.T.);
#6142=ORIENTED_EDGE('',*,*,#4345,.T.);
#6143=ORIENTED_EDGE('',*,*,#4346,.T.);
#6144=ORIENTED_EDGE('',*,*,#4347,.F.);
#6145=ORIENTED_EDGE('',*,*,#4348,.F.);
#6146=ORIENTED_EDGE('',*,*,#4342,.T.);
#6147=ORIENTED_EDGE('',*,*,#4349,.T.);
#6148=ORIENTED_EDGE('',*,*,#4350,.F.);
#6149=ORIENTED_EDGE('',*,*,#4351,.F.);
#6150=ORIENTED_EDGE('',*,*,#4352,.F.);
#6151=ORIENTED_EDGE('',*,*,#4347,.T.);
#6152=ORIENTED_EDGE('',*,*,#4353,.T.);
#6153=ORIENTED_EDGE('',*,*,#4354,.T.);
#6154=ORIENTED_EDGE('',*,*,#4355,.F.);
#6155=ORIENTED_EDGE('',*,*,#4356,.F.);
#6156=ORIENTED_EDGE('',*,*,#4350,.T.);
#6157=ORIENTED_EDGE('',*,*,#4357,.T.);
#6158=ORIENTED_EDGE('',*,*,#4358,.F.);
#6159=ORIENTED_EDGE('',*,*,#4359,.F.);
#6160=ORIENTED_EDGE('',*,*,#4360,.F.);
#6161=ORIENTED_EDGE('',*,*,#4355,.T.);
#6162=ORIENTED_EDGE('',*,*,#4361,.T.);
#6163=ORIENTED_EDGE('',*,*,#4362,.T.);
#6164=ORIENTED_EDGE('',*,*,#4363,.F.);
#6165=ORIENTED_EDGE('',*,*,#4364,.F.);
#6166=ORIENTED_EDGE('',*,*,#4358,.T.);
#6167=ORIENTED_EDGE('',*,*,#4365,.T.);
#6168=ORIENTED_EDGE('',*,*,#4366,.T.);
#6169=ORIENTED_EDGE('',*,*,#4367,.T.);
#6170=ORIENTED_EDGE('',*,*,#4368,.T.);
#6171=ORIENTED_EDGE('',*,*,#4369,.T.);
#6172=ORIENTED_EDGE('',*,*,#4370,.T.);
#6173=ORIENTED_EDGE('',*,*,#4371,.T.);
#6174=ORIENTED_EDGE('',*,*,#4372,.T.);
#6175=ORIENTED_EDGE('',*,*,#4373,.T.);
#6176=ORIENTED_EDGE('',*,*,#4374,.T.);
#6177=ORIENTED_EDGE('',*,*,#4375,.T.);
#6178=ORIENTED_EDGE('',*,*,#4376,.T.);
#6179=ORIENTED_EDGE('',*,*,#4377,.T.);
#6180=ORIENTED_EDGE('',*,*,#4378,.T.);
#6181=ORIENTED_EDGE('',*,*,#4379,.T.);
#6182=ORIENTED_EDGE('',*,*,#4380,.T.);
#6183=ORIENTED_EDGE('',*,*,#4381,.T.);
#6184=ORIENTED_EDGE('',*,*,#4382,.T.);
#6185=ORIENTED_EDGE('',*,*,#4383,.T.);
#6186=ORIENTED_EDGE('',*,*,#4384,.T.);
#6187=ORIENTED_EDGE('',*,*,#4385,.T.);
#6188=ORIENTED_EDGE('',*,*,#4386,.T.);
#6189=ORIENTED_EDGE('',*,*,#4387,.T.);
#6190=ORIENTED_EDGE('',*,*,#4388,.T.);
#6191=ORIENTED_EDGE('',*,*,#4389,.T.);
#6192=ORIENTED_EDGE('',*,*,#4390,.T.);
#6193=ORIENTED_EDGE('',*,*,#4391,.T.);
#6194=ORIENTED_EDGE('',*,*,#4363,.T.);
#6195=ORIENTED_EDGE('',*,*,#4392,.T.);
#6196=ORIENTED_EDGE('',*,*,#4393,.T.);
#6197=ORIENTED_EDGE('',*,*,#4394,.T.);
#6198=ORIENTED_EDGE('',*,*,#4395,.F.);
#6199=ORIENTED_EDGE('',*,*,#4396,.F.);
#6200=ORIENTED_EDGE('',*,*,#4397,.F.);
#6201=ORIENTED_EDGE('',*,*,#4394,.F.);
#6202=ORIENTED_EDGE('',*,*,#4398,.F.);
#6203=ORIENTED_EDGE('',*,*,#4380,.F.);
#6204=ORIENTED_EDGE('',*,*,#4399,.F.);
#6205=ORIENTED_EDGE('',*,*,#4400,.T.);
#6206=ORIENTED_EDGE('',*,*,#4401,.F.);
#6207=ORIENTED_EDGE('',*,*,#4400,.F.);
#6208=ORIENTED_EDGE('',*,*,#4398,.T.);
#6209=ORIENTED_EDGE('',*,*,#4393,.F.);
#6210=ORIENTED_EDGE('',*,*,#4392,.F.);
#6211=ORIENTED_EDGE('',*,*,#4365,.F.);
#6212=ORIENTED_EDGE('',*,*,#4362,.F.);
#6213=ORIENTED_EDGE('',*,*,#4361,.F.);
#6214=ORIENTED_EDGE('',*,*,#4357,.F.);
#6215=ORIENTED_EDGE('',*,*,#4354,.F.);
#6216=ORIENTED_EDGE('',*,*,#4353,.F.);
#6217=ORIENTED_EDGE('',*,*,#4349,.F.);
#6218=ORIENTED_EDGE('',*,*,#4346,.F.);
#6219=ORIENTED_EDGE('',*,*,#4345,.F.);
#6220=ORIENTED_EDGE('',*,*,#4341,.F.);
#6221=ORIENTED_EDGE('',*,*,#4338,.F.);
#6222=ORIENTED_EDGE('',*,*,#4337,.F.);
#6223=ORIENTED_EDGE('',*,*,#4333,.F.);
#6224=ORIENTED_EDGE('',*,*,#4330,.F.);
#6225=ORIENTED_EDGE('',*,*,#4329,.F.);
#6226=ORIENTED_EDGE('',*,*,#4325,.F.);
#6227=ORIENTED_EDGE('',*,*,#4402,.F.);
#6228=ORIENTED_EDGE('',*,*,#4366,.F.);
#6229=ORIENTED_EDGE('',*,*,#4391,.F.);
#6230=ORIENTED_EDGE('',*,*,#4390,.F.);
#6231=ORIENTED_EDGE('',*,*,#4389,.F.);
#6232=ORIENTED_EDGE('',*,*,#4388,.F.);
#6233=ORIENTED_EDGE('',*,*,#4387,.F.);
#6234=ORIENTED_EDGE('',*,*,#4386,.F.);
#6235=ORIENTED_EDGE('',*,*,#4385,.F.);
#6236=ORIENTED_EDGE('',*,*,#4384,.F.);
#6237=ORIENTED_EDGE('',*,*,#4383,.F.);
#6238=ORIENTED_EDGE('',*,*,#4382,.F.);
#6239=ORIENTED_EDGE('',*,*,#4381,.F.);
#6240=ORIENTED_EDGE('',*,*,#4397,.T.);
#6241=ORIENTED_EDGE('',*,*,#4399,.T.);
#6242=ORIENTED_EDGE('',*,*,#4379,.F.);
#6243=ORIENTED_EDGE('',*,*,#4378,.F.);
#6244=ORIENTED_EDGE('',*,*,#4377,.F.);
#6245=ORIENTED_EDGE('',*,*,#4376,.F.);
#6246=ORIENTED_EDGE('',*,*,#4375,.F.);
#6247=ORIENTED_EDGE('',*,*,#4374,.F.);
#6248=ORIENTED_EDGE('',*,*,#4373,.F.);
#6249=ORIENTED_EDGE('',*,*,#4372,.F.);
#6250=ORIENTED_EDGE('',*,*,#4371,.F.);
#6251=ORIENTED_EDGE('',*,*,#4370,.F.);
#6252=ORIENTED_EDGE('',*,*,#4369,.F.);
#6253=ORIENTED_EDGE('',*,*,#4368,.F.);
#6254=ORIENTED_EDGE('',*,*,#4403,.F.);
#6255=ORIENTED_EDGE('',*,*,#4323,.T.);
#6256=ORIENTED_EDGE('',*,*,#4328,.T.);
#6257=ORIENTED_EDGE('',*,*,#4327,.T.);
#6258=ORIENTED_EDGE('',*,*,#4332,.T.);
#6259=ORIENTED_EDGE('',*,*,#4336,.T.);
#6260=ORIENTED_EDGE('',*,*,#4335,.T.);
#6261=ORIENTED_EDGE('',*,*,#4340,.T.);
#6262=ORIENTED_EDGE('',*,*,#4344,.T.);
#6263=ORIENTED_EDGE('',*,*,#4343,.T.);
#6264=ORIENTED_EDGE('',*,*,#4348,.T.);
#6265=ORIENTED_EDGE('',*,*,#4352,.T.);
#6266=ORIENTED_EDGE('',*,*,#4351,.T.);
#6267=ORIENTED_EDGE('',*,*,#4356,.T.);
#6268=ORIENTED_EDGE('',*,*,#4360,.T.);
#6269=ORIENTED_EDGE('',*,*,#4359,.T.);
#6270=ORIENTED_EDGE('',*,*,#4364,.T.);
#6271=ORIENTED_EDGE('',*,*,#4396,.T.);
#6272=ORIENTED_EDGE('',*,*,#4395,.T.);
#6273=ORIENTED_EDGE('',*,*,#4404,.F.);
#6274=ORIENTED_EDGE('',*,*,#4405,.T.);
#6275=ORIENTED_EDGE('',*,*,#4406,.T.);
#6276=ORIENTED_EDGE('',*,*,#4407,.F.);
#6277=ORIENTED_EDGE('',*,*,#4408,.F.);
#6278=ORIENTED_EDGE('',*,*,#4409,.T.);
#6279=ORIENTED_EDGE('',*,*,#4410,.T.);
#6280=ORIENTED_EDGE('',*,*,#4405,.F.);
#6281=ORIENTED_EDGE('',*,*,#4411,.F.);
#6282=ORIENTED_EDGE('',*,*,#4412,.T.);
#6283=ORIENTED_EDGE('',*,*,#4413,.T.);
#6284=ORIENTED_EDGE('',*,*,#4409,.F.);
#6285=ORIENTED_EDGE('',*,*,#4414,.F.);
#6286=ORIENTED_EDGE('',*,*,#4415,.T.);
#6287=ORIENTED_EDGE('',*,*,#4416,.T.);
#6288=ORIENTED_EDGE('',*,*,#4412,.F.);
#6289=ORIENTED_EDGE('',*,*,#4417,.F.);
#6290=ORIENTED_EDGE('',*,*,#4418,.T.);
#6291=ORIENTED_EDGE('',*,*,#4419,.T.);
#6292=ORIENTED_EDGE('',*,*,#4415,.F.);
#6293=ORIENTED_EDGE('',*,*,#4420,.F.);
#6294=ORIENTED_EDGE('',*,*,#4407,.T.);
#6295=ORIENTED_EDGE('',*,*,#4421,.T.);
#6296=ORIENTED_EDGE('',*,*,#4418,.F.);
#6297=ORIENTED_EDGE('',*,*,#4421,.F.);
#6298=ORIENTED_EDGE('',*,*,#4406,.F.);
#6299=ORIENTED_EDGE('',*,*,#4410,.F.);
#6300=ORIENTED_EDGE('',*,*,#4413,.F.);
#6301=ORIENTED_EDGE('',*,*,#4416,.F.);
#6302=ORIENTED_EDGE('',*,*,#4419,.F.);
#6303=ORIENTED_EDGE('',*,*,#4422,.T.);
#6304=ORIENTED_EDGE('',*,*,#4402,.T.);
#6305=ORIENTED_EDGE('',*,*,#4324,.T.);
#6306=ORIENTED_EDGE('',*,*,#4403,.T.);
#6307=ORIENTED_EDGE('',*,*,#4367,.F.);
#6308=ORIENTED_EDGE('',*,*,#4422,.F.);
#6309=ORIENTED_EDGE('',*,*,#4423,.T.);
#6310=ORIENTED_EDGE('',*,*,#4424,.T.);
#6311=ORIENTED_EDGE('',*,*,#4423,.F.);
#6312=ORIENTED_EDGE('',*,*,#4424,.F.);
#6313=ORIENTED_EDGE('',*,*,#4404,.T.);
#6314=ORIENTED_EDGE('',*,*,#4420,.T.);
#6315=ORIENTED_EDGE('',*,*,#4417,.T.);
#6316=ORIENTED_EDGE('',*,*,#4414,.T.);
#6317=ORIENTED_EDGE('',*,*,#4411,.T.);
#6318=ORIENTED_EDGE('',*,*,#4408,.T.);
#6319=ORIENTED_EDGE('',*,*,#4401,.T.);
#7753=CYLINDRICAL_SURFACE('',#8615,2.37175);
#7754=CYLINDRICAL_SURFACE('',#8617,2.37175);
#7755=CYLINDRICAL_SURFACE('',#8618,2.37175);
#7756=CYLINDRICAL_SURFACE('',#8619,2.37175);
#7757=CYLINDRICAL_SURFACE('',#8620,2.37175);
#7758=CYLINDRICAL_SURFACE('',#8621,2.37175);
#7759=CYLINDRICAL_SURFACE('',#8622,2.37175);
#7760=CYLINDRICAL_SURFACE('',#8623,2.37175);
#7761=CYLINDRICAL_SURFACE('',#8624,2.37175);
#7762=CYLINDRICAL_SURFACE('',#8625,2.37175);
#7763=CYLINDRICAL_SURFACE('',#8626,2.37175);
#7764=CYLINDRICAL_SURFACE('',#8627,2.942);
#7765=CYLINDRICAL_SURFACE('',#8630,2.37175);
#7766=CYLINDRICAL_SURFACE('',#8643,5.);
#8032=ADVANCED_FACE('',(#1295),#7753,.T.);
#8033=ADVANCED_FACE('',(#1296),#7754,.T.);
#8034=ADVANCED_FACE('',(#1297),#7755,.T.);
#8035=ADVANCED_FACE('',(#1298),#7756,.T.);
#8036=ADVANCED_FACE('',(#1299),#7757,.T.);
#8037=ADVANCED_FACE('',(#1300),#7758,.T.);
#8038=ADVANCED_FACE('',(#1301),#7759,.T.);
#8039=ADVANCED_FACE('',(#1302),#7760,.T.);
#8040=ADVANCED_FACE('',(#1303),#7761,.T.);
#8041=ADVANCED_FACE('',(#1304),#7762,.T.);
#8042=ADVANCED_FACE('',(#1305),#7763,.T.);
#8043=ADVANCED_FACE('',(#1306),#7764,.T.);
#8044=ADVANCED_FACE('',(#1307),#7765,.T.);
#8045=ADVANCED_FACE('',(#1308),#151,.T.);
#8046=ADVANCED_FACE('',(#1309),#158,.F.);
#8047=ADVANCED_FACE('',(#1310),#159,.F.);
#8048=ADVANCED_FACE('',(#1311),#1096,.F.);
#8049=ADVANCED_FACE('',(#1312),#1097,.F.);
#8050=ADVANCED_FACE('',(#1313),#1098,.F.);
#8051=ADVANCED_FACE('',(#1314),#1099,.F.);
#8052=ADVANCED_FACE('',(#1315),#1100,.F.);
#8053=ADVANCED_FACE('',(#1316),#1101,.F.);
#8054=ADVANCED_FACE('',(#1317),#1102,.F.);
#8055=ADVANCED_FACE('',(#1318,#1014),#1103,.T.);
#8056=ADVANCED_FACE('',(#1319),#7766,.T.);
#8057=ADVANCED_FACE('',(#1320,#1015),#1104,.F.);
#8058=ADVANCED_FACE('',(#1321),#1105,.T.);
#8256=CLOSED_SHELL('',(#8032,#8033,#8034,#8035,#8036,#8037,#8038,#8039,
#8040,#8041,#8042,#8043,#8044,#8045,#8046,#8047,#8048,#8049,#8050,#8051,
#8052,#8053,#8054,#8055,#8056,#8057,#8058));
#8614=AXIS2_PLACEMENT_3D('',#40981,#9471,#9472);
#8615=AXIS2_PLACEMENT_3D('',#40982,#9473,#9474);
#8616=AXIS2_PLACEMENT_3D('',#41148,#9476,#9477);
#8617=AXIS2_PLACEMENT_3D('',#41273,#9478,#9479);
#8618=AXIS2_PLACEMENT_3D('',#41647,#9481,#9482);
#8619=AXIS2_PLACEMENT_3D('',#42027,#9484,#9485);
#8620=AXIS2_PLACEMENT_3D('',#42405,#9487,#9488);
#8621=AXIS2_PLACEMENT_3D('',#42777,#9490,#9491);
#8622=AXIS2_PLACEMENT_3D('',#43167,#9493,#9494);
#8623=AXIS2_PLACEMENT_3D('',#43543,#9496,#9497);
#8624=AXIS2_PLACEMENT_3D('',#43919,#9499,#9500);
#8625=AXIS2_PLACEMENT_3D('',#44291,#9502,#9503);
#8626=AXIS2_PLACEMENT_3D('',#44677,#9505,#9506);
#8627=AXIS2_PLACEMENT_3D('',#45053,#9508,#9509);
#8628=AXIS2_PLACEMENT_3D('',#45063,#9510,#9511);
#8629=AXIS2_PLACEMENT_3D('',#46396,#9512,#9513);
#8630=AXIS2_PLACEMENT_3D('',#47063,#9514,#9515);
#8631=AXIS2_PLACEMENT_3D('',#47258,#9516,#9517);
#8632=AXIS2_PLACEMENT_3D('',#47423,#9518,#9519);
#8633=AXIS2_PLACEMENT_3D('',#47554,#9521,#9522);
#8634=AXIS2_PLACEMENT_3D('',#48352,#9523,#9524);
#8635=AXIS2_PLACEMENT_3D('',#48361,#9529,#9530);
#8636=AXIS2_PLACEMENT_3D('',#48367,#9534,#9535);
#8637=AXIS2_PLACEMENT_3D('',#48373,#9539,#9540);
#8638=AXIS2_PLACEMENT_3D('',#48379,#9544,#9545);
#8639=AXIS2_PLACEMENT_3D('',#48385,#9549,#9550);
#8640=AXIS2_PLACEMENT_3D('',#48388,#9553,#9554);
#8641=AXIS2_PLACEMENT_3D('',#48389,#9555,#9556);
#8642=AXIS2_PLACEMENT_3D('',#48391,#9557,#9558);
#8643=AXIS2_PLACEMENT_3D('',#48392,#9559,#9560);
#8644=AXIS2_PLACEMENT_3D('',#48395,#9562,#9563);
#8645=AXIS2_PLACEMENT_3D('',#48396,#9564,#9565);
#8646=AXIS2_PLACEMENT_3D('',#48397,#9566,#9567);
#9471=DIRECTION('axis',(0.,0.,1.));
#9472=DIRECTION('refdir',(1.,0.,0.));
#9473=DIRECTION('center_axis',(0.,0.,1.));
#9474=DIRECTION('ref_axis',(0.997344302588954,-0.0728309144069492,0.));
#9475=DIRECTION('',(0.,0.,-1.));
#9476=DIRECTION('center_axis',(0.,0.,-1.));
#9477=DIRECTION('ref_axis',(1.,7.52212518638754E-14,0.));
#9478=DIRECTION('center_axis',(0.,0.,1.));
#9479=DIRECTION('ref_axis',(0.997344302588954,-0.0728309144069492,0.));
#9480=DIRECTION('',(0.,0.,-1.));
#9481=DIRECTION('center_axis',(0.,0.,1.));
#9482=DIRECTION('ref_axis',(0.997344302588954,-0.0728309144069492,0.));
#9483=DIRECTION('',(0.,0.,-1.));
#9484=DIRECTION('center_axis',(0.,0.,1.));
#9485=DIRECTION('ref_axis',(0.997344302588954,-0.0728309144069492,0.));
#9486=DIRECTION('',(0.,0.,-1.));
#9487=DIRECTION('center_axis',(0.,0.,1.));
#9488=DIRECTION('ref_axis',(0.997344302588954,-0.0728309144069492,0.));
#9489=DIRECTION('',(0.,0.,-1.));
#9490=DIRECTION('center_axis',(0.,0.,1.));
#9491=DIRECTION('ref_axis',(0.997344302588954,-0.0728309144069492,0.));
#9492=DIRECTION('',(0.,0.,-1.));
#9493=DIRECTION('center_axis',(0.,0.,1.));
#9494=DIRECTION('ref_axis',(0.997344302588954,-0.0728309144069492,0.));
#9495=DIRECTION('',(0.,0.,-1.));
#9496=DIRECTION('center_axis',(0.,0.,1.));
#9497=DIRECTION('ref_axis',(0.997344302588954,-0.0728309144069492,0.));
#9498=DIRECTION('',(0.,0.,-1.));
#9499=DIRECTION('center_axis',(0.,0.,1.));
#9500=DIRECTION('ref_axis',(0.997344302588954,-0.0728309144069492,0.));
#9501=DIRECTION('',(0.,0.,-1.));
#9502=DIRECTION('center_axis',(0.,0.,1.));
#9503=DIRECTION('ref_axis',(0.997344302588954,-0.0728309144069492,0.));
#9504=DIRECTION('',(0.,0.,-1.));
#9505=DIRECTION('center_axis',(0.,0.,1.));
#9506=DIRECTION('ref_axis',(0.997344302588954,-0.0728309144069492,0.));
#9507=DIRECTION('',(0.,0.,-1.));
#9508=DIRECTION('center_axis',(0.,0.,1.));
#9509=DIRECTION('ref_axis',(1.,0.,0.));
#9510=DIRECTION('center_axis',(0.,0.,-1.));
#9511=DIRECTION('ref_axis',(1.,0.,0.));
#9512=DIRECTION('center_axis',(0.,0.,-1.));
#9513=DIRECTION('ref_axis',(1.,0.,0.));
#9514=DIRECTION('center_axis',(0.,0.,1.));
#9515=DIRECTION('ref_axis',(0.997344302588954,-0.0728309144069492,0.));
#9516=DIRECTION('center_axis',(0.,0.,-1.));
#9517=DIRECTION('ref_axis',(1.,7.52212518638754E-14,0.));
#9518=DIRECTION('center_axis',(0.,0.,-1.));
#9519=DIRECTION('ref_axis',(1.,0.,0.));
#9520=DIRECTION('',(0.707106781186548,-8.65956056235494E-17,0.707106781186547));
#9521=DIRECTION('center_axis',(0.,0.,1.));
#9522=DIRECTION('ref_axis',(1.,0.,0.));
#9523=DIRECTION('center_axis',(-1.92296268638356E-16,-1.,0.));
#9524=DIRECTION('ref_axis',(1.,-1.92296268638356E-16,0.));
#9525=DIRECTION('',(1.,-1.92296268638356E-16,0.));
#9526=DIRECTION('',(0.,0.,1.));
#9527=DIRECTION('',(1.,-1.92296268638356E-16,0.));
#9528=DIRECTION('',(0.,0.,1.));
#9529=DIRECTION('center_axis',(-0.866025403784439,-0.5,0.));
#9530=DIRECTION('ref_axis',(0.5,-0.866025403784439,0.));
#9531=DIRECTION('',(0.5,-0.866025403784439,0.));
#9532=DIRECTION('',(0.,0.,1.));
#9533=DIRECTION('',(0.5,-0.866025403784439,0.));
#9534=DIRECTION('center_axis',(-0.866025403784439,0.5,0.));
#9535=DIRECTION('ref_axis',(-0.5,-0.866025403784439,0.));
#9536=DIRECTION('',(-0.5,-0.866025403784439,0.));
#9537=DIRECTION('',(0.,0.,1.));
#9538=DIRECTION('',(-0.5,-0.866025403784439,0.));
#9539=DIRECTION('center_axis',(1.92296268638356E-16,1.,0.));
#9540=DIRECTION('ref_axis',(-1.,1.92296268638356E-16,0.));
#9541=DIRECTION('',(-1.,1.92296268638356E-16,0.));
#9542=DIRECTION('',(0.,0.,1.));
#9543=DIRECTION('',(-1.,1.92296268638356E-16,0.));
#9544=DIRECTION('center_axis',(0.866025403784439,0.5,0.));
#9545=DIRECTION('ref_axis',(-0.5,0.866025403784439,0.));
#9546=DIRECTION('',(-0.5,0.866025403784439,0.));
#9547=DIRECTION('',(0.,0.,1.));
#9548=DIRECTION('',(-0.5,0.866025403784439,0.));
#9549=DIRECTION('center_axis',(0.866025403784439,-0.5,0.));
#9550=DIRECTION('ref_axis',(0.5,0.866025403784439,0.));
#9551=DIRECTION('',(0.5,0.866025403784439,0.));
#9552=DIRECTION('',(0.5,0.866025403784439,0.));
#9553=DIRECTION('center_axis',(0.,0.,1.));
#9554=DIRECTION('ref_axis',(1.,0.,0.));
#9555=DIRECTION('center_axis',(0.,0.,1.));
#9556=DIRECTION('ref_axis',(1.,0.,0.));
#9557=DIRECTION('center_axis',(0.,0.,1.));
#9558=DIRECTION('ref_axis',(1.,0.,0.));
#9559=DIRECTION('center_axis',(0.,0.,1.));
#9560=DIRECTION('ref_axis',(1.,0.,0.));
#9561=DIRECTION('',(0.,0.,-1.));
#9562=DIRECTION('center_axis',(0.,0.,1.));
#9563=DIRECTION('ref_axis',(1.,0.,0.));
#9564=DIRECTION('center_axis',(0.,0.,1.));
#9565=DIRECTION('ref_axis',(1.,0.,0.));
#9566=DIRECTION('center_axis',(0.,0.,1.));
#9567=DIRECTION('ref_axis',(1.,0.,0.));
#40981=CARTESIAN_POINT('',(0.,0.,0.));
#40982=CARTESIAN_POINT('Origin',(0.,0.,-1.84858989190501));
#40983=CARTESIAN_POINT('',(-2.36545134966535,0.172736721244679,0.83705293121947));
#40984=CARTESIAN_POINT('',(-2.36545134966535,0.172736721244682,0.639882202840047));
#40985=CARTESIAN_POINT('',(-2.36545134966535,0.172736721244682,-1.84858989190501));
#40986=CARTESIAN_POINT('',(-1.37697654870914,-1.93109648821727,7.5238082697382E-5));
#40987=CARTESIAN_POINT('Ctrl Pts',(-1.37697654870914,-1.93109648821727,
7.5238082697604E-5));
#40988=CARTESIAN_POINT('Ctrl Pts',(-1.31325509998115,-1.97653333773959,
0.00535249991746657));
#40989=CARTESIAN_POINT('Ctrl Pts',(-1.24716040592176,-2.01889953805901,
0.0106297617522353));
#40990=CARTESIAN_POINT('Ctrl Pts',(-1.17902429120828,-2.05793580639456,
0.0159070235870042));
#40991=CARTESIAN_POINT('Ctrl Pts',(-1.11077485413276,-2.09703699892121,
0.0211930624378784));
#40992=CARTESIAN_POINT('Ctrl Pts',(-1.04047756431894,-2.13279685390308,
0.0264791012887525));
#40993=CARTESIAN_POINT('Ctrl Pts',(-0.968497728889413,-2.16499658467076,
0.0317651401396266));
#40994=CARTESIAN_POINT('Ctrl Pts',(-0.896801545952434,-2.19706942526375,
0.0370303481829998));
#40995=CARTESIAN_POINT('Ctrl Pts',(-0.823436481138263,-2.22560992756757,
0.0422955562263733));
#40996=CARTESIAN_POINT('Ctrl Pts',(-0.748789098656628,-2.25044727737243,
0.0475607642697464));
#40997=CARTESIAN_POINT('Ctrl Pts',(-0.674178268397067,-2.27527246519257,
0.0528233941242097));
#40998=CARTESIAN_POINT('Ctrl Pts',(-0.598286820096588,-2.29639794759183,
0.0580860239786726));
#40999=CARTESIAN_POINT('Ctrl Pts',(-0.521519812123941,-2.31370161171708,
0.0633486538331358));
#41000=CARTESIAN_POINT('Ctrl Pts',(-0.444765325767524,-2.33100245340797,
0.0686104252897907));
#41001=CARTESIAN_POINT('Ctrl Pts',(-0.367136030644985,-2.34448261023254,
0.0738721967464463));
#41002=CARTESIAN_POINT('Ctrl Pts',(-0.289049019812454,-2.35407067154864,
0.0791339682031011));
#41003=CARTESIAN_POINT('Ctrl Pts',(-0.210347700874272,-2.36373416184737,
0.0844371338535079));
#41004=CARTESIAN_POINT('Ctrl Pts',(-0.131181919288033,-2.36944396338326,
0.0897402995039141));
#41005=CARTESIAN_POINT('Ctrl Pts',(-0.0519839748310875,-2.37118023964033,
0.0950434651543208));
#41006=CARTESIAN_POINT('Ctrl Pts',(0.0266910588187834,-2.37290505199357,
0.100311616226391));
#41007=CARTESIAN_POINT('Ctrl Pts',(0.105397349674217,-2.3707087231638,0.105579767298461));
#41008=CARTESIAN_POINT('Ctrl Pts',(0.183713167325577,-2.36462418465413,
0.110847918370531));
#41009=CARTESIAN_POINT('Ctrl Pts',(0.262809769913051,-2.35847898514194,
0.116168591310106));
#41010=CARTESIAN_POINT('Ctrl Pts',(0.341507573963179,-2.3483676763795,0.121489264249681));
#41011=CARTESIAN_POINT('Ctrl Pts',(0.41938164989237,-2.33437723905832,0.126809937189256));
#41012=CARTESIAN_POINT('Ctrl Pts',(0.49725572582156,-2.32038680173715,0.132130610128831));
#41013=CARTESIAN_POINT('Ctrl Pts',(0.57430560516479,-2.30251741176943,0.137451283068406));
#41014=CARTESIAN_POINT('Ctrl Pts',(0.650123141366246,-2.28090726763718,
0.142771956007981));
#41015=CARTESIAN_POINT('Ctrl Pts',(0.726320721013956,-2.25918880036411,
0.148119299385315));
#41016=CARTESIAN_POINT('Ctrl Pts',(0.801563345012648,-2.23360957253032,
0.15346664276265));
#41017=CARTESIAN_POINT('Ctrl Pts',(0.875433222024128,-2.20427192884101,
0.158813986139985));
#41018=CARTESIAN_POINT('Ctrl Pts',(0.949201129375983,-2.17497478270851,
0.164153948067584));
#41019=CARTESIAN_POINT('Ctrl Pts',(1.02159962420124,-2.14192969644625,0.169493909995184));
#41020=CARTESIAN_POINT('Ctrl Pts',(1.0922254709914,-2.105288954756,0.174833871922784));
#41021=CARTESIAN_POINT('Ctrl Pts',(1.1627745208271,-2.06868805538268,0.180168027296104));
#41022=CARTESIAN_POINT('Ctrl Pts',(1.2315543421985,-2.02849948476341,0.185502182669422));
#41023=CARTESIAN_POINT('Ctrl Pts',(1.29818246975213,-1.98492325739013,0.190836338042741));
#41024=CARTESIAN_POINT('Ctrl Pts',(1.36477125603836,-1.94137276005125,0.196167343808821));
#41025=CARTESIAN_POINT('Ctrl Pts',(1.42921048209172,-1.89443883140355,0.201498349574901));
#41026=CARTESIAN_POINT('Ctrl Pts',(1.49114410933806,-1.84436637024383,0.206829355340981));
#41027=CARTESIAN_POINT('Ctrl Pts',(1.55306012909141,-1.79430814449302,0.212158845522541));
#41028=CARTESIAN_POINT('Ctrl Pts',(1.61247160311578,-1.74111345109366,0.217488335704101));
#41029=CARTESIAN_POINT('Ctrl Pts',(1.66905438187736,-1.68506840598119,0.22281782588566));
#41030=CARTESIAN_POINT('Ctrl Pts',(1.7256383972715,-1.62902213598849,0.228147432544728));
#41031=CARTESIAN_POINT('Ctrl Pts',(1.77939326494072,-1.57012571929049,0.233477039203796));
#41032=CARTESIAN_POINT('Ctrl Pts',(1.83003166647521,-1.50870214495704,0.238806645862863));
#41033=CARTESIAN_POINT('Ctrl Pts',(1.88072081430783,-1.4472170161724,0.244141593484524));
#41034=CARTESIAN_POINT('Ctrl Pts',(1.9282869615661,-1.38320003164342,0.249476541106185));
#41035=CARTESIAN_POINT('Ctrl Pts',(1.97248347534309,-1.31700683445396,0.254811488727847));
#41036=CARTESIAN_POINT('Ctrl Pts',(2.01670221749346,-1.25078034579019,0.260149119529642));
#41037=CARTESIAN_POINT('Ctrl Pts',(2.05754771094884,-1.18237586412966,0.265486750331438));
#41038=CARTESIAN_POINT('Ctrl Pts',(2.09481835040345,-1.11217540941749,0.270824381133234));
#41039=CARTESIAN_POINT('Ctrl Pts',(2.13215413564378,-1.04185225051118,0.276171341642205));
#41040=CARTESIAN_POINT('Ctrl Pts',(2.16590238523173,-0.969727269235076,
0.281518302151176));
#41041=CARTESIAN_POINT('Ctrl Pts',(2.19590899540261,-0.896204076318512,
0.286865262660148));
#41042=CARTESIAN_POINT('Ctrl Pts',(2.22067994092979,-0.835509482815629,
0.291279265666469));
#41043=CARTESIAN_POINT('Ctrl Pts',(2.24290190653961,-0.773862515759138,
0.295693268672789));
#41044=CARTESIAN_POINT('Ctrl Pts',(2.26251409998074,-0.711497020294777,
0.30010727167911));
#41045=CARTESIAN_POINT('Ctrl Pts',(2.28620292971343,-0.636168087420177,
0.305438779649915));
#41046=CARTESIAN_POINT('Ctrl Pts',(2.30617025515604,-0.55951282801373,0.310770287620719));
#41047=CARTESIAN_POINT('Ctrl Pts',(2.3222700872644,-0.481933298597426,0.316101795591524));
#41048=CARTESIAN_POINT('Ctrl Pts',(2.33834675774283,-0.404465377074862,
0.321425633518702));
#41049=CARTESIAN_POINT('Ctrl Pts',(2.35056688962335,-0.32607628139956,0.326749471445881));
#41050=CARTESIAN_POINT('Ctrl Pts',(2.3588340904911,-0.247183729312878,0.33207330937306));
#41051=CARTESIAN_POINT('Ctrl Pts',(2.36709172107772,-0.168382504861136,
0.33739098431636));
#41052=CARTESIAN_POINT('Ctrl Pts',(2.3714054657222,-0.0890794461318766,
0.34270865925966));
#41053=CARTESIAN_POINT('Ctrl Pts',(2.37173015832874,-0.00970147277017596,
0.34802633420296));
#41054=CARTESIAN_POINT('Ctrl Pts',(2.3720546458506,0.0696263633028662,0.353340650358017));
#41055=CARTESIAN_POINT('Ctrl Pts',(2.36839508053346,0.14902855246632,0.358654966513075));
#41056=CARTESIAN_POINT('Ctrl Pts',(2.36075829608094,0.228075272629455,0.363969282668133));
#41057=CARTESIAN_POINT('Ctrl Pts',(2.35312395550452,0.307096696754529,0.369281898168901));
#41058=CARTESIAN_POINT('Ctrl Pts',(2.34151496834921,0.385762411435533,0.374594513669668));
#41059=CARTESIAN_POINT('Ctrl Pts',(2.32599014549971,0.463646315134985,0.379907129170436));
#41060=CARTESIAN_POINT('Ctrl Pts',(2.310465453176,0.54152956402124,0.385219700005098));
#41061=CARTESIAN_POINT('Ctrl Pts',(2.29102508376493,0.618630555491412,0.390532270839759));
#41062=CARTESIAN_POINT('Ctrl Pts',(2.26777893925327,0.694533473044543,0.395844841674421));
#41063=CARTESIAN_POINT('Ctrl Pts',(2.2445100106022,0.770510784983969,0.401162619495317));
#41064=CARTESIAN_POINT('Ctrl Pts',(2.21742799400823,0.845287228269891,0.406480397316214));
#41065=CARTESIAN_POINT('Ctrl Pts',(2.18669248809532,0.918462859895552,0.41179817513711));
#41066=CARTESIAN_POINT('Ctrl Pts',(2.15594205066763,0.991674040733512,0.417118536370114));
#41067=CARTESIAN_POINT('Ctrl Pts',(2.12153479162253,1.0632824376745,0.422438897603118));
#41068=CARTESIAN_POINT('Ctrl Pts',(2.0836771562134,1.13291110470965,0.427759258836121));
#41069=CARTESIAN_POINT('Ctrl Pts',(2.04575292380814,1.20266225853034,0.4330889793456));
#41070=CARTESIAN_POINT('Ctrl Pts',(2.00436643334651,1.2704263236269,0.438418699855078));
#41071=CARTESIAN_POINT('Ctrl Pts',(1.95976834177835,1.33585407476391,0.443748420364556));
#41072=CARTESIAN_POINT('Ctrl Pts',(1.92157161006786,1.39189069356813,0.448313142693117));
#41073=CARTESIAN_POINT('Ctrl Pts',(1.88101988697258,1.44621391972536,0.452877865021678));
#41074=CARTESIAN_POINT('Ctrl Pts',(1.838293254832,1.49862469342366,0.457442587350239));
#41075=CARTESIAN_POINT('Ctrl Pts',(1.78830766153796,1.5599396973699,0.462782824630466));
#41076=CARTESIAN_POINT('Ctrl Pts',(1.73515966602798,1.61886321765742,0.468123061910692));
#41077=CARTESIAN_POINT('Ctrl Pts',(1.67910660018427,1.67505196567677,0.473463299190919));
#41078=CARTESIAN_POINT('Ctrl Pts',(1.62313286426383,1.73116119174667,0.478795978622039));
#41079=CARTESIAN_POINT('Ctrl Pts',(1.56426255103442,1.7845430045804,0.48412865805316));
#41080=CARTESIAN_POINT('Ctrl Pts',(1.50279323671745,1.83488706741759,0.48946133748428));
#41081=CARTESIAN_POINT('Ctrl Pts',(1.4413935039843,1.88517414215156,0.494787980468028));
#41082=CARTESIAN_POINT('Ctrl Pts',(1.37740097674126,1.93243000641459,0.500114623451776));
#41083=CARTESIAN_POINT('Ctrl Pts',(1.31114898180007,1.97638215181797,0.505441266435525));
#41084=CARTESIAN_POINT('Ctrl Pts',(1.24493785724153,2.02030718345668,0.510764623451248));
#41085=CARTESIAN_POINT('Ctrl Pts',(1.17647042019243,2.0609322844446,0.516087980466972));
#41086=CARTESIAN_POINT('Ctrl Pts',(1.10611091149314,2.09802686207203,0.521411337482695));
#41087=CARTESIAN_POINT('Ctrl Pts',(1.03577308794568,2.13511000696546,0.526733053813212));
#41088=CARTESIAN_POINT('Ctrl Pts',(0.96354476380698,2.16866457193147,0.53205477014373));
#41089=CARTESIAN_POINT('Ctrl Pts',(0.88981556110165,2.19850547639103,0.537376486474247));
#41090=CARTESIAN_POINT('Ctrl Pts',(0.816086323548374,2.22834639495484,0.542698205320061));
#41091=CARTESIAN_POINT('Ctrl Pts',(0.740856639558851,2.25447347577933,0.548019924165875));
#41092=CARTESIAN_POINT('Ctrl Pts',(0.664535558446455,2.27674999814654,0.55334164301169));
#41093=CARTESIAN_POINT('Ctrl Pts',(0.588139649237234,2.29904836126533,0.558668579473493));
#41094=CARTESIAN_POINT('Ctrl Pts',(0.51065065500065,2.31748849433755,0.563995515935295));
#41095=CARTESIAN_POINT('Ctrl Pts',(0.432491633224321,2.33198392998129,0.569322452397098));
#41096=CARTESIAN_POINT('Ctrl Pts',(0.354294414425984,2.34648644967573,0.574651992181008));
#41097=CARTESIAN_POINT('Ctrl Pts',(0.275426979207465,2.35704036931227,0.579981531964919));
#41098=CARTESIAN_POINT('Ctrl Pts',(0.196318902637212,2.36361099823286,0.585311071748829));
#41099=CARTESIAN_POINT('Ctrl Pts',(0.117072958990159,2.37019307823962,0.590649899687661));
#41100=CARTESIAN_POINT('Ctrl Pts',(0.0375860038524554,2.37277798287157,
0.595988727626492));
#41101=CARTESIAN_POINT('Ctrl Pts',(-0.0417112580064065,2.3713831899243,
0.601327555565324));
#41102=CARTESIAN_POINT('Ctrl Pts',(-0.108303634743619,2.37021186855407,
0.605811004717334));
#41103=CARTESIAN_POINT('Ctrl Pts',(-0.174762115708698,2.36623487599976,
0.610294453869343));
#41104=CARTESIAN_POINT('Ctrl Pts',(-0.240835850885874,2.3594906559315,0.614777903021352));
#41105=CARTESIAN_POINT('Ctrl Pts',(-0.319526047864752,2.35145865949272,
0.620117445215696));
#41106=CARTESIAN_POINT('Ctrl Pts',(-0.397957859843874,2.33947115381473,
0.62545698741004));
#41107=CARTESIAN_POINT('Ctrl Pts',(-0.475703142599591,2.32355429947761,
0.630796529604384));
#41108=CARTESIAN_POINT('Ctrl Pts',(-0.553338566404695,2.3076599366519,0.636128526691405));
#41109=CARTESIAN_POINT('Ctrl Pts',(-0.630288933620861,2.28784734575792,
0.641460523778426));
#41110=CARTESIAN_POINT('Ctrl Pts',(-0.706131494106662,2.26419442087704,
0.646792520865447));
#41111=CARTESIAN_POINT('Ctrl Pts',(-0.781888514598013,2.24056817324769,
0.652118504191879));
#41112=CARTESIAN_POINT('Ctrl Pts',(-0.856539767648141,2.21311033818684,
0.657444487518312));
#41113=CARTESIAN_POINT('Ctrl Pts',(-0.929674440966726,2.18194947153072,
0.662770470844744));
#41114=CARTESIAN_POINT('Ctrl Pts',(-1.00276418804744,2.150807746828,0.668093182448162));
#41115=CARTESIAN_POINT('Ctrl Pts',(-1.07433877602337,2.11596768884218,0.673415894051581));
#41116=CARTESIAN_POINT('Ctrl Pts',(-1.14400540778191,2.07760672155866,0.678738605654999));
#41117=CARTESIAN_POINT('Ctrl Pts',(-1.21365076471705,2.03925746896242,0.684059691806655));
#41118=CARTESIAN_POINT('Ctrl Pts',(-1.28138891363587,1.9973896677277,0.689380777958311));
#41119=CARTESIAN_POINT('Ctrl Pts',(-1.34685112030407,1.95222696483674,0.694701864109966));
#41120=CARTESIAN_POINT('Ctrl Pts',(-1.41231355765948,1.90706410279353,0.700022969012999));
#41121=CARTESIAN_POINT('Ctrl Pts',(-1.47549965318234,1.85860658265147,0.70534407391603));
#41122=CARTESIAN_POINT('Ctrl Pts',(-1.53607038904226,1.80712086546738,0.710665178819062));
#41123=CARTESIAN_POINT('Ctrl Pts',(-1.59670085789442,1.75558437465636,0.715991531231694));
#41124=CARTESIAN_POINT('Ctrl Pts',(-1.65471045884588,1.70101402542165,0.721317883644325));
#41125=CARTESIAN_POINT('Ctrl Pts',(-1.70979445051785,1.64371560784656,0.726644236056956));
#41126=CARTESIAN_POINT('Ctrl Pts',(-1.76490552656311,1.58638901708205,0.731973207395934));
#41127=CARTESIAN_POINT('Ctrl Pts',(-1.81708782084753,1.52633203883876,0.737302178734913));
#41128=CARTESIAN_POINT('Ctrl Pts',(-1.8660762626614,1.46388436853177,0.74263115007389));
#41129=CARTESIAN_POINT('Ctrl Pts',(-1.91515038989168,1.40132747134522,0.747969442287575));
#41130=CARTESIAN_POINT('Ctrl Pts',(-1.96101923363549,1.33637191017052,0.753307734501259));
#41131=CARTESIAN_POINT('Ctrl Pts',(-2.00346068159012,1.26938700159662,0.758646026714944));
#41132=CARTESIAN_POINT('Ctrl Pts',(-2.03915044306756,1.21305821158582,0.763135090707457));
#41133=CARTESIAN_POINT('Ctrl Pts',(-2.07241726709839,1.1552950002603,0.76762415469997));
#41134=CARTESIAN_POINT('Ctrl Pts',(-2.10315499186712,1.09632893908919,0.772113218692483));
#41135=CARTESIAN_POINT('Ctrl Pts',(-2.14175463753469,1.02228087324364,0.777750470011304));
#41136=CARTESIAN_POINT('Ctrl Pts',(-2.17649347082348,0.946089393183921,
0.783387721330125));
#41137=CARTESIAN_POINT('Ctrl Pts',(-2.20714291909767,0.868169451879649,
0.789024972648946));
#41138=CARTESIAN_POINT('Ctrl Pts',(-2.23773470878619,0.790396095713576,
0.79465161901543));
#41139=CARTESIAN_POINT('Ctrl Pts',(-2.26425227792704,0.710901105848379,
0.800278265381915));
#41140=CARTESIAN_POINT('Ctrl Pts',(-2.28651336647709,0.630122755835394,
0.805904911748399));
#41141=CARTESIAN_POINT('Ctrl Pts',(-2.30871711961896,0.549552457628127,
0.811517066188068));
#41142=CARTESIAN_POINT('Ctrl Pts',(-2.32668612814396,0.467705755804625,
0.817129220627735));
#41143=CARTESIAN_POINT('Ctrl Pts',(-2.34028712478705,0.385037967031752,
0.822741375067404));
#41144=CARTESIAN_POINT('Ctrl Pts',(-2.35184842620135,0.314767585504852,
0.827511893784759));
#41145=CARTESIAN_POINT('Ctrl Pts',(-2.36025434182662,0.243904386798142,
0.832282412502115));
#41146=CARTESIAN_POINT('Ctrl Pts',(-2.36545134966535,0.172736721244678,
0.837052931219471));
#41147=CARTESIAN_POINT('',(1.37702479013102,-1.93106208855765,0.));
#41148=CARTESIAN_POINT('Origin',(0.,0.,0.));
#41149=CARTESIAN_POINT('Ctrl Pts',(1.37702479013101,-1.93106208855765,-2.44249065417534E-15));
#41150=CARTESIAN_POINT('Ctrl Pts',(1.44329081618841,-1.88380832019609,0.00546153625436459));
#41151=CARTESIAN_POINT('Ctrl Pts',(1.50716795013277,-1.83310728246389,0.0109230725087317));
#41152=CARTESIAN_POINT('Ctrl Pts',(1.56829444550799,-1.77922752752109,0.0163846087630988));
#41153=CARTESIAN_POINT('Ctrl Pts',(1.62938466103035,-1.7253797513392,0.0218429034815246));
#41154=CARTESIAN_POINT('Ctrl Pts',(1.68772716014062,-1.66835729997501,0.027301198199951));
#41155=CARTESIAN_POINT('Ctrl Pts',(1.74299340962789,-1.60846884846855,0.0327594929183768));
#41156=CARTESIAN_POINT('Ctrl Pts',(1.79825459974566,-1.5485858794728,0.0382172879551702));
#41157=CARTESIAN_POINT('Ctrl Pts',(1.85043979750689,-1.48583774573482,0.0436750829919633));
#41158=CARTESIAN_POINT('Ctrl Pts',(1.8992580012273,-1.42056928985322,0.0491328780287568));
#41159=CARTESIAN_POINT('Ctrl Pts',(1.94807564400118,-1.35530158394011,0.0545906103526478));
#41160=CARTESIAN_POINT('Ctrl Pts',(1.99352610807435,-1.28751396261289,0.0600483426765391));
#41161=CARTESIAN_POINT('Ctrl Pts',(2.03536010969931,-1.21758255832811,0.0655060750004302));
#41162=CARTESIAN_POINT('Ctrl Pts',(2.07720378652246,-1.14763498059184,0.0709650695665131));
#41163=CARTESIAN_POINT('Ctrl Pts',(2.11542911331289,-1.07554300813758,0.0764240641325964));
#41164=CARTESIAN_POINT('Ctrl Pts',(2.14983194318074,-1.00170887915588,0.0818830586986794));
#41165=CARTESIAN_POINT('Ctrl Pts',(2.18425108443838,-0.927839743249973,
0.087344641534058));
#41166=CARTESIAN_POINT('Ctrl Pts',(2.21484393973068,-0.85222720308178,0.0928062243694362));
#41167=CARTESIAN_POINT('Ctrl Pts',(2.2414542624766,-0.775294042106259,0.0982678072048149));
#41168=CARTESIAN_POINT('Ctrl Pts',(2.26810339717719,-0.698248671805628,
0.103737355922737));
#41169=CARTESIAN_POINT('Ctrl Pts',(2.29075825754318,-0.619879247457034,
0.109206904640659));
#41170=CARTESIAN_POINT('Ctrl Pts',(2.30931234658886,-0.540624221055853,
0.11467645335858));
#41171=CARTESIAN_POINT('Ctrl Pts',(2.32788094035391,-0.461307236780397,
0.120150277913975));
#41172=CARTESIAN_POINT('Ctrl Pts',(2.34234229640014,-0.381103699970898,
0.125624102469369));
#41173=CARTESIAN_POINT('Ctrl Pts',(2.35264140166807,-0.300460476031863,
0.131097927024764));
#41174=CARTESIAN_POINT('Ctrl Pts',(2.36295968183619,-0.219667110334866,
0.136581942760538));
#41175=CARTESIAN_POINT('Ctrl Pts',(2.36910019563012,-0.138432857311421,
0.142065958496312));
#41176=CARTESIAN_POINT('Ctrl Pts',(2.37105995620251,-0.0572079242145295,
0.147549974232085));
#41177=CARTESIAN_POINT('Ctrl Pts',(2.37220213875243,-0.00986862036883413,
0.150746153992562));
#41178=CARTESIAN_POINT('Ctrl Pts',(2.37192519994692,0.0374675362085513,
0.15394233375304));
#41179=CARTESIAN_POINT('Ctrl Pts',(2.37023667769141,0.084712184639374,0.157138513513516));
#41180=CARTESIAN_POINT('Ctrl Pts',(2.36744413080288,0.162847308736816,0.162424485798573));
#41181=CARTESIAN_POINT('Ctrl Pts',(2.36077748227605,0.241017935962905,0.167710458083629));
#41182=CARTESIAN_POINT('Ctrl Pts',(2.35022604973245,0.318803352647091,0.172996430368686));
#41183=CARTESIAN_POINT('Ctrl Pts',(2.33969127462521,0.396465970306297,0.1782740577445));
#41184=CARTESIAN_POINT('Ctrl Pts',(2.32528395068704,0.473744115683103,0.183551685120315));
#41185=CARTESIAN_POINT('Ctrl Pts',(2.30704538116865,0.55021784024912,0.188829312496129));
#41186=CARTESIAN_POINT('Ctrl Pts',(2.28883093718442,0.626590407240669,0.194099958755391));
#41187=CARTESIAN_POINT('Ctrl Pts',(2.26679542482695,0.702160205168564,0.199370605014654));
#41188=CARTESIAN_POINT('Ctrl Pts',(2.24103162067994,0.776514866317857,0.204641251273917));
#41189=CARTESIAN_POINT('Ctrl Pts',(2.2152865989447,0.850815321191758,0.209908055109609));
#41190=CARTESIAN_POINT('Ctrl Pts',(2.18581883281674,0.923901946362171,0.2151748589453));
#41191=CARTESIAN_POINT('Ctrl Pts',(2.15277128772683,0.995376233008883,0.220441662780992));
#41192=CARTESIAN_POINT('Ctrl Pts',(2.1197370814658,1.0668216708175,0.225706340800837));
#41193=CARTESIAN_POINT('Ctrl Pts',(2.08312616405238,1.13665562810727,0.230971018820683));
#41194=CARTESIAN_POINT('Ctrl Pts',(2.0431295094889,1.20449984223977,0.236235696840528));
#41195=CARTESIAN_POINT('Ctrl Pts',(2.00313598427935,1.27233874821438,0.241499962949903));
#41196=CARTESIAN_POINT('Ctrl Pts',(1.95975749191866,1.33818780901973,0.246764229059279));
#41197=CARTESIAN_POINT('Ctrl Pts',(1.91323000399408,1.40169505040034,0.252028495168653));
#41198=CARTESIAN_POINT('Ctrl Pts',(1.86665894877539,1.46526175853462,0.257297690618512));
#41199=CARTESIAN_POINT('Ctrl Pts',(1.81693329080277,1.52648188012333,0.26256688606837));
#41200=CARTESIAN_POINT('Ctrl Pts',(1.76433079845327,1.58503466716954,0.267836081518229));
#41201=CARTESIAN_POINT('Ctrl Pts',(1.71170476509385,1.64361365814029,0.273107635072747));
#41202=CARTESIAN_POINT('Ctrl Pts',(1.65619967103344,1.69952259795037,0.278379188627265));
#41203=CARTESIAN_POINT('Ctrl Pts',(1.5981299772164,1.75247785675663,0.283650742181783));
#41204=CARTESIAN_POINT('Ctrl Pts',(1.53995581739583,1.805528380819,0.288931779136265));
#41205=CARTESIAN_POINT('Ctrl Pts',(1.47920821056172,1.85561430383625,0.294212816090746));
#41206=CARTESIAN_POINT('Ctrl Pts',(1.41623422365411,1.9024927558997,0.299493853045228));
#41207=CARTESIAN_POINT('Ctrl Pts',(1.35747332670612,1.94623494257153,0.304421577705825));
#41208=CARTESIAN_POINT('Ctrl Pts',(1.2967745557132,1.98718474081386,0.309349302366423));
#41209=CARTESIAN_POINT('Ctrl Pts',(1.23443937156907,2.02518085622499,0.314277027027021));
#41210=CARTESIAN_POINT('Ctrl Pts',(1.16679049745889,2.06641590611558,0.319624809820821));
#41211=CARTESIAN_POINT('Ctrl Pts',(1.09695195078784,2.10433161823903,0.324972592614622));
#41212=CARTESIAN_POINT('Ctrl Pts',(1.02528200200408,2.13868999129526,0.330320375408422));
#41213=CARTESIAN_POINT('Ctrl Pts',(0.953712963733243,2.17299998813374,0.335660628581874));
#41214=CARTESIAN_POINT('Ctrl Pts',(0.880318061697311,2.20376239492551,0.341000881755326));
#41215=CARTESIAN_POINT('Ctrl Pts',(0.805482457184367,2.23078373529758,0.346341134928778));
#41216=CARTESIAN_POINT('Ctrl Pts',(0.730731435113846,2.25777453498009,0.351675352316731));
#41217=CARTESIAN_POINT('Ctrl Pts',(0.654543382842364,2.28103251516069,0.357009569704682));
#41218=CARTESIAN_POINT('Ctrl Pts',(0.577324500590568,2.30041180737664,0.362343787092635));
#41219=CARTESIAN_POINT('Ctrl Pts',(0.50015322956025,2.31977915080822,0.36767471553625));
#41220=CARTESIAN_POINT('Ctrl Pts',(0.421952840784171,2.33527244119564,0.373005643979866));
#41221=CARTESIAN_POINT('Ctrl Pts',(0.343144670295126,2.34679564464997,0.378336572423482));
#41222=CARTESIAN_POINT('Ctrl Pts',(0.264360971746756,2.35831526985664,0.383665845478274));
#41223=CARTESIAN_POINT('Ctrl Pts',(0.184970326640474,2.36586718957559,0.388995118533067));
#41224=CARTESIAN_POINT('Ctrl Pts',(0.105402811188834,2.36940674218115,0.394324391587859));
#41225=CARTESIAN_POINT('Ctrl Pts',(0.0258356529750808,2.37294627889502,
0.399653640715572));
#41226=CARTESIAN_POINT('Ctrl Pts',(-0.0539079089206988,2.37247346521709,
0.404982889843285));
#41227=CARTESIAN_POINT('Ctrl Pts',(-0.133395599791717,2.3679957087073,0.410312138970998));
#41228=CARTESIAN_POINT('Ctrl Pts',(-0.212959413064762,2.36351366401683,
0.41564649172218));
#41229=CARTESIAN_POINT('Ctrl Pts',(-0.292266400132336,2.3550190420733,0.420980844473363));
#41230=CARTESIAN_POINT('Ctrl Pts',(-0.370887824258233,2.34257129759523,
0.426315197224544));
#41231=CARTESIAN_POINT('Ctrl Pts',(-0.449547011114101,2.33011757432933,
0.4316521121237));
#41232=CARTESIAN_POINT('Ctrl Pts',(-0.527519522867585,2.31370704118153,
0.436989027022855));
#41233=CARTESIAN_POINT('Ctrl Pts',(-0.604387690555749,2.29345014814028,
0.44232594192201));
#41234=CARTESIAN_POINT('Ctrl Pts',(-0.68138671233925,2.27315877141752,0.447671941949536));
#41235=CARTESIAN_POINT('Ctrl Pts',(-0.757277189581784,2.24900809422682,
0.453017941977062));
#41236=CARTESIAN_POINT('Ctrl Pts',(-0.83165774481026,2.22115813439681,0.458363942004587));
#41237=CARTESIAN_POINT('Ctrl Pts',(-0.892188056615047,2.19849405576654,
0.462714474849906));
#41238=CARTESIAN_POINT('Ctrl Pts',(-0.95171866636475,2.17338107488758,0.467065007695225));
#41239=CARTESIAN_POINT('Ctrl Pts',(-1.01004516747242,2.14592796294881,0.471415540540543));
#41240=CARTESIAN_POINT('Ctrl Pts',(-1.08174595762753,2.11217984192586,0.476763652233876));
#41241=CARTESIAN_POINT('Ctrl Pts',(-1.15187962006272,2.07477490174953,0.482111763927208));
#41242=CARTESIAN_POINT('Ctrl Pts',(-1.22005032815419,2.03388182037965,0.48745987562054));
#41243=CARTESIAN_POINT('Ctrl Pts',(-1.28812716923514,1.99304504635067,0.492800623282156));
#41244=CARTESIAN_POINT('Ctrl Pts',(-1.35424602863012,1.9487299090355,0.498141370943772));
#41245=CARTESIAN_POINT('Ctrl Pts',(-1.41803353126763,1.90115201041386,0.503482118605387));
#41246=CARTESIAN_POINT('Ctrl Pts',(-1.4817519108599,1.85362566937172,0.50881707878941));
#41247=CARTESIAN_POINT('Ctrl Pts',(-1.54314358348597,1.80284387121132,0.514152038973432));
#41248=CARTESIAN_POINT('Ctrl Pts',(-1.60186339745384,1.74906595598841,0.519486999157454));
#41249=CARTESIAN_POINT('Ctrl Pts',(-1.66054868190695,1.69531966425324,0.524818822179181));
#41250=CARTESIAN_POINT('Ctrl Pts',(-1.71656488456289,1.63858106693363,0.530150645200908));
#41251=CARTESIAN_POINT('Ctrl Pts',(-1.7696001976057,1.57914951892905,0.535482468222635));
#41252=CARTESIAN_POINT('Ctrl Pts',(-1.82262054620086,1.51973474013423,0.540812786816804));
#41253=CARTESIAN_POINT('Ctrl Pts',(-1.87266136618552,1.45762886700911,0.546143105410973));
#41254=CARTESIAN_POINT('Ctrl Pts',(-1.91944898854585,1.39316676778853,0.551473424005142));
#41255=CARTESIAN_POINT('Ctrl Pts',(-1.96623772002074,1.32870314047463,0.556803868956105));
#41256=CARTESIAN_POINT('Ctrl Pts',(-2.00977282860423,1.26188355369521,0.562134313907067));
#41257=CARTESIAN_POINT('Ctrl Pts',(-2.04982295656368,1.19307330422088,0.567464758858029));
#41258=CARTESIAN_POINT('Ctrl Pts',(-2.08991314485198,1.1241942269709,0.572800535611623));
#41259=CARTESIAN_POINT('Ctrl Pts',(-2.12651115585645,1.05332091333084,0.578136312365216));
#41260=CARTESIAN_POINT('Ctrl Pts',(-2.15943106457146,0.980844299501093,
0.583472089118809));
#41261=CARTESIAN_POINT('Ctrl Pts',(-2.19236757196774,0.908331141942655,
0.588810556246135));
#41262=CARTESIAN_POINT('Ctrl Pts',(-2.22162211137489,0.834213507035436,
0.594149023373461));
#41263=CARTESIAN_POINT('Ctrl Pts',(-2.24705745683915,0.758901079300586,
0.599487490500786));
#41264=CARTESIAN_POINT('Ctrl Pts',(-2.27253702841281,0.683457700890284,
0.604835239972304));
#41265=CARTESIAN_POINT('Ctrl Pts',(-2.29418401214726,0.606815827876289,
0.610182989443822));
#41266=CARTESIAN_POINT('Ctrl Pts',(-2.31191155015882,0.529398759672008,
0.615530738915341));
#41267=CARTESIAN_POINT('Ctrl Pts',(-2.32630210923964,0.466554449698934,
0.619871843961577));
#41268=CARTESIAN_POINT('Ctrl Pts',(-2.3381108747471,0.40319963826319,0.624212949007814));
#41269=CARTESIAN_POINT('Ctrl Pts',(-2.34731653972495,0.339563138213948,
0.62855405405405));
#41270=CARTESIAN_POINT('Ctrl Pts',(-2.35532395883693,0.284209817411997,
0.632330103649382));
#41271=CARTESIAN_POINT('Ctrl Pts',(-2.36137449625126,0.228565026548074,
0.636106153244714));
#41272=CARTESIAN_POINT('Ctrl Pts',(-2.36545134966535,0.172736721244682,
0.639882202840047));
#41273=CARTESIAN_POINT('Origin',(0.,0.,-1.84858989190501));
#41274=CARTESIAN_POINT('',(-2.36545132977957,0.17273699355969,1.83684621836633));
#41275=CARTESIAN_POINT('',(-2.3654513498954,0.172736718094382,1.63785909343774));
#41276=CARTESIAN_POINT('',(-2.36545134966535,0.172736721244682,-1.84858989190501));
#41277=CARTESIAN_POINT('',(-2.37174999149347,0.00019724836186693,0.848751148665265));
#41278=CARTESIAN_POINT('Ctrl Pts',(-2.36545132977956,0.172736993559942,
1.83684621836632));
#41279=CARTESIAN_POINT('Ctrl Pts',(-2.35464804740561,0.320676575758163,
1.8277274167204));
#41280=CARTESIAN_POINT('Ctrl Pts',(-2.32998181411189,0.467398739448049,
1.81858518484146));
#41281=CARTESIAN_POINT('Ctrl Pts',(-2.28259556239425,0.645140233773284,
1.80672465140104));
#41282=CARTESIAN_POINT('Ctrl Pts',(-2.27272401047721,0.679097774815498,
1.80442343594766));
#41283=CARTESIAN_POINT('Ctrl Pts',(-2.25564957646514,0.73328256320601,1.80068757430668));
#41284=CARTESIAN_POINT('Ctrl Pts',(-2.2489245512852,0.753655519605635,1.79926820645086));
#41285=CARTESIAN_POINT('Ctrl Pts',(-2.2354785472076,0.792605774192321,1.79652475289482));
#41286=CARTESIAN_POINT('Ctrl Pts',(-2.22879999767541,0.811195894221982,
1.79520213923863));
#41287=CARTESIAN_POINT('Ctrl Pts',(-2.21267165189738,0.85438670407692,1.79209722876589));
#41288=CARTESIAN_POINT('Ctrl Pts',(-2.2030426526902,0.87891720555185,1.79030920336862));
#41289=CARTESIAN_POINT('Ctrl Pts',(-2.16907136675365,0.961393474542494,
1.78421130849708));
#41290=CARTESIAN_POINT('Ctrl Pts',(-2.14283715579601,1.01852624007698,1.77984046139933));
#41291=CARTESIAN_POINT('Ctrl Pts',(-2.06996539938773,1.16191488806456,1.76848579076181));
#41292=CARTESIAN_POINT('Ctrl Pts',(-2.02019466103313,1.24644026871397,1.76141583426954));
#41293=CARTESIAN_POINT('Ctrl Pts',(-1.88198291394013,1.45103935633154,1.74346126613437));
#41294=CARTESIAN_POINT('Ctrl Pts',(-1.78718026286442,1.56632298732763,1.73252966648431));
#41295=CARTESIAN_POINT('Ctrl Pts',(-1.66566776307086,1.6885786939201,1.7204796952185));
#41296=CARTESIAN_POINT('Ctrl Pts',(-1.64890356547969,1.70495285413968,1.71885569819598));
#41297=CARTESIAN_POINT('Ctrl Pts',(-1.62256842834581,1.72992343132611,1.71636698809508));
#41298=CARTESIAN_POINT('Ctrl Pts',(-1.61316609545785,1.7386944959781,1.71549042383356));
#41299=CARTESIAN_POINT('Ctrl Pts',(-1.59548765626292,1.75491915122687,1.71386523393306));
#41300=CARTESIAN_POINT('Ctrl Pts',(-1.58723005301484,1.76239123153072,1.71311535360085));
#41301=CARTESIAN_POINT('Ctrl Pts',(-1.5673305219545,1.78014446125934,1.71132968584785));
#41302=CARTESIAN_POINT('Ctrl Pts',(-1.55563975286473,1.79036986653117,1.71029784306977));
#41303=CARTESIAN_POINT('Ctrl Pts',(-1.51381833989229,1.82623027357081,1.70666364432644));
#41304=CARTESIAN_POINT('Ctrl Pts',(-1.4831461024168,1.85122689995472,1.7041016511453));
#41305=CARTESIAN_POINT('Ctrl Pts',(-1.40135799279215,1.91454248028618,1.69749204081709));
#41306=CARTESIAN_POINT('Ctrl Pts',(-1.34929319965399,1.9515855140747,1.69350107331283));
#41307=CARTESIAN_POINT('Ctrl Pts',(-1.1280557030759,2.09589987375625,1.67714158346809));
#41308=CARTESIAN_POINT('Ctrl Pts',(-0.947149752408485,2.18362302817075,
1.66507327098708));
#41309=CARTESIAN_POINT('Ctrl Pts',(-0.722521704518835,2.25931695648376,
1.64981128904514));
#41310=CARTESIAN_POINT('Ctrl Pts',(-0.687401910936438,2.27024868784409,
1.64742046279927));
#41311=CARTESIAN_POINT('Ctrl Pts',(-0.631137911039719,2.2863367601363,1.64357502739875));
#41312=CARTESIAN_POINT('Ctrl Pts',(-0.610151609211697,2.29202657175618,
1.64213740362893));
#41313=CARTESIAN_POINT('Ctrl Pts',(-0.570036573505999,2.30231259684495,
1.63938167749373));
#41314=CARTESIAN_POINT('Ctrl Pts',(-0.550923001188113,2.30696094378568,
1.63806535251114));
#41315=CARTESIAN_POINT('Ctrl Pts',(-0.506681300738281,2.31713919530339,
1.6350098310146));
#41316=CARTESIAN_POINT('Ctrl Pts',(-0.481516985704815,2.32249893317183,
1.63326546406677));
#41317=CARTESIAN_POINT('Ctrl Pts',(-0.398656387857117,2.33874286640403,
1.62749834876422));
#41318=CARTESIAN_POINT('Ctrl Pts',(-0.340646599130598,2.34789352304172,
1.62342336536928));
#41319=CARTESIAN_POINT('Ctrl Pts',(-0.195052606014149,2.36535090716893,
1.61309893372714));
#41320=CARTESIAN_POINT('Ctrl Pts',(-0.107237002091558,2.37095512134007,
1.60678289174567));
#41321=CARTESIAN_POINT('Ctrl Pts',(0.119026523861113,2.37279830575996,1.59036990779681));
#41322=CARTESIAN_POINT('Ctrl Pts',(0.257208585780112,2.36181813063321,1.58020166716128));
#41323=CARTESIAN_POINT('Ctrl Pts',(0.434056895759979,2.3320531299917,1.56745246526195));
#41324=CARTESIAN_POINT('Ctrl Pts',(0.474285525021769,2.32420543229086,1.56457202356149));
#41325=CARTESIAN_POINT('Ctrl Pts',(0.530052594517722,2.31181809885717,1.56062403552056));
#41326=CARTESIAN_POINT('Ctrl Pts',(0.545776387002374,2.30815659049947,1.55951593499902));
#41327=CARTESIAN_POINT('Ctrl Pts',(0.572369449341775,2.301677064512,1.55765180784972));
#41328=CARTESIAN_POINT('Ctrl Pts',(0.58325812904105,2.29894194623905,1.55689140381995));
#41329=CARTESIAN_POINT('Ctrl Pts',(0.606285120919396,2.29298367127748,1.55528984356908));
#41330=CARTESIAN_POINT('Ctrl Pts',(0.618417838186489,2.28974128661817,1.55444974049966));
#41331=CARTESIAN_POINT('Ctrl Pts',(0.652357883281247,2.28038159105728,1.55210867908778));
#41332=CARTESIAN_POINT('Ctrl Pts',(0.67410480187661,2.27404789200983,1.55061916582575));
#41333=CARTESIAN_POINT('Ctrl Pts',(0.799742383327257,2.23549567465549,1.54205718662485));
#41334=CARTESIAN_POINT('Ctrl Pts',(0.901420676276634,2.19646876201649,1.53529754222402));
#41335=CARTESIAN_POINT('Ctrl Pts',(1.16622545863182,2.07332913834315,1.51729376176956));
#41336=CARTESIAN_POINT('Ctrl Pts',(1.32285040011715,1.97707761353991,1.50616207489864));
#41337=CARTESIAN_POINT('Ctrl Pts',(1.49464348893898,1.84187176215918,1.49206666883163));
#41338=CARTESIAN_POINT('Ctrl Pts',(1.52196143823089,1.81936360306158,1.48976336520943));
#41339=CARTESIAN_POINT('Ctrl Pts',(1.56501858401806,1.78223890114579,1.48602487214174));
#41340=CARTESIAN_POINT('Ctrl Pts',(1.58108128568205,1.76800469099866,1.48460499728036));
#41341=CARTESIAN_POINT('Ctrl Pts',(1.61155250686322,1.74025479667892,1.48186105875631));
#41342=CARTESIAN_POINT('Ctrl Pts',(1.62598972051335,1.726773183908,1.48053847378397));
#41343=CARTESIAN_POINT('Ctrl Pts',(1.65928205316862,1.6948967343755,1.47743438854282));
#41344=CARTESIAN_POINT('Ctrl Pts',(1.67800214005842,1.67636529277775,1.47564717165789));
#41345=CARTESIAN_POINT('Ctrl Pts',(1.74027007152932,1.61263666922781,1.4695561952939));
#41346=CARTESIAN_POINT('Ctrl Pts',(1.78232823487315,1.56602739057756,1.46519165738248));
#41347=CARTESIAN_POINT('Ctrl Pts',(1.88505892168161,1.44267508313141,1.45385986364717));
#41348=CARTESIAN_POINT('Ctrl Pts',(1.94292055342253,1.36375038880253,1.44680695292137));
#41349=CARTESIAN_POINT('Ctrl Pts',(2.07643395921466,1.15582142048797,1.42883895203757));
#41350=CARTESIAN_POINT('Ctrl Pts',(2.14508106227687,1.02280715781205,1.41787522279012));
#41351=CARTESIAN_POINT('Ctrl Pts',(2.20948528617555,0.862507949569433,1.405799169735));
#41352=CARTESIAN_POINT('Ctrl Pts',(2.21788446555892,0.840674604372123,1.40417807212877));
#41353=CARTESIAN_POINT('Ctrl Pts',(2.23039516910707,0.806660124877918,1.40169280594942));
#41354=CARTESIAN_POINT('Ctrl Pts',(2.23473276105734,0.794564454924873,1.40081683620472));
#41355=CARTESIAN_POINT('Ctrl Pts',(2.242646454656,0.771919039650832,1.3991921427615));
#41356=CARTESIAN_POINT('Ctrl Pts',(2.2462467040576,0.761378929568453,1.39844217282981));
#41357=CARTESIAN_POINT('Ctrl Pts',(2.25469406728847,0.736066844893238,1.39665543138161));
#41358=CARTESIAN_POINT('Ctrl Pts',(2.25947041125486,0.721271952624277,1.39562261907189));
#41359=CARTESIAN_POINT('Ctrl Pts',(2.27591681237142,0.668561452349381,1.39198025899634));
#41360=CARTESIAN_POINT('Ctrl Pts',(2.28678137634935,0.630399167458296,1.38941132134774));
#41361=CARTESIAN_POINT('Ctrl Pts',(2.31269378923288,0.529867653087519,1.38277780427696));
#41362=CARTESIAN_POINT('Ctrl Pts',(2.32617823563843,0.467127544589651,1.37877039518622));
#41363=CARTESIAN_POINT('Ctrl Pts',(2.37109181040211,0.207251502796512,1.36243890650623));
#41364=CARTESIAN_POINT('Ctrl Pts',(2.38012086018376,0.00710148455932806,
1.35040995572103));
#41365=CARTESIAN_POINT('Ctrl Pts',(2.36099495772909,-0.228613223734846,
1.33518557292967));
#41366=CARTESIAN_POINT('Ctrl Pts',(2.35715029368854,-0.265336494569707,
1.33278578873205));
#41367=CARTESIAN_POINT('Ctrl Pts',(2.34967853496698,-0.323547236235964,
1.32892950709386));
#41368=CARTESIAN_POINT('Ctrl Pts',(2.34660972503881,-0.345101113126554,
1.32749017331415));
#41369=CARTESIAN_POINT('Ctrl Pts',(2.3402056851717,-0.386033626716818,1.32473342967413));
#41370=CARTESIAN_POINT('Ctrl Pts',(2.33692531641986,-0.405419086950399,
1.32341782769056));
#41371=CARTESIAN_POINT('Ctrl Pts',(2.32880791734409,-0.450011629192578,
1.32036734362408));
#41372=CARTESIAN_POINT('Ctrl Pts',(2.32380202601752,-0.475185056562063,
1.31862734446474));
#41373=CARTESIAN_POINT('Ctrl Pts',(2.30608680057119,-0.55728204188785,1.31289157957098));
#41374=CARTESIAN_POINT('Ctrl Pts',(2.29168712816545,-0.613814892254642,
1.30884435797765));
#41375=CARTESIAN_POINT('Ctrl Pts',(2.25064268309215,-0.753246518820026,
1.29861331140109));
#41376=CARTESIAN_POINT('Ctrl Pts',(2.2214907019716,-0.835313984454225,1.29236450136531));
#41377=CARTESIAN_POINT('Ctrl Pts',(2.13543055612175,-1.04096422827599,1.27619811812788));
#41378=CARTESIAN_POINT('Ctrl Pts',(2.07228291301253,-1.16160032931202,1.26621050543948));
#41379=CARTESIAN_POINT('Ctrl Pts',(1.97551187223355,-1.31319488213282,1.25339818423819));
#41380=CARTESIAN_POINT('Ctrl Pts',(1.95084819330827,-1.34956283179926,1.25030446045176));
#41381=CARTESIAN_POINT('Ctrl Pts',(1.91551449459827,-1.39866955941618,1.24612014442449));
#41382=CARTESIAN_POINT('Ctrl Pts',(1.90570137134627,-1.41201084877623,1.24498263784939));
#41383=CARTESIAN_POINT('Ctrl Pts',(1.88902868851754,-1.43418748435966,1.24309206880024));
#41384=CARTESIAN_POINT('Ctrl Pts',(1.88224503683565,-1.44307891971692,1.24233415629681));
#41385=CARTESIAN_POINT('Ctrl Pts',(1.8678449097303,-1.46167906951128,1.24074932216542));
#41386=CARTESIAN_POINT('Ctrl Pts',(1.86021517904386,-1.47137684279918,1.23992330908665));
#41387=CARTESIAN_POINT('Ctrl Pts',(1.8390138662032,-1.49789625328526,1.23766392946694));
#41388=CARTESIAN_POINT('Ctrl Pts',(1.82528713287918,-1.51459306337046,1.23624076231451));
#41389=CARTESIAN_POINT('Ctrl Pts',(1.79359239987193,-1.55208879144417,1.23303720058768));
#41390=CARTESIAN_POINT('Ctrl Pts',(1.77548706839401,-1.57276797893649,1.23126494883763));
#41391=CARTESIAN_POINT('Ctrl Pts',(1.71375476790853,-1.64085113825727,1.22539329143886));
#41392=CARTESIAN_POINT('Ctrl Pts',(1.66855475869492,-1.68679397789092,1.22136928279714));
#41393=CARTESIAN_POINT('Ctrl Pts',(1.47635145197169,-1.86685945081195,1.20506183220831));
#41394=CARTESIAN_POINT('Ctrl Pts',(1.31464165814232,-1.98405928836357,1.19306871053852));
#41395=CARTESIAN_POINT('Ctrl Pts',(1.10770064399898,-2.09751547300224,1.17787772412464));
#41396=CARTESIAN_POINT('Ctrl Pts',(1.07478804155704,-2.11456905898879,1.17546880631996));
#41397=CARTESIAN_POINT('Ctrl Pts',(1.02190320813182,-2.1404175349209,1.171601232347));
#41398=CARTESIAN_POINT('Ctrl Pts',(1.0021851697813,-2.14972049904551,1.1701599156739));
#41399=CARTESIAN_POINT('Ctrl Pts',(0.964450889725479,-2.16689153553028,
1.16740150302429));
#41400=CARTESIAN_POINT('Ctrl Pts',(0.946459517789672,-2.17481005777178,
1.16608624425905));
#41401=CARTESIAN_POINT('Ctrl Pts',(0.904802392982881,-2.1925297601584,1.16303968855379));
#41402=CARTESIAN_POINT('Ctrl Pts',(0.881072497691933,-2.20217285554434,
1.16130332308496));
#41403=CARTESIAN_POINT('Ctrl Pts',(0.803130633843565,-2.23238459540515,
1.15559493610862));
#41404=CARTESIAN_POINT('Ctrl Pts',(0.748323476888627,-2.2513486618235,1.15157215961699));
#41405=CARTESIAN_POINT('Ctrl Pts',(0.610396831172572,-2.29348035447054,
1.14142296165023));
#41406=CARTESIAN_POINT('Ctrl Pts',(0.526607457732485,-2.31415614238286,
1.13523297528626));
#41407=CARTESIAN_POINT('Ctrl Pts',(0.310403281285454,-2.35515540625786,
1.11927933476394));
#41408=CARTESIAN_POINT('Ctrl Pts',(0.177046256836943,-2.36891601756291,
1.10944685395313));
#41409=CARTESIAN_POINT('Ctrl Pts',(-0.00323629014956441,-2.3722032443458,
1.09658012018351));
#41410=CARTESIAN_POINT('Ctrl Pts',(-0.0497297408774496,-2.37168427538983,
1.09330174506795));
#41411=CARTESIAN_POINT('Ctrl Pts',(-0.113076200900375,-2.36911328318783,
1.08891403328352));
#41412=CARTESIAN_POINT('Ctrl Pts',(-0.12996405346272,-2.3682468961745,1.08775198206795));
#41413=CARTESIAN_POINT('Ctrl Pts',(-0.158068013671682,-2.36650355561102,
1.08583251261782));
#41414=CARTESIAN_POINT('Ctrl Pts',(-0.169289546561466,-2.36572729742231,
1.08506992399689));
#41415=CARTESIAN_POINT('Ctrl Pts',(-0.192694447740749,-2.36394085050548,
1.08348788754328));
#41416=CARTESIAN_POINT('Ctrl Pts',(-0.204876206756606,-2.36291625987324,
1.08266920595484));
#41417=CARTESIAN_POINT('Ctrl Pts',(-0.238006403714775,-2.35987158577458,
1.08045424470994));
#41418=CARTESIAN_POINT('Ctrl Pts',(-0.25893728863444,-2.35766674993709,
1.07906749155779));
#41419=CARTESIAN_POINT('Ctrl Pts',(-0.306183623860976,-2.35205306061748,
1.07596017688574));
#41420=CARTESIAN_POINT('Ctrl Pts',(-0.332477092089665,-2.34848059715367,
1.07424704437971));
#41421=CARTESIAN_POINT('Ctrl Pts',(-0.418852426913508,-2.33526507357372,
1.0686564357062));
#41422=CARTESIAN_POINT('Ctrl Pts',(-0.478626152164646,-2.3237509001182,
1.0648467014174));
#41423=CARTESIAN_POINT('Ctrl Pts',(-0.740448165038656,-2.26278310196466,
1.04817166483396));
#41424=CARTESIAN_POINT('Ctrl Pts',(-0.93590276929647,-2.18918563957954,
1.03566627579771));
#41425=CARTESIAN_POINT('Ctrl Pts',(-1.15019441625413,-2.07448364215316,
1.01998979754206));
#41426=CARTESIAN_POINT('Ctrl Pts',(-1.18076124768336,-2.05723898711783,
1.01770543780304));
#41427=CARTESIAN_POINT('Ctrl Pts',(-1.22933840958818,-2.02839427546507,
1.01398974945035));
#41428=CARTESIAN_POINT('Ctrl Pts',(-1.2475944629091,-2.01721696125745,1.01257337151276));
#41429=CARTESIAN_POINT('Ctrl Pts',(-1.28242628158196,-1.99523738906493,
1.00983083738293));
#41430=CARTESIAN_POINT('Ctrl Pts',(-1.29902313477684,-1.98447178405137,
1.00850609029389));
#41431=CARTESIAN_POINT('Ctrl Pts',(-1.33753656318517,-1.95879975139335,
1.0053885364006));
#41432=CARTESIAN_POINT('Ctrl Pts',(-1.35934140348433,-1.94373130232705,
1.00358987253713));
#41433=CARTESIAN_POINT('Ctrl Pts',(-1.43279842120747,-1.89112751344668,
0.997411981686479));
#41434=CARTESIAN_POINT('Ctrl Pts',(-1.48318167605389,-1.85187618865771,
0.992969601369592));
#41435=CARTESIAN_POINT('Ctrl Pts',(-1.60868449666613,-1.74569301666673,
0.981357150716677));
#41436=CARTESIAN_POINT('Ctrl Pts',(-1.68123734883176,-1.6759318505116,0.974095627242334));
#41437=CARTESIAN_POINT('Ctrl Pts',(-1.8466793688405,-1.49527011490924,0.956274130076739));
#41438=CARTESIAN_POINT('Ctrl Pts',(-1.93429347589134,-1.38006236221279,
0.945684068816811));
#41439=CARTESIAN_POINT('Ctrl Pts',(-2.02349685345405,-1.23742646019694,
0.933918328788326));
#41440=CARTESIAN_POINT('Ctrl Pts',(-2.03580479229626,-1.21707136719064,
0.932269296470122));
#41441=CARTESIAN_POINT('Ctrl Pts',(-2.05433054010817,-1.18536551513263,
0.929750542546412));
#41442=CARTESIAN_POINT('Ctrl Pts',(-2.06076480599553,-1.17414386091902,
0.928868543619198));
#41443=CARTESIAN_POINT('Ctrl Pts',(-2.07255539196082,-1.15318501920323,
0.927239516810714));
#41444=CARTESIAN_POINT('Ctrl Pts',(-2.07793533401818,-1.14346241518685,
0.92649114925813));
#41445=CARTESIAN_POINT('Ctrl Pts',(-2.09059823752764,-1.12019354729023,
0.924716966866783));
#41446=CARTESIAN_POINT('Ctrl Pts',(-2.09781808350303,-1.10661370564523,
0.923694962010024));
#41447=CARTESIAN_POINT('Ctrl Pts',(-2.12268368389257,-1.05872582188888,
0.920134403586227));
#41448=CARTESIAN_POINT('Ctrl Pts',(-2.13962496476518,-1.02405653596338,
0.917634149250662));
#41449=CARTESIAN_POINT('Ctrl Pts',(-2.18135678665411,-0.933092897859914,
0.911233316040393));
#41450=CARTESIAN_POINT('Ctrl Pts',(-2.20481773771799,-0.876218850789425,
0.907385114852131));
#41451=CARTESIAN_POINT('Ctrl Pts',(-2.28521664448587,-0.657559434172317,
0.892941572194925));
#41452=CARTESIAN_POINT('Ctrl Pts',(-2.32676218537592,-0.490689728306029,
0.882590252418731));
#41453=CARTESIAN_POINT('Ctrl Pts',(-2.35754816176512,-0.265172945859477,
0.868172710527603));
#41454=CARTESIAN_POINT('Ctrl Pts',(-2.3631638913273,-0.209298115508005,
0.864570841929052));
#41455=CARTESIAN_POINT('Ctrl Pts',(-2.36842780337635,-0.128018092227238,
0.859258561225237));
#41456=CARTESIAN_POINT('Ctrl Pts',(-2.36965921881742,-0.102732656837708,
0.857595897147773));
#41457=CARTESIAN_POINT('Ctrl Pts',(-2.37096058569031,-0.0628934828436836,
0.854958239102695));
#41458=CARTESIAN_POINT('Ctrl Pts',(-2.37130174057408,-0.0483500622696361,
0.853991585794441));
#41459=CARTESIAN_POINT('Ctrl Pts',(-2.37167126373329,-0.0224268086792617,
0.85226145946354));
#41460=CARTESIAN_POINT('Ctrl Pts',(-2.37175156271517,-0.0110481096338858,
0.85149960721778));
#41461=CARTESIAN_POINT('Ctrl Pts',(-2.37174997696831,0.000330531137167949,
0.850735237974249));
#41462=CARTESIAN_POINT('Ctrl Pts',(-2.36545134966535,0.172736721244678,
0.837052931219471));
#41463=CARTESIAN_POINT('Ctrl Pts',(-2.36964080846894,0.115366401199833,
0.840898584768258));
#41464=CARTESIAN_POINT('Ctrl Pts',(-2.37174546446208,0.057798410806183,
0.844744238317046));
#41465=CARTESIAN_POINT('Ctrl Pts',(-2.37174999267401,0.000186415808278105,
0.848589891865832));
#41466=CARTESIAN_POINT('',(-2.37174928376065,0.00184322565632311,0.651410108094984));
#41467=CARTESIAN_POINT('Ctrl Pts',(-2.36545134966535,0.172736721244682,
0.639882202840047));
#41468=CARTESIAN_POINT('Ctrl Pts',(-2.36960009283458,0.115923959844792,
0.643724837925026));
#41469=CARTESIAN_POINT('Ctrl Pts',(-2.37170492520006,0.0589210901913182,
0.647567473010006));
#41470=CARTESIAN_POINT('Ctrl Pts',(-2.37174928376066,0.00184322565632311,
0.651410108094985));
#41471=CARTESIAN_POINT('Ctrl Pts',(-2.37174922947978,0.00191179551492997,
0.652512471420324));
#41472=CARTESIAN_POINT('Ctrl Pts',(-2.37191126216802,-0.199103899144939,
0.665016268510595));
#41473=CARTESIAN_POINT('Ctrl Pts',(-2.34651945566196,-0.399324539138869,
0.677075520136256));
#41474=CARTESIAN_POINT('Ctrl Pts',(-2.28520666596991,-0.636354103094203,
0.692736184251922));
#41475=CARTESIAN_POINT('Ctrl Pts',(-2.27306750346192,-0.678439235429362,
0.695568368220726));
#41476=CARTESIAN_POINT('Ctrl Pts',(-2.25264373364539,-0.74252623970411,
0.699974677491279));
#41477=CARTESIAN_POINT('Ctrl Pts',(-2.24518521081825,-0.764782525883648,
0.701522499479531));
#41478=CARTESIAN_POINT('Ctrl Pts',(-2.23076691243074,-0.805776925393405,
0.704408099382541));
#41479=CARTESIAN_POINT('Ctrl Pts',(-2.22389816069032,-0.82454496585285,
0.705742810651493));
#41480=CARTESIAN_POINT('Ctrl Pts',(-2.2080731687877,-0.866148093963545,
0.708733065856802));
#41481=CARTESIAN_POINT('Ctrl Pts',(-2.19899832240328,-0.888935284605259,
0.710392393200129));
#41482=CARTESIAN_POINT('Ctrl Pts',(-2.17479194600454,-0.947078050459369,
0.714683448015121));
#41483=CARTESIAN_POINT('Ctrl Pts',(-2.15915144930666,-0.982212588466088,
0.717331639947056));
#41484=CARTESIAN_POINT('Ctrl Pts',(-2.05821227939559,-1.19488660051909,
0.733709689733471));
#41485=CARTESIAN_POINT('Ctrl Pts',(-1.95193344448354,-1.36158818032688,
0.748149173304034));
#41486=CARTESIAN_POINT('Ctrl Pts',(-1.78822553465202,-1.55916991681346,
0.766771877128838));
#41487=CARTESIAN_POINT('Ctrl Pts',(-1.748416248211,-1.6036841440578,0.771076524526458));
#41488=CARTESIAN_POINT('Ctrl Pts',(-1.68059420543115,-1.67399049534243,
0.77800378582117));
#41489=CARTESIAN_POINT('Ctrl Pts',(-1.65356602181679,-1.70069422726658,
0.780667661284586));
#41490=CARTESIAN_POINT('Ctrl Pts',(-1.61462030824582,-1.73736571491181,
0.784358915898909));
#41491=CARTESIAN_POINT('Ctrl Pts',(-1.6032300434013,-1.74788209763561,0.785421461407439));
#41492=CARTESIAN_POINT('Ctrl Pts',(-1.58329869885147,-1.76592549543948,
0.787250264384511));
#41493=CARTESIAN_POINT('Ctrl Pts',(-1.57480537351169,-1.77350378600904,
0.788020108656043));
#41494=CARTESIAN_POINT('Ctrl Pts',(-1.55608156126111,-1.78996979313978,
0.789696545966776));
#41495=CARTESIAN_POINT('Ctrl Pts',(-1.54582906513156,-1.7988313452953,0.790601330730788));
#41496=CARTESIAN_POINT('Ctrl Pts',(-1.51601355261087,-1.8241586434434,0.793196716777426));
#41497=CARTESIAN_POINT('Ctrl Pts',(-1.49625886437082,-1.84039707250557,
0.794872456336476));
#41498=CARTESIAN_POINT('Ctrl Pts',(-1.39186518699151,-1.92341676842146,
0.803525211988779));
#41499=CARTESIAN_POINT('Ctrl Pts',(-1.30299922090806,-1.9846961458972,0.810212632602846));
#41500=CARTESIAN_POINT('Ctrl Pts',(-1.12436746591585,-2.09068684003399,
0.823013037413721));
#41501=CARTESIAN_POINT('Ctrl Pts',(-1.03534010255263,-2.13617509073719,
0.829119809993047));
#41502=CARTESIAN_POINT('Ctrl Pts',(-0.861063347311503,-2.21176028439724,
0.840949468662011));
#41503=CARTESIAN_POINT('Ctrl Pts',(-0.776448029666017,-2.24286413884088,
0.846641027254705));
#41504=CARTESIAN_POINT('Ctrl Pts',(-0.661428498930152,-2.27785414852269,
0.854441562293542));
#41505=CARTESIAN_POINT('Ctrl Pts',(-0.632418529197615,-2.28607826940603,
0.856413863146435));
#41506=CARTESIAN_POINT('Ctrl Pts',(-0.583041475695171,-2.29906454762876,
0.859783238447097));
#41507=CARTESIAN_POINT('Ctrl Pts',(-0.562753399642459,-2.30411452005984,
0.861171133227325));
#41508=CARTESIAN_POINT('Ctrl Pts',(-0.521668025104564,-2.31376622521375,
0.863990061846888));
#41509=CARTESIAN_POINT('Ctrl Pts',(-0.500870237089178,-2.31835731263685,
0.865421285266575));
#41510=CARTESIAN_POINT('Ctrl Pts',(-0.448469685563391,-2.32918667050399,
0.869039248180442));
#41511=CARTESIAN_POINT('Ctrl Pts',(-0.416797228329559,-2.33506220536889,
0.871236951790047));
#41512=CARTESIAN_POINT('Ctrl Pts',(-0.278256467903017,-2.35785443334156,
0.880902088855557));
#41513=CARTESIAN_POINT('Ctrl Pts',(-0.170434327431137,-2.36809010273844,
0.888566613256902));
#41514=CARTESIAN_POINT('Ctrl Pts',(0.0576981276387517,-2.3740849016633,
0.905017240485764));
#41515=CARTESIAN_POINT('Ctrl Pts',(0.17776088966951,-2.3681233153469,0.913812339441916));
#41516=CARTESIAN_POINT('Ctrl Pts',(0.371124861478,-2.34372957930793,0.927891197594405));
#41517=CARTESIAN_POINT('Ctrl Pts',(0.44491778864012,-2.33084797457111,0.933240060042184));
#41518=CARTESIAN_POINT('Ctrl Pts',(0.536947687548176,-2.3102516917753,0.93979052373252));
#41519=CARTESIAN_POINT('Ctrl Pts',(0.555859317464115,-2.3057745287176,0.941130029945019));
#41520=CARTESIAN_POINT('Ctrl Pts',(0.58649552343711,-2.29812282387941,0.943286998527937));
#41521=CARTESIAN_POINT('Ctrl Pts',(0.598254092126595,-2.29508988280001,
0.944111740096526));
#41522=CARTESIAN_POINT('Ctrl Pts',(0.62033426106946,-2.28921341697813,0.94565387573166));
#41523=CARTESIAN_POINT('Ctrl Pts',(0.630660827984366,-2.28639007921324,
0.946372388625348));
#41524=CARTESIAN_POINT('Ctrl Pts',(0.65854503996355,-2.27856309581989,0.94830605285849));
#41525=CARTESIAN_POINT('Ctrl Pts',(0.676065026682413,-2.27342637455781,
0.949514005244516));
#41526=CARTESIAN_POINT('Ctrl Pts',(0.746357213305388,-2.2519327784342,0.954338708032254));
#41527=CARTESIAN_POINT('Ctrl Pts',(0.798613683144038,-2.2339354325253,0.957875997934973));
#41528=CARTESIAN_POINT('Ctrl Pts',(1.01206442875967,-2.15197297034043,0.97229938017342));
#41529=CARTESIAN_POINT('Ctrl Pts',(1.1666328977421,-2.07225392823316,0.982719219503754));
#41530=CARTESIAN_POINT('Ctrl Pts',(1.38109739063671,-1.92997847127507,0.998788098801221));
#41531=CARTESIAN_POINT('Ctrl Pts',(1.44853940187333,-1.87988785728605,1.00410655736001));
#41532=CARTESIAN_POINT('Ctrl Pts',(1.53588868338096,-1.80751589902515,1.01147241576628));
#41533=CARTESIAN_POINT('Ctrl Pts',(1.55824392718966,-1.78827948404009,1.01340273218654));
#41534=CARTESIAN_POINT('Ctrl Pts',(1.59570725418244,-1.75480682083839,1.01671968588537));
#41535=CARTESIAN_POINT('Ctrl Pts',(1.61099807016648,-1.74077965065701,1.01809775766645));
#41536=CARTESIAN_POINT('Ctrl Pts',(1.6416716930361,-1.71189063033207,1.02091327919703));
#41537=CARTESIAN_POINT('Ctrl Pts',(1.65704140523732,-1.69701773961953,1.0223511194052));
#41538=CARTESIAN_POINT('Ctrl Pts',(1.69549797911102,-1.6587836815328,1.02601956610504));
#41539=CARTESIAN_POINT('Ctrl Pts',(1.71830396213562,-1.63514770270913,1.02826187424703));
#41540=CARTESIAN_POINT('Ctrl Pts',(1.82774739959666,-1.51690257081733,1.03936266243522));
#41541=CARTESIAN_POINT('Ctrl Pts',(1.90708930317009,-1.41585851877461,1.04850864411624));
#41542=CARTESIAN_POINT('Ctrl Pts',(2.03072211240654,-1.22903990540586,1.06474758053518));
#41543=CARTESIAN_POINT('Ctrl Pts',(2.07869221514349,-1.14604097547829,1.07175479705561));
#41544=CARTESIAN_POINT('Ctrl Pts',(2.15681060526284,-0.989747209267179,
1.08439979836071));
#41545=CARTESIAN_POINT('Ctrl Pts',(2.1885640305246,-0.917399274419508,1.09005304862441));
#41546=CARTESIAN_POINT('Ctrl Pts',(2.22363848928257,-0.825236812181466,
1.0969066102231));
#41547=CARTESIAN_POINT('Ctrl Pts',(2.23039729851647,-0.806791100429943,
1.09826131052796));
#41548=CARTESIAN_POINT('Ctrl Pts',(2.24096444596045,-0.776803727452273,
1.10043394241082));
#41549=CARTESIAN_POINT('Ctrl Pts',(2.24491447757594,-0.765313454563482,
1.10125943754474));
#41550=CARTESIAN_POINT('Ctrl Pts',(2.25215366614211,-0.743716923281928,
1.1027972645983));
#41551=CARTESIAN_POINT('Ctrl Pts',(2.25546350178369,-0.733618020407526,
1.10351078088389));
#41552=CARTESIAN_POINT('Ctrl Pts',(2.2641731667591,-0.706427074629628,1.10541775036709));
#41553=CARTESIAN_POINT('Ctrl Pts',(2.26944743503956,-0.689295094743829,
1.10660431245804));
#41554=CARTESIAN_POINT('Ctrl Pts',(2.28935989085404,-0.62190760940321,1.11121919188182));
#41555=CARTESIAN_POINT('Ctrl Pts',(2.30252806493034,-0.571229522221275,
1.11457632443595));
#41556=CARTESIAN_POINT('Ctrl Pts',(2.34541138388366,-0.380454245494688,
1.12693425727061));
#41557=CARTESIAN_POINT('Ctrl Pts',(2.36410029454129,-0.238190831549242,
1.13560901022335));
#41558=CARTESIAN_POINT('Ctrl Pts',(2.373424692229,-0.00583977620744467,
1.1499829964217));
#41559=CARTESIAN_POINT('Ctrl Pts',(2.37196049852422,0.0835479996810568,
1.15555847964464));
#41560=CARTESIAN_POINT('Ctrl Pts',(2.36222366855902,0.216962633049453,1.16411334252959));
#41561=CARTESIAN_POINT('Ctrl Pts',(2.3577433969088,0.261187912047189,1.16698718051451));
#41562=CARTESIAN_POINT('Ctrl Pts',(2.3489751644962,0.328747199732648,1.1714499398246));
#41563=CARTESIAN_POINT('Ctrl Pts',(2.34557517404521,0.352187566022606,1.17301179425879));
#41564=CARTESIAN_POINT('Ctrl Pts',(2.33864087326628,0.395425346752585,1.1759196530551));
#41565=CARTESIAN_POINT('Ctrl Pts',(2.33520469769557,0.415236459204942,1.17726250468013));
#41566=CARTESIAN_POINT('Ctrl Pts',(2.32700354786808,0.459192960234471,1.18026652517117));
#41567=CARTESIAN_POINT('Ctrl Pts',(2.32211384883979,0.483312406198441,1.18193143678596));
#41568=CARTESIAN_POINT('Ctrl Pts',(2.30627951227469,0.555620938536484,1.18697472469319));
#41569=CARTESIAN_POINT('Ctrl Pts',(2.2942039232873,0.603545826024765,1.19038756115135));
#41570=CARTESIAN_POINT('Ctrl Pts',(2.2331810183158,0.817308387369813,1.20593640691556));
#41571=CARTESIAN_POINT('Ctrl Pts',(2.16768914440289,0.977853807280558,1.21856242851948));
#41572=CARTESIAN_POINT('Ctrl Pts',(2.05328810121645,1.18900628121615,1.23601762489984));
#41573=CARTESIAN_POINT('Ctrl Pts',(2.01871999839616,1.24679530499095,1.24088534818926));
#41574=CARTESIAN_POINT('Ctrl Pts',(1.95913936471236,1.33740909480629,1.24859136379094));
#41575=CARTESIAN_POINT('Ctrl Pts',(1.93564794366562,1.37118840546614,1.25148125758077));
#41576=CARTESIAN_POINT('Ctrl Pts',(1.90179867757114,1.41725675172584,1.25542925324394));
#41577=CARTESIAN_POINT('Ctrl Pts',(1.8921782219736,1.4300757048678,1.25652855837444));
#41578=CARTESIAN_POINT('Ctrl Pts',(1.87544434064011,1.45190853368045,1.25840077599928));
#41579=CARTESIAN_POINT('Ctrl Pts',(1.86839422807745,1.46096984749999,1.25917773579917));
#41580=CARTESIAN_POINT('Ctrl Pts',(1.85302702110034,1.48042769280371,1.26084567646308));
#41581=CARTESIAN_POINT('Ctrl Pts',(1.84468782628783,1.49080586893371,1.26173514709399));
#41582=CARTESIAN_POINT('Ctrl Pts',(1.8207812217944,1.52005000922234,1.26424288320383));
#41583=CARTESIAN_POINT('Ctrl Pts',(1.80500828083771,1.53874673205063,1.26584776889485));
#41584=CARTESIAN_POINT('Ctrl Pts',(1.69849461256428,1.66111239361092,1.27638791884378));
#41585=CARTESIAN_POINT('Ctrl Pts',(1.59914726608953,1.75696203934371,1.28483147287725));
#41586=CARTESIAN_POINT('Ctrl Pts',(1.41161768434159,1.90872578278869,1.29966783380997));
#41587=CARTESIAN_POINT('Ctrl Pts',(1.32703916719225,1.96846740887906,1.30602945227724));
#41588=CARTESIAN_POINT('Ctrl Pts',(1.20064955030336,2.0458846445821,1.31537187367624));
#41589=CARTESIAN_POINT('Ctrl Pts',(1.16181063614574,2.06818737521527,1.31822124648786));
#41590=CARTESIAN_POINT('Ctrl Pts',(1.09011313618483,2.10670163465591,1.3234638559335));
#41591=CARTESIAN_POINT('Ctrl Pts',(1.05746558234757,2.12327688757886,1.32584473413999));
#41592=CARTESIAN_POINT('Ctrl Pts',(1.00447214297391,2.1486564116057,1.32970704263957));
#41593=CARTESIAN_POINT('Ctrl Pts',(0.984363007648859,2.15794301960502,1.33117210058001));
#41594=CARTESIAN_POINT('Ctrl Pts',(0.945500914593175,2.17523371279521,1.33400393593717));
#41595=CARTESIAN_POINT('Ctrl Pts',(0.926768955101656,2.1832803175405,1.33536913987012));
#41596=CARTESIAN_POINT('Ctrl Pts',(0.883217490626617,2.2013270657985,1.33854489002083));
#41597=CARTESIAN_POINT('Ctrl Pts',(0.85832824731487,2.21115049390966,1.34036105690564));
#41598=CARTESIAN_POINT('Ctrl Pts',(0.788824073810611,2.23723248076674,1.34543836227829));
#41599=CARTESIAN_POINT('Ctrl Pts',(0.743881087860137,2.25257474556141,1.34872799989816));
#41600=CARTESIAN_POINT('Ctrl Pts',(0.53685201675325,2.31637723436353,1.36391618862283));
#41601=CARTESIAN_POINT('Ctrl Pts',(0.370344477178653,2.34875372249066,1.37627457767995));
#41602=CARTESIAN_POINT('Ctrl Pts',(0.135771072431408,2.36878896842941,1.39337989428021));
#41603=CARTESIAN_POINT('Ctrl Pts',(0.0694911106989449,2.3716591070089,1.39817299464699));
#41604=CARTESIAN_POINT('Ctrl Pts',(-0.0375725223054501,2.37180241770526,
1.40577785610045));
#41605=CARTESIAN_POINT('Ctrl Pts',(-0.0783172833811533,2.37080687981982,
1.40863961680838));
#41606=CARTESIAN_POINT('Ctrl Pts',(-0.134985165715778,2.3679595933879,1.41255750300973));
#41607=CARTESIAN_POINT('Ctrl Pts',(-0.150943559825744,2.36699592466261,
1.41365392878035));
#41608=CARTESIAN_POINT('Ctrl Pts',(-0.178348807825658,2.36506272386894,
1.41552359723415));
#41609=CARTESIAN_POINT('Ctrl Pts',(-0.189800316596872,2.36417128118926,
1.41630083785366));
#41610=CARTESIAN_POINT('Ctrl Pts',(-0.214550942478451,2.36206356212865,
1.41797170730982));
#41611=CARTESIAN_POINT('Ctrl Pts',(-0.22784686885415,2.36081812169737,1.41886379366944));
#41612=CARTESIAN_POINT('Ctrl Pts',(-0.265654009311369,2.35695431044917,
1.4213865987279));
#41613=CARTESIAN_POINT('Ctrl Pts',(-0.290136656495056,2.35406595240916,
1.42300368563891));
#41614=CARTESIAN_POINT('Ctrl Pts',(-0.483790682796548,2.32815220962286,
1.43569428799089));
#41615=CARTESIAN_POINT('Ctrl Pts',(-0.650092674923883,2.28729990221417,
1.44601133815751));
#41616=CARTESIAN_POINT('Ctrl Pts',(-0.88801217705426,2.2007773020901,1.46162602566395));
#41617=CARTESIAN_POINT('Ctrl Pts',(-0.963918203657382,2.16860478602989,
1.46674179712511));
#41618=CARTESIAN_POINT('Ctrl Pts',(-1.08883338780146,2.10780385165979,1.47554677031167));
#41619=CARTESIAN_POINT('Ctrl Pts',(-1.13876963467015,2.0812491872958,1.4791765932924));
#41620=CARTESIAN_POINT('Ctrl Pts',(-1.21007887980382,2.03999392478637,1.48455343370311));
#41621=CARTESIAN_POINT('Ctrl Pts',(-1.23223732888119,2.02668625820122,1.48625242413198));
#41622=CARTESIAN_POINT('Ctrl Pts',(-1.27132719058742,2.00233207000811,1.48930294541399));
#41623=CARTESIAN_POINT('Ctrl Pts',(-1.2883434173872,1.99142605707816,1.4906493466567));
#41624=CARTESIAN_POINT('Ctrl Pts',(-1.32428496462124,1.96773699653786,1.49353403372071));
#41625=CARTESIAN_POINT('Ctrl Pts',(-1.34316908379902,1.95489547176612,1.49507436708538));
#41626=CARTESIAN_POINT('Ctrl Pts',(-1.39378969747723,1.91939285218127,1.49927242251767));
#41627=CARTESIAN_POINT('Ctrl Pts',(-1.4251563456092,1.8962193248837,1.50194893353141));
#41628=CARTESIAN_POINT('Ctrl Pts',(-1.62892492623571,1.73776367777958,1.51985267697584));
#41629=CARTESIAN_POINT('Ctrl Pts',(-1.78241538033212,1.57993040584799,1.53598997546018));
#41630=CARTESIAN_POINT('Ctrl Pts',(-1.95464163831369,1.34527349619535,1.55700646335));
#41631=CARTESIAN_POINT('Ctrl Pts',(-1.99459158501783,1.28529804733741,1.56214776874525));
#41632=CARTESIAN_POINT('Ctrl Pts',(-2.04165535094396,1.20714949575484,1.56848337287424));
#41633=CARTESIAN_POINT('Ctrl Pts',(-2.05135808238401,1.19058664231235,1.56980626267898));
#41634=CARTESIAN_POINT('Ctrl Pts',(-2.06682629918302,1.1634313315272,1.57194084467282));
#41635=CARTESIAN_POINT('Ctrl Pts',(-2.07271377772006,1.1529098089861,1.57275964132894));
#41636=CARTESIAN_POINT('Ctrl Pts',(-2.08367601906124,1.13296375274879,1.57429568885592));
#41637=CARTESIAN_POINT('Ctrl Pts',(-2.08876766516299,1.1235489618026,1.57501400923182));
#41638=CARTESIAN_POINT('Ctrl Pts',(-2.1024018330279,1.09792544068666,1.5769517524714));
#41639=CARTESIAN_POINT('Ctrl Pts',(-2.11082075532756,1.08165129770391,1.57816388657386));
#41640=CARTESIAN_POINT('Ctrl Pts',(-2.14423006842767,1.01519366988212,1.58304547596345));
#41641=CARTESIAN_POINT('Ctrl Pts',(-2.16762798873382,0.964225451219779,
1.58663283713487));
#41642=CARTESIAN_POINT('Ctrl Pts',(-2.27429536440735,0.708309455603149,
1.60411171063068));
#41643=CARTESIAN_POINT('Ctrl Pts',(-2.3304158127949,0.493248120243888,1.61725279128887));
#41644=CARTESIAN_POINT('Ctrl Pts',(-2.35981811703602,0.239990689206501,
1.63350195156645));
#41645=CARTESIAN_POINT('Ctrl Pts',(-2.36299379611575,0.206390384608692,
1.63567032553817));
#41646=CARTESIAN_POINT('Ctrl Pts',(-2.3654513498954,0.172736718094382,1.63785909343774));
#41647=CARTESIAN_POINT('Origin',(0.,0.,-1.84858989190501));
#41648=CARTESIAN_POINT('',(-2.36545134753269,0.172736750449338,2.83572259012909));
#41649=CARTESIAN_POINT('',(-2.36545139057093,0.172736161084027,2.64008830168392));
#41650=CARTESIAN_POINT('',(-2.36545134966535,0.172736721244682,-1.84858989190501));
#41651=CARTESIAN_POINT('Ctrl Pts',(-2.36545134753269,0.172736750449338,
2.83572259012909));
#41652=CARTESIAN_POINT('Ctrl Pts',(-2.36334042788976,0.201643614222682,
2.83363353379938));
#41653=CARTESIAN_POINT('Ctrl Pts',(-2.36069940514974,0.230514817336211,
2.8315546832682));
#41654=CARTESIAN_POINT('Ctrl Pts',(-2.35369907162262,0.294152347824024,
2.826998243979));
#41655=CARTESIAN_POINT('Ctrl Pts',(-2.34909811675042,0.328881796846493,
2.82452864919489));
#41656=CARTESIAN_POINT('Ctrl Pts',(-2.34145312675036,0.378174407967134,
2.82105880332428));
#41657=CARTESIAN_POINT('Ctrl Pts',(-2.33903910560916,0.392829118240582,
2.82003169899207));
#41658=CARTESIAN_POINT('Ctrl Pts',(-2.33459966990723,0.418286023279023,
2.8182563934489));
#41659=CARTESIAN_POINT('Ctrl Pts',(-2.33263656645484,0.429098446100914,
2.81750516261938));
#41660=CARTESIAN_POINT('Ctrl Pts',(-2.3285451644487,0.450774912959025,2.81600526353117));
#41661=CARTESIAN_POINT('Ctrl Pts',(-2.32641584106716,0.461638340572145,
2.81525673515386));
#41662=CARTESIAN_POINT('Ctrl Pts',(-2.32157869365001,0.485432740955418,
2.81362434620353));
#41663=CARTESIAN_POINT('Ctrl Pts',(-2.31883880354422,0.498356499140129,
2.81274222866067));
#41664=CARTESIAN_POINT('Ctrl Pts',(-2.31058207310167,0.535759431525327,
2.8102005708944));
#41665=CARTESIAN_POINT('Ctrl Pts',(-2.30478439591019,0.560175591159726,
2.80855548904454));
#41666=CARTESIAN_POINT('Ctrl Pts',(-2.27402972870867,0.681121920390583,
2.80045594428058));
#41667=CARTESIAN_POINT('Ctrl Pts',(-2.24338838325232,0.776112753777745,
2.79424969793554));
#41668=CARTESIAN_POINT('Ctrl Pts',(-2.15926203390543,0.989778768504046,
2.78008121501327));
#41669=CARTESIAN_POINT('Ctrl Pts',(-2.10182014360091,1.10653762206543,2.77217228203211));
#41670=CARTESIAN_POINT('Ctrl Pts',(-1.99817070695529,1.27972073209173,2.75951087324629));
#41671=CARTESIAN_POINT('Ctrl Pts',(-1.95844837833089,1.33972005915607,2.75493492323077));
#41672=CARTESIAN_POINT('Ctrl Pts',(-1.89923602888978,1.42088558859733,2.74840672041238));
#41673=CARTESIAN_POINT('Ctrl Pts',(-1.88199328350514,1.44364625774669,2.74653689660864));
#41674=CARTESIAN_POINT('Ctrl Pts',(-1.85191329759649,1.48189730595256,2.74332334559211));
#41675=CARTESIAN_POINT('Ctrl Pts',(-1.83928195160299,1.49754610891323,2.74198765767879));
#41676=CARTESIAN_POINT('Ctrl Pts',(-1.8132380342129,1.52898496990926,2.73926001118541));
#41677=CARTESIAN_POINT('Ctrl Pts',(-1.79981454262205,1.54476366247098,2.73786769031826));
#41678=CARTESIAN_POINT('Ctrl Pts',(-1.76531542316314,1.58425563754174,2.73432191565675));
#41679=CARTESIAN_POINT('Ctrl Pts',(-1.7439680673205,1.60772500217544,2.73215754368813));
#41680=CARTESIAN_POINT('Ctrl Pts',(-1.64678726836699,1.71035249010092,2.72242913161553));
#41681=CARTESIAN_POINT('Ctrl Pts',(-1.56600038750526,1.78461504463547,2.71465986523717));
#41682=CARTESIAN_POINT('Ctrl Pts',(-1.3913907473097,1.92411094899125,2.69853542409325));
#41683=CARTESIAN_POINT('Ctrl Pts',(-1.29739773871484,1.98870034069226,2.69018951502757));
#41684=CARTESIAN_POINT('Ctrl Pts',(-1.15142809630391,2.07423929167262,2.6779356901154));
#41685=CARTESIAN_POINT('Ctrl Pts',(-1.10275750478588,2.10051943275307,2.67395909258983));
#41686=CARTESIAN_POINT('Ctrl Pts',(-1.02102520403788,2.14102683591385,2.66750313941681));
#41687=CARTESIAN_POINT('Ctrl Pts',(-0.988479873407547,2.15624586852976,
2.66498829682542));
#41688=CARTESIAN_POINT('Ctrl Pts',(-0.941886196949669,2.17675743939155,
2.66147834913373));
#41689=CARTESIAN_POINT('Ctrl Pts',(-0.928115652818932,2.18266440891562,
2.66045199643191));
#41690=CARTESIAN_POINT('Ctrl Pts',(-0.904072297315916,2.19270927355332,
2.65868016148559));
#41691=CARTESIAN_POINT('Ctrl Pts',(-0.893825096838485,2.19690632288673,
2.65793137308261));
#41692=CARTESIAN_POINT('Ctrl Pts',(-0.871309683423988,2.20594456327904,
2.65630020261092));
#41693=CARTESIAN_POINT('Ctrl Pts',(-0.859030017648339,2.21075539796449,
2.6554195407495));
#41694=CARTESIAN_POINT('Ctrl Pts',(-0.822652904847154,2.22465807837024,
2.65283525139086));
#41695=CARTESIAN_POINT('Ctrl Pts',(-0.798445958004287,2.23346044260092,
2.65114717788715));
#41696=CARTESIAN_POINT('Ctrl Pts',(-0.673520313924219,2.27659629465779,
2.64257353688474));
#41697=CARTESIAN_POINT('Ctrl Pts',(-0.5707068745239,2.3045213888288,2.63597077709296));
#41698=CARTESIAN_POINT('Ctrl Pts',(-0.346511365080279,2.34948254797305,
2.6218811497574));
#41699=CARTESIAN_POINT('Ctrl Pts',(-0.22499302241912,2.36421556408556,2.61442480574035));
#41700=CARTESIAN_POINT('Ctrl Pts',(-0.0526794870834247,2.3716972935954,
2.60360652990194));
#41701=CARTESIAN_POINT('Ctrl Pts',(-0.0024222066320971,2.37228093742978,
2.60042362342617));
#41702=CARTESIAN_POINT('Ctrl Pts',(0.0874870177756139,2.37046803678667,
2.59464938941809));
#41703=CARTESIAN_POINT('Ctrl Pts',(0.127132278463775,2.3686725794343,2.59207542061028));
#41704=CARTESIAN_POINT('Ctrl Pts',(0.188987207371859,2.36431396840485,2.58800604883393));
#41705=CARTESIAN_POINT('Ctrl Pts',(0.211238368949565,2.3624298934581,2.58653135328852));
#41706=CARTESIAN_POINT('Ctrl Pts',(0.252927148626647,2.35830630682148,2.58374649913439));
#41707=CARTESIAN_POINT('Ctrl Pts',(0.272370212695668,2.3561398956583,2.58243869983621));
#41708=CARTESIAN_POINT('Ctrl Pts',(0.316306578329727,2.35069326383021,2.5794620185146));
#41709=CARTESIAN_POINT('Ctrl Pts',(0.340779551043279,2.34727030633404,2.57778886685938));
#41710=CARTESIAN_POINT('Ctrl Pts',(0.404921617976307,2.33727473200564,2.573362141352));
#41711=CARTESIAN_POINT('Ctrl Pts',(0.444483395951404,2.33007486339111,2.57058976938614));
#41712=CARTESIAN_POINT('Ctrl Pts',(0.658658014303677,2.28544431167203,2.55534515743));
#41713=CARTESIAN_POINT('Ctrl Pts',(0.828779053912086,2.22939283654233,2.54231476710808));
#41714=CARTESIAN_POINT('Ctrl Pts',(1.05384041460813,2.12588976412907,2.52429933854261));
#41715=CARTESIAN_POINT('Ctrl Pts',(1.11542002318246,2.0942364099189,2.51929022682933));
#41716=CARTESIAN_POINT('Ctrl Pts',(1.20046390046497,2.04570492371843,2.51232930970138));
#41717=CARTESIAN_POINT('Ctrl Pts',(1.22513839085955,2.03102394978628,2.51030446664061));
#41718=CARTESIAN_POINT('Ctrl Pts',(1.26852998466481,2.00412795069126,2.50674183794915));
#41719=CARTESIAN_POINT('Ctrl Pts',(1.28735225424754,1.99208971350519,2.50519583318597));
#41720=CARTESIAN_POINT('Ctrl Pts',(1.31643067667237,1.97290760243381,2.50280973965758));
#41721=CARTESIAN_POINT('Ctrl Pts',(1.32680471069011,1.96594593298879,2.50195894692974));
#41722=CARTESIAN_POINT('Ctrl Pts',(1.34641537558599,1.95255992594008,2.50035226455621));
#41723=CARTESIAN_POINT('Ctrl Pts',(1.35566195670665,1.94615140520819,2.49959548313258));
#41724=CARTESIAN_POINT('Ctrl Pts',(1.37818477762112,1.93030311879665,2.49775328466571));
#41725=CARTESIAN_POINT('Ctrl Pts',(1.391410305204,1.92079171448511,2.49667249579058));
#41726=CARTESIAN_POINT('Ctrl Pts',(1.43829320496628,1.8863365600018,2.49284057348281));
#41727=CARTESIAN_POINT('Ctrl Pts',(1.47138835234922,1.86063692353074,2.49013431894508));
#41728=CARTESIAN_POINT('Ctrl Pts',(1.62302667067938,1.73630605430581,2.47763797038065));
#41729=CARTESIAN_POINT('Ctrl Pts',(1.73245697380583,1.6271370904306,2.46831424669657));
#41730=CARTESIAN_POINT('Ctrl Pts',(1.87984941930382,1.44823427371662,2.45399900593351));
#41731=CARTESIAN_POINT('Ctrl Pts',(1.92620814829436,1.38597882338579,2.44917031781089));
#41732=CARTESIAN_POINT('Ctrl Pts',(1.99955555997284,1.27667476233576,2.44081425599431));
#41733=CARTESIAN_POINT('Ctrl Pts',(2.02813449121015,1.23076833470534,2.43733900084326));
#41734=CARTESIAN_POINT('Ctrl Pts',(2.06758748648854,1.162283955079,2.43217718438621));
#41735=CARTESIAN_POINT('Ctrl Pts',(2.07971330954708,1.14044486048034,2.43053445725686));
#41736=CARTESIAN_POINT('Ctrl Pts',(2.10072825431499,1.10114601009879,2.4275819916053));
#41737=CARTESIAN_POINT('Ctrl Pts',(2.10975035138646,1.08375972906174,2.42627701377475));
#41738=CARTESIAN_POINT('Ctrl Pts',(2.12851804620491,1.04647027257227,2.42347969146593));
#41739=CARTESIAN_POINT('Ctrl Pts',(2.13820205243666,1.02653837271674,2.4219853904321));
#41740=CARTESIAN_POINT('Ctrl Pts',(2.16365155921366,0.972234460786808,2.41791522740838));
#41741=CARTESIAN_POINT('Ctrl Pts',(2.17887606577426,0.937617580699433,2.41532163738879));
#41742=CARTESIAN_POINT('Ctrl Pts',(2.24598467258466,0.774557150989222,2.40310293836556));
#41743=CARTESIAN_POINT('Ctrl Pts',(2.28737253639754,0.642107684911512,2.39315065803889));
#41744=CARTESIAN_POINT('Ctrl Pts',(2.33942868543062,0.404131130618277,2.37543102833928));
#41745=CARTESIAN_POINT('Ctrl Pts',(2.35504065377719,0.300055587120037,2.36774052726046));
#41746=CARTESIAN_POINT('Ctrl Pts',(2.36808922825888,0.142117955501362,2.35639138080684));
#41747=CARTESIAN_POINT('Ctrl Pts',(2.37068708483292,0.0888131858678933,
2.35261686586998));
#41748=CARTESIAN_POINT('Ctrl Pts',(2.37174265137471,0.0182234767299164,
2.34772798243264));
#41749=CARTESIAN_POINT('Ctrl Pts',(2.37181246691622,0.000981914649346083,
2.34654253800131));
#41750=CARTESIAN_POINT('Ctrl Pts',(2.37161597671251,-0.0276791809721018,
2.34458798610151));
#41751=CARTESIAN_POINT('Ctrl Pts',(2.37145520730219,-0.0390985767487486,
2.3438134797004));
#41752=CARTESIAN_POINT('Ctrl Pts',(2.37095334572605,-0.0626554661950777,
2.3422250672482));
#41753=CARTESIAN_POINT('Ctrl Pts',(2.37060152970334,-0.0747922357072169,
2.3414117267864));
#41754=CARTESIAN_POINT('Ctrl Pts',(2.36939857456663,-0.10759241905691,2.33922594058344));
#41755=CARTESIAN_POINT('Ctrl Pts',(2.36837033650107,-0.12824879409271,2.33786261733806));
#41756=CARTESIAN_POINT('Ctrl Pts',(2.35971143109423,-0.265909244036946,
2.32884946034921));
#41757=CARTESIAN_POINT('Ctrl Pts',(2.34368246171409,-0.382237021521754,
2.32157786325115));
#41758=CARTESIAN_POINT('Ctrl Pts',(2.29381421198584,-0.614973497550293,
2.30691633521917));
#41759=CARTESIAN_POINT('Ctrl Pts',(2.25954070074646,-0.7309244331178,2.2995471268618));
#41760=CARTESIAN_POINT('Ctrl Pts',(2.19043844425199,-0.912458706760118,
2.28736064012625));
#41761=CARTESIAN_POINT('Ctrl Pts',(2.16111028196973,-0.979899115424568,
2.28268198580112));
#41762=CARTESIAN_POINT('Ctrl Pts',(2.11644772781317,-1.07080302756555,2.27609421212494));
#41763=CARTESIAN_POINT('Ctrl Pts',(2.10375827394799,-1.09552322156963,2.274273136907));
#41764=CARTESIAN_POINT('Ctrl Pts',(2.08120412750174,-1.13762318995999,2.27111715546875));
#41765=CARTESIAN_POINT('Ctrl Pts',(2.07154851745287,-1.15511204732381,2.26978956171781));
#41766=CARTESIAN_POINT('Ctrl Pts',(2.05132523403797,-1.19067251115208,2.26705486739343));
#41767=CARTESIAN_POINT('Ctrl Pts',(2.04073693973913,-1.20873030064777,2.26564712666204));
#41768=CARTESIAN_POINT('Ctrl Pts',(2.01294570671396,-1.25472056961508,2.26201132249815));
#41769=CARTESIAN_POINT('Ctrl Pts',(1.99540024645773,-1.28243978385698,2.25977119321619));
#41770=CARTESIAN_POINT('Ctrl Pts',(1.90351103905125,-1.42115816879178,2.24830453649796));
#41771=CARTESIAN_POINT('Ctrl Pts',(1.82046949371683,-1.52608176236397,2.23876270080917));
#41772=CARTESIAN_POINT('Ctrl Pts',(1.65154206630797,-1.70599817253438,2.22085092420353));
#41773=CARTESIAN_POINT('Ctrl Pts',(1.56821830625224,-1.78289454833961,2.21255115864241));
#41774=CARTESIAN_POINT('Ctrl Pts',(1.4333989783112,-1.89052331311069,2.20015928783483));
#41775=CARTESIAN_POINT('Ctrl Pts',(1.38570464114618,-1.92575566781719,2.19595305570193));
#41776=CARTESIAN_POINT('Ctrl Pts',(1.32201074710681,-1.96921391409807,2.19060796559253));
#41777=CARTESIAN_POINT('Ctrl Pts',(1.30717174272897,-1.97909523193783,2.18938116819368));
#41778=CARTESIAN_POINT('Ctrl Pts',(1.28254933383123,-1.99509356500489,2.1873775190909));
#41779=CARTESIAN_POINT('Ctrl Pts',(1.27283041275375,-2.00130804386985,2.18659471417639));
#41780=CARTESIAN_POINT('Ctrl Pts',(1.25418813482182,-2.01303755740389,2.18510908094778));
#41781=CARTESIAN_POINT('Ctrl Pts',(1.245272926418,-2.01856469657572,2.1844054312002));
#41782=CARTESIAN_POINT('Ctrl Pts',(1.22067686485566,-2.03358848130557,2.18248195195641));
#41783=CARTESIAN_POINT('Ctrl Pts',(1.20492174909996,-2.04296298264404,2.18126957625663));
#41784=CARTESIAN_POINT('Ctrl Pts',(1.13736696082669,-2.08210556972155,2.17614756533318));
#41785=CARTESIAN_POINT('Ctrl Pts',(1.08455713275543,-2.11009579781193,2.17233256785448));
#41786=CARTESIAN_POINT('Ctrl Pts',(0.833311477659495,-2.23133257502607,
2.15478757739932));
#41787=CARTESIAN_POINT('Ctrl Pts',(0.623629037850769,-2.29877101113557,
2.14175345959954));
#41788=CARTESIAN_POINT('Ctrl Pts',(0.360532544108672,-2.34467541369039,
2.12472189895163));
#41789=CARTESIAN_POINT('Ctrl Pts',(0.313171501010043,-2.3514696761712,2.12163557715339));
#41790=CARTESIAN_POINT('Ctrl Pts',(0.241897493407644,-2.35950302456354,
2.11694266858223));
#41791=CARTESIAN_POINT('Ctrl Pts',(0.218116849781469,-2.36182003811804,
2.11536893238843));
#41792=CARTESIAN_POINT('Ctrl Pts',(0.176745371104177,-2.3652208340448,2.11261538452592));
#41793=CARTESIAN_POINT('Ctrl Pts',(0.15916966564872,-2.36646857352011,2.1114407009258));
#41794=CARTESIAN_POINT('Ctrl Pts',(0.119403087795279,-2.36884668815227,
2.10877099791222));
#41795=CARTESIAN_POINT('Ctrl Pts',(0.0972072219740444,-2.36986126770937,
2.1072725383911));
#41796=CARTESIAN_POINT('Ctrl Pts',(0.0369280851861319,-2.37176840716111,
2.10317892860491));
#41797=CARTESIAN_POINT('Ctrl Pts',(-0.00116633259554981,-2.37205552537581,
2.10056570214269));
#41798=CARTESIAN_POINT('Ctrl Pts',(-0.167155880341428,-2.36930824017253,
2.08905891438497));
#41799=CARTESIAN_POINT('Ctrl Pts',(-0.294663533878714,-2.356846954488,2.07989277137061));
#41800=CARTESIAN_POINT('Ctrl Pts',(-0.531500669652834,-2.31417797928882,
2.0624116941614));
#41801=CARTESIAN_POINT('Ctrl Pts',(-0.640907713365617,-2.28629635454371,
2.05415008350441));
#41802=CARTESIAN_POINT('Ctrl Pts',(-0.800443066188376,-2.23328289640376,
2.04209786324687));
#41803=CARTESIAN_POINT('Ctrl Pts',(-0.85234569383876,-2.21399400131151,
2.0381776781263));
#41804=CARTESIAN_POINT('Ctrl Pts',(-0.919661519618189,-2.18625825645097,
2.03313404613041));
#41805=CARTESIAN_POINT('Ctrl Pts',(-0.935720043385641,-2.17943353175747,
2.0319340116131));
#41806=CARTESIAN_POINT('Ctrl Pts',(-0.962199258403491,-2.16783347620682,
2.02996218076256));
#41807=CARTESIAN_POINT('Ctrl Pts',(-0.972663065306776,-2.16315879565978,
2.02918479080003));
#41808=CARTESIAN_POINT('Ctrl Pts',(-0.994083743563671,-2.15340229153987,
2.02759769567279));
#41809=CARTESIAN_POINT('Ctrl Pts',(-1.00503638094071,-2.14831231604814,
2.02678847534491));
#41810=CARTESIAN_POINT('Ctrl Pts',(-1.03436461743194,-2.13440933359863,
2.02462648597835));
#41811=CARTESIAN_POINT('Ctrl Pts',(-1.05266675366861,-2.12544257468181,
2.02328250217499));
#41812=CARTESIAN_POINT('Ctrl Pts',(-1.15920044921697,-2.07153481334418,
2.01547683169071));
#41813=CARTESIAN_POINT('Ctrl Pts',(-1.24467354114231,-2.02133482243089,
2.00928286398295));
#41814=CARTESIAN_POINT('Ctrl Pts',(-1.44016653204764,-1.88940074161149,
1.99469894881576));
#41815=CARTESIAN_POINT('Ctrl Pts',(-1.54672960284108,-1.80320319075302,
1.98638927235827));
#41816=CARTESIAN_POINT('Ctrl Pts',(-1.69973664815756,-1.65584185129473,
1.97307606276733));
#41817=CARTESIAN_POINT('Ctrl Pts',(-1.75166096847359,-1.60081201310641,
1.96826751018936));
#41818=CARTESIAN_POINT('Ctrl Pts',(-1.81911346214293,-1.52210730741402,
1.96152778895392));
#41819=CARTESIAN_POINT('Ctrl Pts',(-1.83698219572638,-1.50049350182988,
1.95969040205577));
#41820=CARTESIAN_POINT('Ctrl Pts',(-1.86694413498688,-1.46291438462146,
1.95651520823513));
#41821=CARTESIAN_POINT('Ctrl Pts',(-1.87922629867624,-1.44710309839294,
1.95518495500906));
#41822=CARTESIAN_POINT('Ctrl Pts',(-1.90389153966823,-1.41450700277021,
1.95245292311002));
#41823=CARTESIAN_POINT('Ctrl Pts',(-1.9162562811197,-1.3977105829214,1.95105059983466));
#41824=CARTESIAN_POINT('Ctrl Pts',(-1.94727411379477,-1.3543902483671,1.9474463936452));
#41825=CARTESIAN_POINT('Ctrl Pts',(-1.9656071975433,-1.32764362202015,1.94523285225192));
#41826=CARTESIAN_POINT('Ctrl Pts',(-2.05459898517378,-1.1919259309087,1.93405339279219));
#41827=CARTESIAN_POINT('Ctrl Pts',(-2.11676108894222,-1.0776722766733,1.92479034279789));
#41828=CARTESIAN_POINT('Ctrl Pts',(-2.2178710010374,-0.84894362716249,1.90665506299714));
#41829=CARTESIAN_POINT('Ctrl Pts',(-2.25805354808094,-0.735426308349322,
1.89783375800942));
#41830=CARTESIAN_POINT('Ctrl Pts',(-2.30438429372222,-0.564162802279199,
1.88510243910304));
#41831=CARTESIAN_POINT('Ctrl Pts',(-2.31731482045602,-0.508448398162815,
1.88104941324044));
#41832=CARTESIAN_POINT('Ctrl Pts',(-2.33158167486305,-0.435012298465262,
1.87586539028095));
#41833=CARTESIAN_POINT('Ctrl Pts',(-2.33475059823288,-0.417670319863833,
1.87465262086695));
#41834=CARTESIAN_POINT('Ctrl Pts',(-2.33966615602071,-0.388963351298039,
1.87266566716924));
#41835=CARTESIAN_POINT('Ctrl Pts',(-2.34152399418825,-0.377618345455078,
1.87188571857914));
#41836=CARTESIAN_POINT('Ctrl Pts',(-2.34515606463268,-0.354380666805676,
1.87029957447984));
#41837=CARTESIAN_POINT('Ctrl Pts',(-2.34692248183306,-0.34248723251976,
1.86949379534961));
#41838=CARTESIAN_POINT('Ctrl Pts',(-2.35140408449674,-0.31064783758922,
1.86735156450242));
#41839=CARTESIAN_POINT('Ctrl Pts',(-2.35395598882936,-0.290679403076856,
1.86602362271669));
#41840=CARTESIAN_POINT('Ctrl Pts',(-2.36650432268375,-0.181446938995612,
1.85883256437167));
#41841=CARTESIAN_POINT('Ctrl Pts',(-2.37167906593707,-0.0916932481035841,
1.85318862828644));
#41842=CARTESIAN_POINT('Ctrl Pts',(-2.37179484178429,0.0564523055511605,
1.84400223820082));
#41843=CARTESIAN_POINT('Ctrl Pts',(-2.36969033606028,0.114688263886919,
1.8404242658626));
#41844=CARTESIAN_POINT('Ctrl Pts',(-2.36545132977956,0.172736993559942,
1.83684621836632));
#41845=CARTESIAN_POINT('Ctrl Pts',(-2.3654513498954,0.172736718094382,1.63785909343774));
#41846=CARTESIAN_POINT('Ctrl Pts',(-2.36654719596649,0.157730235415224,
1.63883508538677));
#41847=CARTESIAN_POINT('Ctrl Pts',(-2.36750025325823,0.142713141653489,
1.63981511942869));
#41848=CARTESIAN_POINT('Ctrl Pts',(-2.36962990794866,0.103212916705495,
1.64240262684809));
#41849=CARTESIAN_POINT('Ctrl Pts',(-2.3705699460905,0.0787201675594078,
1.64401682505237));
#41850=CARTESIAN_POINT('Ctrl Pts',(-2.37154534091713,0.036062942540206,
1.64684724059731));
#41851=CARTESIAN_POINT('Ctrl Pts',(-2.3717519367411,0.0179041825275535,
1.64805813099086));
#41852=CARTESIAN_POINT('Ctrl Pts',(-2.37174751163658,-0.0232946734318096,
1.65081992710143));
#41853=CARTESIAN_POINT('Ctrl Pts',(-2.37140931205067,-0.0463326228033727,
1.65237459638538));
#41854=CARTESIAN_POINT('Ctrl Pts',(-2.3695342497042,-0.110421327414875,
1.65672980933126));
#41855=CARTESIAN_POINT('Ctrl Pts',(-2.36726651100573,-0.15144088271088,
1.65955211068397));
#41856=CARTESIAN_POINT('Ctrl Pts',(-2.35969524824681,-0.244475938589024,
1.6660359407548));
#41857=CARTESIAN_POINT('Ctrl Pts',(-2.35373478989167,-0.296415304166481,
1.669714930991));
#41858=CARTESIAN_POINT('Ctrl Pts',(-2.3253747220977,-0.487544759041735,
1.68346486913336));
#41859=CARTESIAN_POINT('Ctrl Pts',(-2.29229751164423,-0.624846928967425,
1.69378209767941));
#41860=CARTESIAN_POINT('Ctrl Pts',(-2.21779108325948,-0.845622755576177,
1.7106983813133));
#41861=CARTESIAN_POINT('Ctrl Pts',(-2.18329272077936,-0.931080769404213,
1.71732614367497));
#41862=CARTESIAN_POINT('Ctrl Pts',(-2.1351133200973,-1.03291439904969,1.72516634258405));
#41863=CARTESIAN_POINT('Ctrl Pts',(-2.1260758353813,-1.05139082065905,1.72658629267499));
#41864=CARTESIAN_POINT('Ctrl Pts',(-2.1112288379414,-1.08076979912125,1.72883736596415));
#41865=CARTESIAN_POINT('Ctrl Pts',(-2.10557273999476,-1.09174814792008,
1.72967701414564));
#41866=CARTESIAN_POINT('Ctrl Pts',(-2.09428981179005,-1.11323416090081,
1.73131656358107));
#41867=CARTESIAN_POINT('Ctrl Pts',(-2.08866907864324,-1.12374445614983,
1.7321167523793));
#41868=CARTESIAN_POINT('Ctrl Pts',(-2.07411171327606,-1.15047891219663,
1.73414858721058));
#41869=CARTESIAN_POINT('Ctrl Pts',(-2.06506359447816,-1.16664198834318,
1.73537361767912));
#41870=CARTESIAN_POINT('Ctrl Pts',(-2.02421612041418,-1.23764517585572,
1.74074754181101));
#41871=CARTESIAN_POINT('Ctrl Pts',(-1.99041237346468,-1.29130806603578,
1.74478920201906));
#41872=CARTESIAN_POINT('Ctrl Pts',(-1.86979535448828,-1.46677184212455,
1.75815821860776));
#41873=CARTESIAN_POINT('Ctrl Pts',(-1.77363062110573,-1.58170559429831,
1.76719613909452));
#41874=CARTESIAN_POINT('Ctrl Pts',(-1.59987921910734,-1.75344397644576,
1.78237190486569));
#41875=CARTESIAN_POINT('Ctrl Pts',(-1.52855209563023,-1.81595840926948,
1.7883407466005));
#41876=CARTESIAN_POINT('Ctrl Pts',(-1.42878216562506,-1.89334958496809,
1.79651915603755));
#41877=CARTESIAN_POINT('Ctrl Pts',(-1.40350078251773,-1.91216540397392,
1.79857757024046));
#41878=CARTESIAN_POINT('Ctrl Pts',(-1.36237723014878,-1.94151689379679,
1.80190843934111));
#41879=CARTESIAN_POINT('Ctrl Pts',(-1.34676963614764,-1.95237575240946,
1.80316868883825));
#41880=CARTESIAN_POINT('Ctrl Pts',(-1.31397202734376,-1.97461401260761,
1.80580991903696));
#41881=CARTESIAN_POINT('Ctrl Pts',(-1.29676089158136,-1.98595924737829,
1.80719201414072));
#41882=CARTESIAN_POINT('Ctrl Pts',(-1.25521473956508,-2.01257529514511,
1.81052012431879));
#41883=CARTESIAN_POINT('Ctrl Pts',(-1.23074635485711,-2.02763079675443,
1.81247366545656));
#41884=CARTESIAN_POINT('Ctrl Pts',(-1.139576297964,-2.08146984577536,1.81973211141));
#41885=CARTESIAN_POINT('Ctrl Pts',(-1.07127323573097,-2.11743295375691,
1.82513233190086));
#41886=CARTESIAN_POINT('Ctrl Pts',(-0.872973816873279,-2.209789276814,1.84070018983906));
#41887=CARTESIAN_POINT('Ctrl Pts',(-0.739512781128365,-2.25795633813337,
1.85106693815446));
#41888=CARTESIAN_POINT('Ctrl Pts',(-0.514336564277445,-2.31710549841442,
1.86796609553948));
#41889=CARTESIAN_POINT('Ctrl Pts',(-0.424832284520196,-2.33517468839432,
1.87453078407858));
#41890=CARTESIAN_POINT('Ctrl Pts',(-0.314168352659941,-2.35093984180814,
1.88230973266009));
#41891=CARTESIAN_POINT('Ctrl Pts',(-0.293797495290138,-2.35357239005546,
1.88372769062193));
#41892=CARTESIAN_POINT('Ctrl Pts',(-0.261131577271575,-2.35736309430761,
1.88597649192701));
#41893=CARTESIAN_POINT('Ctrl Pts',(-0.248857699329382,-2.3586903827263,
1.88681582713224));
#41894=CARTESIAN_POINT('Ctrl Pts',(-0.224709241457831,-2.36111117882403,
1.88845541479804));
#41895=CARTESIAN_POINT('Ctrl Pts',(-0.212835808804666,-2.3622110766265,
1.88925594681536));
#41896=CARTESIAN_POINT('Ctrl Pts',(-0.182472497352711,-2.36479299293019,
1.89128986106421));
#41897=CARTESIAN_POINT('Ctrl Pts',(-0.163972134449447,-2.3661477770163,
1.89251660057047));
#41898=CARTESIAN_POINT('Ctrl Pts',(-0.0818734459237205,-2.37119230452873,
1.89791251117477));
#41899=CARTESIAN_POINT('Ctrl Pts',(-0.01815225922352,-2.37253623255923,
1.90197335576717));
#41900=CARTESIAN_POINT('Ctrl Pts',(0.196845610564631,-2.36840628692787,
1.91547268789195));
#41901=CARTESIAN_POINT('Ctrl Pts',(0.347519075781397,-2.35102762939105,
1.92461558103027));
#41902=CARTESIAN_POINT('Ctrl Pts',(0.586445551710573,-2.29998380133406,
1.93980225343132));
#41903=CARTESIAN_POINT('Ctrl Pts',(0.676146672386169,-2.27522896257397,
1.94566306210147));
#41904=CARTESIAN_POINT('Ctrl Pts',(0.793817755561029,-2.23518077025074,
1.95371571285254));
#41905=CARTESIAN_POINT('Ctrl Pts',(0.823274064726649,-2.22449980276319,
1.95576260561974));
#41906=CARTESIAN_POINT('Ctrl Pts',(0.870221161956724,-2.20641642823471,
1.9590797366206));
#41907=CARTESIAN_POINT('Ctrl Pts',(0.887850252337718,-2.19938178141263,
1.96033796217619));
#41908=CARTESIAN_POINT('Ctrl Pts',(0.924466365445204,-2.18425865459622,
1.96297881103345));
#41909=CARTESIAN_POINT('Ctrl Pts',(0.943435973877932,-2.17613245203599,
1.96436259105091));
#41910=CARTESIAN_POINT('Ctrl Pts',(0.988684108260003,-2.15604622099577,
1.96770224662581));
#41911=CARTESIAN_POINT('Ctrl Pts',(1.01485446048899,-2.14385211058749,1.96966578677096));
#41912=CARTESIAN_POINT('Ctrl Pts',(1.1112273581862,-2.09678699705268,1.9770196338284));
#41913=CARTESIAN_POINT('Ctrl Pts',(1.17990417459937,-2.05892345458027,1.98250864731601));
#41914=CARTESIAN_POINT('Ctrl Pts',(1.37123128507644,-1.9407197557494,1.998523852608));
#41915=CARTESIAN_POINT('Ctrl Pts',(1.488475949544,-1.85232328560055,2.00926540172555));
#41916=CARTESIAN_POINT('Ctrl Pts',(1.6598440323203,-1.69628558433629,2.02606679136148));
#41917=CARTESIAN_POINT('Ctrl Pts',(1.7197498710968,-1.63552139311466,2.03218829732791));
#41918=CARTESIAN_POINT('Ctrl Pts',(1.7897013536335,-1.55646352464351,2.03953177587582));
#41919=CARTESIAN_POINT('Ctrl Pts',(1.8029499684322,-1.54109737446693,2.04093196651037));
#41920=CARTESIAN_POINT('Ctrl Pts',(1.82390564601439,-1.51615213820122,2.0431593841685));
#41921=CARTESIAN_POINT('Ctrl Pts',(1.83173793933251,-1.50668020832993,2.04399483810991));
#41922=CARTESIAN_POINT('Ctrl Pts',(1.84704906109139,-1.48786793152956,2.04563319536527));
#41923=CARTESIAN_POINT('Ctrl Pts',(1.85453147343717,-1.47853110924855,2.04643630854342));
#41924=CARTESIAN_POINT('Ctrl Pts',(1.8735575028594,-1.45441806712347,2.04848597520045));
#41925=CARTESIAN_POINT('Ctrl Pts',(1.88499742426595,-1.43956048655148,2.04972567741397));
#41926=CARTESIAN_POINT('Ctrl Pts',(1.93598244172652,-1.37169370037781,2.05529215505019));
#41927=CARTESIAN_POINT('Ctrl Pts',(1.97347943298454,-1.31717583229765,2.05950193928785));
#41928=CARTESIAN_POINT('Ctrl Pts',(2.09722486672678,-1.12008581911671,2.07409085967496));
#41929=CARTESIAN_POINT('Ctrl Pts',(2.17069203216557,-0.970074474317937,
2.08412099742966));
#41930=CARTESIAN_POINT('Ctrl Pts',(2.25486304642878,-0.739593060952089,
2.09946653763378));
#41931=CARTESIAN_POINT('Ctrl Pts',(2.27818293213832,-0.664293585535105,
2.10446458509643));
#41932=CARTESIAN_POINT('Ctrl Pts',(2.30505131001156,-0.559296898056516,
2.11150076645997));
#41933=CARTESIAN_POINT('Ctrl Pts',(2.31185289062396,-0.530481525902981,
2.1134382791473));
#41934=CARTESIAN_POINT('Ctrl Pts',(2.32246050689161,-0.481453946559815,
2.11674974631156));
#41935=CARTESIAN_POINT('Ctrl Pts',(2.32654637016368,-0.461305378419504,
2.11811485356412));
#41936=CARTESIAN_POINT('Ctrl Pts',(2.3343314156325,-0.420176935455452,2.120911190234));
#41937=CARTESIAN_POINT('Ctrl Pts',(2.33801088154881,-0.399195294041209,
2.12234289466152));
#41938=CARTESIAN_POINT('Ctrl Pts',(2.34657899441084,-0.34614620754104,2.12597703930065));
#41939=CARTESIAN_POINT('Ctrl Pts',(2.35109318640605,-0.314023607666797,
2.12819075162327));
#41940=CARTESIAN_POINT('Ctrl Pts',(2.3696820198827,-0.158691327416637,2.13896390528826));
#41941=CARTESIAN_POINT('Ctrl Pts',(2.37473564361942,-0.0346151462326547,
2.14779094708367));
#41942=CARTESIAN_POINT('Ctrl Pts',(2.3636818580042,0.25885386791482,2.16905448838635));
#41943=CARTESIAN_POINT('Ctrl Pts',(2.3391122421271,0.427265330510222,2.18157852282985));
#41944=CARTESIAN_POINT('Ctrl Pts',(2.29058335972866,0.61566433998418,2.19519917302738));
#41945=CARTESIAN_POINT('Ctrl Pts',(2.28401151629569,0.639614116995389,2.19692233546188));
#41946=CARTESIAN_POINT('Ctrl Pts',(2.27331852205391,0.67631374221941,2.19954552916359));
#41947=CARTESIAN_POINT('Ctrl Pts',(2.26946369569198,0.68913854618233,2.20045892647933));
#41948=CARTESIAN_POINT('Ctrl Pts',(2.26210544288602,0.712887516914196,2.20214337313136));
#41949=CARTESIAN_POINT('Ctrl Pts',(2.2586312311089,0.723819462909523,2.2029158750223));
#41950=CARTESIAN_POINT('Ctrl Pts',(2.25015115622019,0.749847145849368,2.20474882985971));
#41951=CARTESIAN_POINT('Ctrl Pts',(2.2450725648758,0.764918414125853,2.20580521498074));
#41952=CARTESIAN_POINT('Ctrl Pts',(2.22661991997986,0.817911116336573,2.2095057478403));
#41953=CARTESIAN_POINT('Ctrl Pts',(2.21243281491838,0.855544467836024,2.21210854298126));
#41954=CARTESIAN_POINT('Ctrl Pts',(2.17283760329181,0.952993192564637,2.21882657644898));
#41955=CARTESIAN_POINT('Ctrl Pts',(2.14591595133694,1.01215861297101,2.22288389865251));
#41956=CARTESIAN_POINT('Ctrl Pts',(2.02818561000403,1.24501229011298,2.23903908820727));
#41957=CARTESIAN_POINT('Ctrl Pts',(1.91845402014795,1.40823387897523,2.25086585964863));
#41958=CARTESIAN_POINT('Ctrl Pts',(1.76509493988458,1.5846348038616,2.26590461970806));
#41959=CARTESIAN_POINT('Ctrl Pts',(1.73961070548738,1.6125699836099,2.26836108307984));
#41960=CARTESIAN_POINT('Ctrl Pts',(1.69799245970479,1.65605579837115,2.27231532172865));
#41961=CARTESIAN_POINT('Ctrl Pts',(1.68228643563223,1.67200822153385,2.2737952303158));
#41962=CARTESIAN_POINT('Ctrl Pts',(1.65190819199447,1.70200167173956,2.2766360539972));
#41963=CARTESIAN_POINT('Ctrl Pts',(1.63727677971212,1.71608131184288,2.277995127723));
#41964=CARTESIAN_POINT('Ctrl Pts',(1.60300849844241,1.74822008626292,2.28115838970975));
#41965=CARTESIAN_POINT('Ctrl Pts',(1.58324442948389,1.76613892259814,2.28296818540969));
#41966=CARTESIAN_POINT('Ctrl Pts',(1.51667532359892,1.82447750443183,2.28901880161535));
#41967=CARTESIAN_POINT('Ctrl Pts',(1.4685953396413,1.86339710252776,2.29331770780599));
#41968=CARTESIAN_POINT('Ctrl Pts',(1.34311505976353,1.95709529108439,2.30436599142154));
#41969=CARTESIAN_POINT('Ctrl Pts',(1.26385294231681,2.00919209831419,2.31119377511628));
#41970=CARTESIAN_POINT('Ctrl Pts',(1.0487023163016,2.13282644491195,2.3292224757838));
#41971=CARTESIAN_POINT('Ctrl Pts',(0.90860329398233,2.19617198053371,2.34049057208151));
#41972=CARTESIAN_POINT('Ctrl Pts',(0.741191978470014,2.25308250126753,2.35284402226576));
#41973=CARTESIAN_POINT('Ctrl Pts',(0.718911870851121,2.26029027537264,2.3544658167008));
#41974=CARTESIAN_POINT('Ctrl Pts',(0.684147020658825,2.27097086396686,2.35695819240205));
#41975=CARTESIAN_POINT('Ctrl Pts',(0.671735050921496,2.27467313072325,2.35784054553979));
#41976=CARTESIAN_POINT('Ctrl Pts',(0.648153882010265,2.28149711350644,2.35950194032967));
#41977=CARTESIAN_POINT('Ctrl Pts',(0.636991275923464,2.28463884528914,2.3602819849293));
#41978=CARTESIAN_POINT('Ctrl Pts',(0.609623388168784,2.29212540119212,2.36217961556006));
#41979=CARTESIAN_POINT('Ctrl Pts',(0.593393861678064,2.29638047683091,2.3632923202811));
#41980=CARTESIAN_POINT('Ctrl Pts',(0.531831379473651,2.31182473180188,2.36747023293445));
#41981=CARTESIAN_POINT('Ctrl Pts',(0.4862136975798,2.32184734565715,2.37047864595902));
#41982=CARTESIAN_POINT('Ctrl Pts',(0.359291850114696,2.34582788666199,2.37868266362779));
#41983=CARTESIAN_POINT('Ctrl Pts',(0.277508407270747,2.35690260772842,2.38378385170301));
#41984=CARTESIAN_POINT('Ctrl Pts',(0.0249800131020579,2.37776877591972,
2.39938974117179));
#41985=CARTESIAN_POINT('Ctrl Pts',(-0.146354628853781,2.37339046599887,
2.40981451058443));
#41986=CARTESIAN_POINT('Ctrl Pts',(-0.352627515240425,2.34568502630476,
2.42321251274684));
#41987=CARTESIAN_POINT('Ctrl Pts',(-0.389406246152691,2.33986045383947,
2.42563265525156));
#41988=CARTESIAN_POINT('Ctrl Pts',(-0.447938143061073,2.32917268604736,
2.42954249705843));
#41989=CARTESIAN_POINT('Ctrl Pts',(-0.469787103924929,2.32486429778378,
2.43101504862357));
#41990=CARTESIAN_POINT('Ctrl Pts',(-0.511466963434117,2.31603393790522,
2.43385082297768));
#41991=CARTESIAN_POINT('Ctrl Pts',(-0.531306783926268,2.31156326199547,
2.43521233002938));
#41992=CARTESIAN_POINT('Ctrl Pts',(-0.577272120095192,2.30058249139106,
2.43839503564563));
#41993=CARTESIAN_POINT('Ctrl Pts',(-0.60334871334723,2.293881672843,2.44022206801229));
#41994=CARTESIAN_POINT('Ctrl Pts',(-0.690524329046958,2.2698911633327,2.44640493076675));
#41995=CARTESIAN_POINT('Ctrl Pts',(-0.751037438165423,2.25059353249019,
2.45082244216168));
#41996=CARTESIAN_POINT('Ctrl Pts',(-0.903681953558604,2.19507325329013,
2.46229351040683));
#41997=CARTESIAN_POINT('Ctrl Pts',(-0.994449394707747,2.15547091956026,
2.46943387768338));
#41998=CARTESIAN_POINT('Ctrl Pts',(-1.21201834639803,2.04387073742402,2.48721410283684));
#41999=CARTESIAN_POINT('Ctrl Pts',(-1.33517973024596,1.96562892411218,2.49789013064329));
#42000=CARTESIAN_POINT('Ctrl Pts',(-1.4693002142571,1.8619682891847,2.50974418884147));
#42001=CARTESIAN_POINT('Ctrl Pts',(-1.48798538419434,1.84707028342696,2.51140072467));
#42002=CARTESIAN_POINT('Ctrl Pts',(-1.516631205429,1.82351359779278,2.51394430278957));
#42003=CARTESIAN_POINT('Ctrl Pts',(-1.52674959428197,1.81505034403511,2.51484354412293));
#42004=CARTESIAN_POINT('Ctrl Pts',(-1.54557133490461,1.79903863562786,2.51651692269486));
#42005=CARTESIAN_POINT('Ctrl Pts',(-1.55429070116523,1.79151086676417,2.51729229850691));
#42006=CARTESIAN_POINT('Ctrl Pts',(-1.57519395151704,1.77319678400936,2.51915222073237));
#42007=CARTESIAN_POINT('Ctrl Pts',(-1.58732225850853,1.76234812208739,2.5202323463702));
#42008=CARTESIAN_POINT('Ctrl Pts',(-1.63096360932807,1.72249527428285,2.52412671424529));
#42009=CARTESIAN_POINT('Ctrl Pts',(-1.66180306751072,1.69276204616273,2.52689364616598));
#42010=CARTESIAN_POINT('Ctrl Pts',(-1.7420574487651,1.6110778225241,2.53419033041726));
#42011=CARTESIAN_POINT('Ctrl Pts',(-1.78995209193275,1.55769339364596,2.53864905113636));
#42012=CARTESIAN_POINT('Ctrl Pts',(-1.95712380270183,1.35344887476906,2.55494915465022));
#42013=CARTESIAN_POINT('Ctrl Pts',(-2.06033953236469,1.19044207352411,2.56659783522856));
#42014=CARTESIAN_POINT('Ctrl Pts',(-2.15749649940084,0.985692756810211,
2.58122954597995));
#42015=CARTESIAN_POINT('Ctrl Pts',(-2.17156489320032,0.954299260830908,
2.58347062928558));
#42016=CARTESIAN_POINT('Ctrl Pts',(-2.19338411794321,0.902626618631597,
2.58716195755577));
#42017=CARTESIAN_POINT('Ctrl Pts',(-2.20154833519359,0.88252681430177,2.58859842555104));
#42018=CARTESIAN_POINT('Ctrl Pts',(-2.21691021404479,0.843166549286795,
2.59141401724238));
#42019=CARTESIAN_POINT('Ctrl Pts',(-2.22413542343369,0.823918867562813,
2.59279208825022));
#42020=CARTESIAN_POINT('Ctrl Pts',(-2.24074498307047,0.777860384310956,
2.59609378211293));
#42021=CARTESIAN_POINT('Ctrl Pts',(-2.24989950488411,0.750970675547836,
2.59802462346734));
#42022=CARTESIAN_POINT('Ctrl Pts',(-2.28130217590741,0.652997565999373,
2.60507455568915));
#42023=CARTESIAN_POINT('Ctrl Pts',(-2.3006799337004,0.581046721417356,2.61028182104385));
#42024=CARTESIAN_POINT('Ctrl Pts',(-2.34091354263455,0.397680607579599,
2.62362330555379));
#42025=CARTESIAN_POINT('Ctrl Pts',(-2.35721448697413,0.285532433415052,
2.63185297112801));
#42026=CARTESIAN_POINT('Ctrl Pts',(-2.36545139057093,0.172736161084002,
2.64008830168392));
#42027=CARTESIAN_POINT('Origin',(0.,0.,-1.84858989190501));
#42028=CARTESIAN_POINT('',(-2.36545134965682,0.17273672136148,3.83914957969666));
#42029=CARTESIAN_POINT('',(-2.3654513605298,0.172736572467239,3.64082947459234));
#42030=CARTESIAN_POINT('',(-2.36545134966535,0.172736721244682,-1.84858989190501));
#42031=CARTESIAN_POINT('',(-2.37174919235095,0.0019573151533352,2.84812596863768));
#42032=CARTESIAN_POINT('Ctrl Pts',(-2.36545134965682,0.17273672136148,3.83914957969666));
#42033=CARTESIAN_POINT('Ctrl Pts',(-2.36496531051115,0.179392526473733,
3.83870004047593));
#42034=CARTESIAN_POINT('Ctrl Pts',(-2.36445118140828,0.186046256021305,
3.8382496373551));
#42035=CARTESIAN_POINT('Ctrl Pts',(-2.36132563377815,0.22438874170804,3.83564829188122));
#42036=CARTESIAN_POINT('Ctrl Pts',(-2.35810538440664,0.256023212159722,
3.83347885285856));
#42037=CARTESIAN_POINT('Ctrl Pts',(-2.33944156017782,0.408811963707815,
3.82288325940782));
#42038=CARTESIAN_POINT('Ctrl Pts',(-2.31529341069665,0.528698882910509,
3.81419633380283));
#42039=CARTESIAN_POINT('Ctrl Pts',(-2.23452559481581,0.813936547990445,
3.79273931456493));
#42040=CARTESIAN_POINT('Ctrl Pts',(-2.16866932197986,0.975948323225499,
3.7798550951437));
#42041=CARTESIAN_POINT('Ctrl Pts',(-2.07424916464073,1.15033102575288,3.76598350972286));
#42042=CARTESIAN_POINT('Ctrl Pts',(-2.06253304411047,1.17120818580878,3.76432359254829));
#42043=CARTESIAN_POINT('Ctrl Pts',(-2.04398617676241,1.20311541334203,3.76179191220107));
#42044=CARTESIAN_POINT('Ctrl Pts',(-2.03737802793863,1.21427220148476,3.7609076811755));
#42045=CARTESIAN_POINT('Ctrl Pts',(-2.0249371331119,1.23488912870589,3.75927634952197));
#42046=CARTESIAN_POINT('Ctrl Pts',(-2.01912915659518,1.2443628925082,3.75852788236576));
#42047=CARTESIAN_POINT('Ctrl Pts',(-2.00514565369015,1.26681658368055,3.75675617775592));
#42048=CARTESIAN_POINT('Ctrl Pts',(-1.99691046536362,1.27975856047989,3.75573670656421));
#42049=CARTESIAN_POINT('Ctrl Pts',(-1.96770379435595,1.32468972345186,3.75220003223985));
#42050=CARTESIAN_POINT('Ctrl Pts',(-1.94608344699825,1.356252441299,3.74972037846208));
#42051=CARTESIAN_POINT('Ctrl Pts',(-1.88820597716092,1.43650971228254,3.74338942979372));
#42052=CARTESIAN_POINT('Ctrl Pts',(-1.85082530978085,1.48436132875604,3.73958900239957));
#42053=CARTESIAN_POINT('Ctrl Pts',(-1.67952830912838,1.68709471662873,3.72312580439512));
#42054=CARTESIAN_POINT('Ctrl Pts',(-1.52773254041533,1.82568740013169,3.71081558557811));
#42055=CARTESIAN_POINT('Ctrl Pts',(-1.32966995051729,1.9643189861908,3.69525387651646));
#42056=CARTESIAN_POINT('Ctrl Pts',(-1.29881865935231,1.98485291908901,3.6928454878576));
#42057=CARTESIAN_POINT('Ctrl Pts',(-1.24907422896689,2.01630525567888,3.68897856807118));
#42058=CARTESIAN_POINT('Ctrl Pts',(-1.23048895088978,2.02770071836518,3.68753736526352));
#42059=CARTESIAN_POINT('Ctrl Pts',(-1.19485187791865,2.04888102403419,3.68477904020907));
#42060=CARTESIAN_POINT('Ctrl Pts',(-1.17783027272596,2.05871325594797,3.68346375335926));
#42061=CARTESIAN_POINT('Ctrl Pts',(-1.13834901662877,2.08086900352375,3.68041693778062));
#42062=CARTESIAN_POINT('Ctrl Pts',(-1.11580832925897,2.09304227815921,3.67868033741289));
#42063=CARTESIAN_POINT('Ctrl Pts',(-1.04160111852939,2.13157907780519,3.67297024844625));
#42064=CARTESIAN_POINT('Ctrl Pts',(-0.989167450738712,2.15641114694513,
3.66894595952278));
#42065=CARTESIAN_POINT('Ctrl Pts',(-0.856591164501748,2.21334492664889,
3.65879194246473));
#42066=CARTESIAN_POINT('Ctrl Pts',(-0.77550996172097,2.2430394827655,3.65259856302511));
#42067=CARTESIAN_POINT('Ctrl Pts',(-0.564920384808152,2.30737903955457,
3.63663425020827));
#42068=CARTESIAN_POINT('Ctrl Pts',(-0.4337579726088,2.33559165911594,3.62679442473676));
#42069=CARTESIAN_POINT('Ctrl Pts',(-0.254911908563656,2.35846746221174,
3.61392909283571));
#42070=CARTESIAN_POINT('Ctrl Pts',(-0.208743858329438,2.36300137378563,
3.61065837530656));
#42071=CARTESIAN_POINT('Ctrl Pts',(-0.145615466565604,2.3673359689762,3.60627916146979));
#42072=CARTESIAN_POINT('Ctrl Pts',(-0.128749123430831,2.36831314607568,
3.60511818905557));
#42073=CARTESIAN_POINT('Ctrl Pts',(-0.100642888636665,2.36964036773299,
3.60320013220399));
#42074=CARTESIAN_POINT('Ctrl Pts',(-0.0894085569419681,2.37009084086739,
3.6024378888533));
#42075=CARTESIAN_POINT('Ctrl Pts',(-0.0659584618580572,2.37086415689739,
3.60085654991306));
#42076=CARTESIAN_POINT('Ctrl Pts',(-0.0537427255754355,2.37117251691621,
3.60003822126383));
#42077=CARTESIAN_POINT('Ctrl Pts',(-0.020483171645991,2.37175491753093,
3.59782362974894));
#42078=CARTESIAN_POINT('Ctrl Pts',(0.000563325769140379,2.37184331386325,
3.59643690395749));
#42079=CARTESIAN_POINT('Ctrl Pts',(0.147784986859749,2.3705019178284,3.5868218610713));
#42080=CARTESIAN_POINT('Ctrl Pts',(0.273684902223934,2.35928473486872,3.57903067362696));
#42081=CARTESIAN_POINT('Ctrl Pts',(0.560624806980556,2.31042755041321,3.56112250808857));
#42082=CARTESIAN_POINT('Ctrl Pts',(0.719797439871965,2.26589074819803,3.55104890807293));
#42083=CARTESIAN_POINT('Ctrl Pts',(0.907880707879646,2.19142721041078,3.53803290704875));
#42084=CARTESIAN_POINT('Ctrl Pts',(0.942368469223541,2.17681924439915,3.53559965615468));
#42085=CARTESIAN_POINT('Ctrl Pts',(0.996434283501278,2.15239297760444,3.53170232929647));
#42086=CARTESIAN_POINT('Ctrl Pts',(1.01624788086959,2.14310919073928,3.53025607253192));
#42087=CARTESIAN_POINT('Ctrl Pts',(1.05359641205499,2.12497490762278,3.52749400360351));
#42088=CARTESIAN_POINT('Ctrl Pts',(1.07115546643094,2.11617808445448,3.52618010814896));
#42089=CARTESIAN_POINT('Ctrl Pts',(1.11122699224198,2.09547634180801,3.52314518941859));
#42090=CARTESIAN_POINT('Ctrl Pts',(1.13366067471577,2.08342504444885,3.52141922947268));
#42091=CARTESIAN_POINT('Ctrl Pts',(1.20570456972575,2.04321520289551,3.51578635106114));
#42092=CARTESIAN_POINT('Ctrl Pts',(1.25449088008122,2.01362945393628,3.51183054090305));
#42093=CARTESIAN_POINT('Ctrl Pts',(1.37245771762206,1.93613842592178,3.50190403980025));
#42094=CARTESIAN_POINT('Ctrl Pts',(1.44024321020899,1.88625805735089,3.49587350235481));
#42095=CARTESIAN_POINT('Ctrl Pts',(1.63538614460526,1.72599982981445,3.4775797798561));
#42096=CARTESIAN_POINT('Ctrl Pts',(1.75378885886107,1.60555052427525,3.46514962819775));
#42097=CARTESIAN_POINT('Ctrl Pts',(1.87395401107852,1.45400075834754,3.45160353440071));
#42098=CARTESIAN_POINT('Ctrl Pts',(1.88916202079736,1.43418576904441,3.44986984885094));
#42099=CARTESIAN_POINT('Ctrl Pts',(1.91191689168535,1.4035475521836,3.44725021458056));
#42100=CARTESIAN_POINT('Ctrl Pts',(1.91969070881282,1.39289609618989,3.4463504913652));
#42101=CARTESIAN_POINT('Ctrl Pts',(1.93382894443396,1.37318108940664,3.44470610932978));
#42102=CARTESIAN_POINT('Ctrl Pts',(1.94021906016955,1.36413734513345,3.4439598610505));
#42103=CARTESIAN_POINT('Ctrl Pts',(1.95510792123208,1.34274929100654,3.44221348877139));
#42104=CARTESIAN_POINT('Ctrl Pts',(1.9635533524251,1.33036870942975,3.44121680314907));
#42105=CARTESIAN_POINT('Ctrl Pts',(1.99185125563075,1.28802881955324,3.43785320810683));
#42106=CARTESIAN_POINT('Ctrl Pts',(2.01114091158604,1.25769718944114,3.43551912013507));
#42107=CARTESIAN_POINT('Ctrl Pts',(2.05835904054724,1.17958373922833,3.42966600445682));
#42108=CARTESIAN_POINT('Ctrl Pts',(2.08531912489945,1.13124030541228,3.42618870170665));
#42109=CARTESIAN_POINT('Ctrl Pts',(2.1625908721236,0.98051226067201,3.41565066818045));
#42110=CARTESIAN_POINT('Ctrl Pts',(2.2072304852554,0.875407497879184,3.40870977820598));
#42111=CARTESIAN_POINT('Ctrl Pts',(2.2795442896056,0.663964378204742,3.3948901449483));
#42112=CARTESIAN_POINT('Ctrl Pts',(2.30774194590003,0.558116455860594,3.38803656110826));
#42113=CARTESIAN_POINT('Ctrl Pts',(2.3345586010097,0.419571231901951,3.37890212065695));
#42114=CARTESIAN_POINT('Ctrl Pts',(2.33996001118584,0.388318006552668,3.37683170790399));
#42115=CARTESIAN_POINT('Ctrl Pts',(2.3478505654471,0.336489008829084,3.37337709063717));
#42116=CARTESIAN_POINT('Ctrl Pts',(2.35069969057951,0.315971597548835,3.37200409873295));
#42117=CARTESIAN_POINT('Ctrl Pts',(2.35578469666723,0.275465063603467,3.36928152986511));
#42118=CARTESIAN_POINT('Ctrl Pts',(2.35803576681631,0.255479585395643,3.36793254437998));
#42119=CARTESIAN_POINT('Ctrl Pts',(2.36286783440648,0.207049156803198,3.36464868742119));
#42120=CARTESIAN_POINT('Ctrl Pts',(2.36518964585235,0.178582121186022,3.36270604930908));
#42121=CARTESIAN_POINT('Ctrl Pts',(2.37206739816128,0.070110004797668,3.35525328110018));
#42122=CARTESIAN_POINT('Ctrl Pts',(2.37308144147758,-0.010058136187945,
3.34963854699891));
#42123=CARTESIAN_POINT('Ctrl Pts',(2.36414040774578,-0.245204303170176,
3.33286688036197));
#42124=CARTESIAN_POINT('Ctrl Pts',(2.3430347746088,-0.399332341407755,3.32146107362126));
#42125=CARTESIAN_POINT('Ctrl Pts',(2.28930142624893,-0.624609359746595,
3.30470821324799));
#42126=CARTESIAN_POINT('Ctrl Pts',(2.26798731288799,-0.698049895537723,
3.29924000878697));
#42127=CARTESIAN_POINT('Ctrl Pts',(2.2367968940019,-0.788873728356599,3.29256432594585));
#42128=CARTESIAN_POINT('Ctrl Pts',(2.2302021058487,-0.807329383066043,3.29121250946687));
#42129=CARTESIAN_POINT('Ctrl Pts',(2.21923293017176,-0.836866236036345,
3.28905893062079));
#42130=CARTESIAN_POINT('Ctrl Pts',(2.2150026567167,-0.847999493803162,3.28824947213989));
#42131=CARTESIAN_POINT('Ctrl Pts',(2.20649393707898,-0.869894632662896,
3.28666272770784));
#42132=CARTESIAN_POINT('Ctrl Pts',(2.20222021493609,-0.880657879806769,
3.2858852331419));
#42133=CARTESIAN_POINT('Ctrl Pts',(2.1910852558284,-0.908112953807342,3.28390740777524));
#42134=CARTESIAN_POINT('Ctrl Pts',(2.18411186395595,-0.924758968044414,
3.28271340791755));
#42135=CARTESIAN_POINT('Ctrl Pts',(2.15245710759393,-0.997965175055557,
3.27747838998661));
#42136=CARTESIAN_POINT('Ctrl Pts',(2.12576182562203,-1.05363376785842,3.27353975523884));
#42137=CARTESIAN_POINT('Ctrl Pts',(2.03071779237441,-1.23347460936641,3.26075588976711));
#42138=CARTESIAN_POINT('Ctrl Pts',(1.95341758325166,-1.35256716708233,3.25217763128086));
#42139=CARTESIAN_POINT('Ctrl Pts',(1.80115701151872,-1.54662449257737,3.2369050784427));
#42140=CARTESIAN_POINT('Ctrl Pts',(1.73096602550294,-1.62479748812019,3.23031969847355));
#42141=CARTESIAN_POINT('Ctrl Pts',(1.63329502933882,-1.72003968782065,3.22148685959775));
#42142=CARTESIAN_POINT('Ctrl Pts',(1.61032090532284,-1.74156699944358,3.21943119209404));
#42143=CARTESIAN_POINT('Ctrl Pts',(1.57156621659445,-1.77645851108627,3.21599444910875));
#42144=CARTESIAN_POINT('Ctrl Pts',(1.55602680485632,-1.79008540372232,3.21462434212483));
#42145=CARTESIAN_POINT('Ctrl Pts',(1.52499378691393,-1.81658960741378,3.2119023566361));
#42146=CARTESIAN_POINT('Ctrl Pts',(1.50951024938476,-1.82947604972054,3.21055100710892));
#42147=CARTESIAN_POINT('Ctrl Pts',(1.47154048211866,-1.86026685858309,3.20725222448123));
#42148=CARTESIAN_POINT('Ctrl Pts',(1.44888976531283,-1.87796232655483,3.20529685156905));
#42149=CARTESIAN_POINT('Ctrl Pts',(1.36056030280287,-1.94441882480595,3.19771562625172));
#42150=CARTESIAN_POINT('Ctrl Pts',(1.2927035622622,-1.99017682536731,3.1919803503454));
#42151=CARTESIAN_POINT('Ctrl Pts',(1.08287713841389,-2.11640559949154,3.17451367873617));
#42152=CARTESIAN_POINT('Ctrl Pts',(0.93483353083411,-2.18583504112227,3.1625033573219));
#42153=CARTESIAN_POINT('Ctrl Pts',(0.717052637924405,-2.26176916254781,
3.14587048381918));
#42154=CARTESIAN_POINT('Ctrl Pts',(0.652318788811348,-2.28128167770181,
3.1410534887113));
#42155=CARTESIAN_POINT('Ctrl Pts',(0.568401635671625,-2.30271135217159,
3.13503795696152));
#42156=CARTESIAN_POINT('Ctrl Pts',(0.54991205703135,-2.30719673562864,3.13372659957361));
#42157=CARTESIAN_POINT('Ctrl Pts',(0.519882866350561,-2.31409999581352,
3.13162162914518));
#42158=CARTESIAN_POINT('Ctrl Pts',(0.508376094621702,-2.31665507720023,
3.13082090036402));
#42159=CARTESIAN_POINT('Ctrl Pts',(0.48542357474766,-2.32157243741844,3.1292359920404));
#42160=CARTESIAN_POINT('Ctrl Pts',(0.473978491943804,-2.32393610742068,
3.12845176478038));
#42161=CARTESIAN_POINT('Ctrl Pts',(0.444318251115926,-2.32983338648486,
3.12643401410098));
#42162=CARTESIAN_POINT('Ctrl Pts',(0.426077850714125,-2.33323810060432,
3.12520733621009));
#42163=CARTESIAN_POINT('Ctrl Pts',(0.340885267093001,-2.34810755786689,
3.11953617647634));
#42164=CARTESIAN_POINT('Ctrl Pts',(0.273494443330123,-2.35690780685675,
3.11521637599224));
#42165=CARTESIAN_POINT('Ctrl Pts',(0.0249017643008804,-2.3785615611046,
3.09958980409025));
#42166=CARTESIAN_POINT('Ctrl Pts',(-0.157220504902397,-2.3734913192797,
3.08869288087847));
#42167=CARTESIAN_POINT('Ctrl Pts',(-0.403007374462072,-2.33821124249097,
3.07306724511153));
#42168=CARTESIAN_POINT('Ctrl Pts',(-0.468595086142282,-2.32595447480647,
3.06881173397738));
#42169=CARTESIAN_POINT('Ctrl Pts',(-0.560431777004879,-2.30475031478132,
3.06267939008483));
#42170=CARTESIAN_POINT('Ctrl Pts',(-0.587177282125869,-2.2980819236241,
3.06087245299169));
#42171=CARTESIAN_POINT('Ctrl Pts',(-0.633060205886138,-2.28578879978997,
3.05773305331591));
#42172=CARTESIAN_POINT('Ctrl Pts',(-0.652254428287186,-2.28038588442379,
3.05640769519611));
#42173=CARTESIAN_POINT('Ctrl Pts',(-0.691521671280252,-2.26879636918036,
3.05367034680632));
#42174=CARTESIAN_POINT('Ctrl Pts',(-0.71158514005088,-2.26258386075118,
3.05225763095738));
#42175=CARTESIAN_POINT('Ctrl Pts',(-0.763096051207286,-2.24588097771203,
3.04859293120847));
#42176=CARTESIAN_POINT('Ctrl Pts',(-0.794409911375765,-2.23499656669142,
3.04632850539249));
#42177=CARTESIAN_POINT('Ctrl Pts',(-0.970132617614989,-2.16975756937009,
3.03340637419198));
#42178=CARTESIAN_POINT('Ctrl Pts',(-1.10917176046243,-2.10207713982111,
3.02231642798197));
#42179=CARTESIAN_POINT('Ctrl Pts',(-1.35924902342421,-1.94859172727142,
3.00096001913634));
#42180=CARTESIAN_POINT('Ctrl Pts',(-1.47123503541127,-1.8654867715933,2.99076869723717));
#42181=CARTESIAN_POINT('Ctrl Pts',(-1.59328992644848,-1.75704435564816,
2.9793458450475));
#42182=CARTESIAN_POINT('Ctrl Pts',(-1.61104370724045,-1.740780267361,2.97767617604026));
#42183=CARTESIAN_POINT('Ctrl Pts',(-1.6379953051163,-1.71532455507567,2.97513284738791));
#42184=CARTESIAN_POINT('Ctrl Pts',(-1.64736982214983,-1.70632342697059,
2.97424655021329));
#42185=CARTESIAN_POINT('Ctrl Pts',(-1.66381872974742,-1.69026775611832,
2.97268921888215));
#42186=CARTESIAN_POINT('Ctrl Pts',(-1.67092294119698,-1.68324519385593,
2.97201594268709));
#42187=CARTESIAN_POINT('Ctrl Pts',(-1.68827298766562,-1.66587645958595,
2.97036966318114));
#42188=CARTESIAN_POINT('Ctrl Pts',(-1.69846824762546,-1.65548050359335,
2.96940046329458));
#42189=CARTESIAN_POINT('Ctrl Pts',(-1.73166768976955,-1.62099795260456,
2.96623568627904));
#42190=CARTESIAN_POINT('Ctrl Pts',(-1.75426136064373,-1.59651955526325,
2.9640679078593));
#42191=CARTESIAN_POINT('Ctrl Pts',(-1.80917120256205,-1.53445547004214,
2.95873955027437));
#42192=CARTESIAN_POINT('Ctrl Pts',(-1.84083978651161,-1.4963166395412,2.95561176719031));
#42193=CARTESIAN_POINT('Ctrl Pts',(-1.98447785519668,-1.31186245852775,
2.94101067545729));
#42194=CARTESIAN_POINT('Ctrl Pts',(-2.08034327435035,-1.1538241375076,2.92995190101031));
#42195=CARTESIAN_POINT('Ctrl Pts',(-2.18200528241339,-0.931493502422634,
2.91451037783979));
#42196=CARTESIAN_POINT('Ctrl Pts',(-2.20495854843782,-0.875776281825256,
2.9106549035364));
#42197=CARTESIAN_POINT('Ctrl Pts',(-2.23407838063787,-0.796662486810262,
2.90516356765353));
#42198=CARTESIAN_POINT('Ctrl Pts',(-2.24204738332637,-0.773951414327082,
2.90358539003129));
#42199=CARTESIAN_POINT('Ctrl Pts',(-2.25597669366231,-0.732232131626875,
2.90068087047535));
#42200=CARTESIAN_POINT('Ctrl Pts',(-2.26204585114382,-0.713262408976186,
2.89935815168019));
#42201=CARTESIAN_POINT('Ctrl Pts',(-2.27392309393666,-0.674461820250767,
2.89664740905895));
#42202=CARTESIAN_POINT('Ctrl Pts',(-2.27971234738101,-0.65462703234631,
2.89525891395057));
#42203=CARTESIAN_POINT('Ctrl Pts',(-2.29365916324721,-0.604412984476821,
2.89173562107873));
#42204=CARTESIAN_POINT('Ctrl Pts',(-2.30147267868288,-0.573943168353824,
2.88959018617532));
#42205=CARTESIAN_POINT('Ctrl Pts',(-2.31947076974247,-0.497466755750736,
2.88418411341739));
#42206=CARTESIAN_POINT('Ctrl Pts',(-2.32889427525843,-0.451296760904466,
2.8809012195654));
#42207=CARTESIAN_POINT('Ctrl Pts',(-2.36021728362533,-0.270502473907583,
2.86797109305728));
#42208=CARTESIAN_POINT('Ctrl Pts',(-2.37186171063907,-0.134385142783268,
2.85805660689887));
#42209=CARTESIAN_POINT('Ctrl Pts',(-2.37174919235095,0.0019573151533352,
2.84812596863768));
#42210=CARTESIAN_POINT('Ctrl Pts',(-2.3717491913197,0.00195856436296467,
2.84812587765026));
#42211=CARTESIAN_POINT('Ctrl Pts',(-2.37170212969245,0.058948458838013,
2.84397496217231));
#42212=CARTESIAN_POINT('Ctrl Pts',(-2.36960100172951,0.115911523124276,
2.83982926533819));
#42213=CARTESIAN_POINT('Ctrl Pts',(-2.36545134753269,0.172736750449338,
2.83572259012909));
#42214=CARTESIAN_POINT('',(-2.37174994626123,-0.00144183595024523,2.65273840708708));
#42215=CARTESIAN_POINT('Ctrl Pts',(-2.36545139057093,0.172736161084002,
2.64008830168392));
#42216=CARTESIAN_POINT('Ctrl Pts',(-2.36968143502358,0.114809873560342,
2.64431753830474));
#42217=CARTESIAN_POINT('Ctrl Pts',(-2.37178483994934,0.0567125215558486,
2.64854624104343));
#42218=CARTESIAN_POINT('Ctrl Pts',(-2.37174956359742,-0.00143877568085956,
2.65273885301577));
#42219=CARTESIAN_POINT('Ctrl Pts',(-2.3717495617682,-0.00144178789911513,
2.65273907019167));
#42220=CARTESIAN_POINT('Ctrl Pts',(-2.37170869729105,-0.0686640928088483,
2.65758568513456));
#42221=CARTESIAN_POINT('Ctrl Pts',(-2.36880991714627,-0.135861689288376,
2.66237712047973));
#42222=CARTESIAN_POINT('Ctrl Pts',(-2.36181720656935,-0.217321062812207,
2.66805674192593));
#42223=CARTESIAN_POINT('Ctrl Pts',(-2.36044222872002,-0.23177892708601,
2.66905980331548));
#42224=CARTESIAN_POINT('Ctrl Pts',(-2.35778607167011,-0.257226117679556,
2.67081546264293));
#42225=CARTESIAN_POINT('Ctrl Pts',(-2.35656065453419,-0.268220671806938,
2.67157076376477));
#42226=CARTESIAN_POINT('Ctrl Pts',(-2.35391963901662,-0.290499069624113,
2.67309413547133));
#42227=CARTESIAN_POINT('Ctrl Pts',(-2.35249977548238,-0.301781704034808,
2.67386184141381));
#42228=CARTESIAN_POINT('Ctrl Pts',(-2.34909542746515,-0.327347920252172,
2.67559294360465));
#42229=CARTESIAN_POINT('Ctrl Pts',(-2.34706176639614,-0.341624177694819,
2.67655370196905));
#42230=CARTESIAN_POINT('Ctrl Pts',(-2.34024572931977,-0.386534953235174,
2.67956001105642));
#42231=CARTESIAN_POINT('Ctrl Pts',(-2.33499260563589,-0.417096019625067,
2.68158213554441));
#42232=CARTESIAN_POINT('Ctrl Pts',(-2.30237959156813,-0.586821949158959,
2.69272418458075));
#42233=CARTESIAN_POINT('Ctrl Pts',(-2.26317650691132,-0.723431075731699,
2.70137278566001));
#42234=CARTESIAN_POINT('Ctrl Pts',(-2.1677453946956,-0.970113232282793,
2.7176478621772));
#42235=CARTESIAN_POINT('Ctrl Pts',(-2.11469384064466,-1.08088193735488,
2.72522965488955));
#42236=CARTESIAN_POINT('Ctrl Pts',(-2.03172695762217,-1.22439569879042,
2.73584337196682));
#42237=CARTESIAN_POINT('Ctrl Pts',(-2.00912096630732,-1.26114703289005,
2.73863549283612));
#42238=CARTESIAN_POINT('Ctrl Pts',(-1.97270169640577,-1.31688869970518,
2.74299960806788));
#42239=CARTESIAN_POINT('Ctrl Pts',(-1.95958699942411,-1.33632576792876,
2.74454649935343));
#42240=CARTESIAN_POINT('Ctrl Pts',(-1.93467517493862,-1.37209172002778,
2.74744198051341));
#42241=CARTESIAN_POINT('Ctrl Pts',(-1.92295394121791,-1.38847103630833,
2.74878766269736));
#42242=CARTESIAN_POINT('Ctrl Pts',(-1.89624604308154,-1.42480586311497,
2.75181840953896));
#42243=CARTESIAN_POINT('Ctrl Pts',(-1.88115034328365,-1.4446778563513,2.75350751363571));
#42244=CARTESIAN_POINT('Ctrl Pts',(-1.84125803292543,-1.49550656698913,
2.75791233091133));
#42245=CARTESIAN_POINT('Ctrl Pts',(-1.81599428612828,-1.52608501441929,
2.76064573332724));
#42246=CARTESIAN_POINT('Ctrl Pts',(-1.66256155153225,-1.70258794352608,
2.77693210955796));
#42247=CARTESIAN_POINT('Ctrl Pts',(-1.51763938085684,-1.83293857533994,
2.79116073647266));
#42248=CARTESIAN_POINT('Ctrl Pts',(-1.3099706068955,-1.97804924258223,2.80953258374712));
#42249=CARTESIAN_POINT('Ctrl Pts',(-1.26019499741816,-2.01012715015836,
2.81379770168163));
#42250=CARTESIAN_POINT('Ctrl Pts',(-1.17674325712806,-2.0595880396713,2.82067308876567));
#42251=CARTESIAN_POINT('Ctrl Pts',(-1.14375932565918,-2.07808627448954,
2.82332341174638));
#42252=CARTESIAN_POINT('Ctrl Pts',(-1.09660846847167,-2.10306671068279,
2.82700464563663));
#42253=CARTESIAN_POINT('Ctrl Pts',(-1.08280012498202,-2.11020938397262,
2.82807000103581));
#42254=CARTESIAN_POINT('Ctrl Pts',(-1.05880850911127,-2.12232206794716,
2.82989791188266));
#42255=CARTESIAN_POINT('Ctrl Pts',(-1.04865833133323,-2.12735566911528,
2.8306641316177));
#42256=CARTESIAN_POINT('Ctrl Pts',(-1.02627730086469,-2.13825558377023,
2.83233783131822));
#42257=CARTESIAN_POINT('Ctrl Pts',(-1.01403169139831,-2.14408996790642,
2.83324345225128));
#42258=CARTESIAN_POINT('Ctrl Pts',(-0.978483987704463,-2.16065388523661,
2.83584512121146));
#42259=CARTESIAN_POINT('Ctrl Pts',(-0.955056255819943,-2.17111119037089,
2.83752617952256));
#42260=CARTESIAN_POINT('Ctrl Pts',(-0.834770283286746,-2.22247857202935,
2.84601019745816));
#42261=CARTESIAN_POINT('Ctrl Pts',(-0.735428734554925,-2.25729964674856,
2.85253882433277));
#42262=CARTESIAN_POINT('Ctrl Pts',(-0.516518127194684,-2.31803700057488,
2.86654457838164));
#42263=CARTESIAN_POINT('Ctrl Pts',(-0.396603811041486,-2.34153597365893,
2.87399001547749));
#42264=CARTESIAN_POINT('Ctrl Pts',(-0.201714657456177,-2.3643213392082,
2.88629683201334));
#42265=CARTESIAN_POINT('Ctrl Pts',(-0.12765566015911,-2.36947392041282,
2.89101798779091));
#42266=CARTESIAN_POINT('Ctrl Pts',(-0.0251190536508085,-2.37178665750307,
2.89768729834219));
#42267=CARTESIAN_POINT('Ctrl Pts',(0.00325183424697385,-2.37191741649685,
2.89954641851911));
#42268=CARTESIAN_POINT('Ctrl Pts',(0.0521687217423089,-2.37126525783505,
2.90277913286163));
#42269=CARTESIAN_POINT('Ctrl Pts',(0.0727151572509987,-2.37072414260413,
2.9041452422231));
#42270=CARTESIAN_POINT('Ctrl Pts',(0.114940132748127,-2.36906267456761,
2.9069709925939));
#42271=CARTESIAN_POINT('Ctrl Pts',(0.136615452463394,-2.36791160208015,
2.90843144486063));
#42272=CARTESIAN_POINT('Ctrl Pts',(0.192649239668986,-2.36416400876877,
2.91223396326531));
#42273=CARTESIAN_POINT('Ctrl Pts',(0.226971345674578,-2.3611160468859,2.91458951885383));
#42274=CARTESIAN_POINT('Ctrl Pts',(0.451946523280566,-2.33618668167587,
2.93021159344092));
#42275=CARTESIAN_POINT('Ctrl Pts',(0.639379483619011,-2.29198418673891,
2.94417220709906));
#42276=CARTESIAN_POINT('Ctrl Pts',(0.886826411991718,-2.20088608415034,
2.96335244675838));
#42277=CARTESIAN_POINT('Ctrl Pts',(0.953094164954423,-2.1730101839167,2.96855805817798));
#42278=CARTESIAN_POINT('Ctrl Pts',(1.04470191421914,-2.12947650195746,2.97577389887777));
#42279=CARTESIAN_POINT('Ctrl Pts',(1.07116835719663,-2.11628702534304,2.97786085362024));
#42280=CARTESIAN_POINT('Ctrl Pts',(1.11774477167394,-2.09197807253441,2.98152932473105));
#42281=CARTESIAN_POINT('Ctrl Pts',(1.13795261407804,-2.08105491854414,2.98311949058891));
#42282=CARTESIAN_POINT('Ctrl Pts',(1.1692214333354,-2.06356115771325,2.98557419632987));
#42283=CARTESIAN_POINT('Ctrl Pts',(1.18039248042138,-2.05719153774944,2.98644997306991));
#42284=CARTESIAN_POINT('Ctrl Pts',(1.20145531498705,-2.04495365431395,2.98809819320477));
#42285=CARTESIAN_POINT('Ctrl Pts',(1.21135698728067,-2.03910386610605,2.98887164389015));
#42286=CARTESIAN_POINT('Ctrl Pts',(1.23569536293664,-2.02448519981646,2.99077019600599));
#42287=CARTESIAN_POINT('Ctrl Pts',(1.25008200183002,-2.01563349420413,2.99189021737386));
#42288=CARTESIAN_POINT('Ctrl Pts',(1.30176854107398,-1.98306589071793,2.99591060864418));
#42289=CARTESIAN_POINT('Ctrl Pts',(1.33850046938457,-1.95846080140712,2.99876117696602));
#42290=CARTESIAN_POINT('Ctrl Pts',(1.525461798208,-1.82550467312162,3.01335305733504));
#42291=CARTESIAN_POINT('Ctrl Pts',(1.66331491984682,-1.70085137525861,3.02444387549821));
#42292=CARTESIAN_POINT('Ctrl Pts',(1.84182812308832,-1.49674610267465,3.04135778370217));
#42293=CARTESIAN_POINT('Ctrl Pts',(1.89482945900008,-1.42905520387532,3.04679530488164));
#42294=CARTESIAN_POINT('Ctrl Pts',(1.96104640828997,-1.33430751236478,3.05429899253281));
#42295=CARTESIAN_POINT('Ctrl Pts',(1.97759500212729,-1.30965546416525,3.05624184506948));
#42296=CARTESIAN_POINT('Ctrl Pts',(2.00493187577039,-1.26723243831559,3.05957330477027));
#42297=CARTESIAN_POINT('Ctrl Pts',(2.01595747690404,-1.24961805565776,3.06095314156852));
#42298=CARTESIAN_POINT('Ctrl Pts',(2.03782668444745,-1.21363721386525,3.06376615313881));
#42299=CARTESIAN_POINT('Ctrl Pts',(2.04865681946319,-1.19526485288394,3.06519964438768));
#42300=CARTESIAN_POINT('Ctrl Pts',(2.07539313195629,-1.14847798923203,3.06884426975619));
#42301=CARTESIAN_POINT('Ctrl Pts',(2.09096418385581,-1.11987809472681,3.07106680985079));
#42302=CARTESIAN_POINT('Ctrl Pts',(2.16091639211851,-0.984846422819331,
3.08154083021186));
#42303=CARTESIAN_POINT('Ctrl Pts',(2.20778402647267,-0.874736764386953,
3.09003859613071));
#42304=CARTESIAN_POINT('Ctrl Pts',(2.29898296873842,-0.605760685433158,
3.11058309603114));
#42305=CARTESIAN_POINT('Ctrl Pts',(2.33545821977983,-0.444866603385176,
3.12272155662123));
#42306=CARTESIAN_POINT('Ctrl Pts',(2.35867617574538,-0.250621661283876,
3.13650514429128));
#42307=CARTESIAN_POINT('Ctrl Pts',(2.36175877074828,-0.219682150610599,
3.13867354568708));
#42308=CARTESIAN_POINT('Ctrl Pts',(2.36538067359745,-0.17430056120115,3.14180641172339));
#42309=CARTESIAN_POINT('Ctrl Pts',(2.36639769489325,-0.159901195871341,
3.14279343932768));
#42310=CARTESIAN_POINT('Ctrl Pts',(2.36798079961768,-0.134142861683774,
3.144545510243));
#42311=CARTESIAN_POINT('Ctrl Pts',(2.36859673361779,-0.122788035389571,
3.14531306499731));
#42312=CARTESIAN_POINT('Ctrl Pts',(2.36981314247163,-0.0969254128201573,
3.14705052339805));
#42313=CARTESIAN_POINT('Ctrl Pts',(2.37036210334426,-0.0824159646999778,
3.14801769161402));
#42314=CARTESIAN_POINT('Ctrl Pts',(2.37168150301097,-0.0363494837505168,
3.15106691468105));
#42315=CARTESIAN_POINT('Ctrl Pts',(2.37195527154187,-0.00478033147960674,
3.15312458579082));
#42316=CARTESIAN_POINT('Ctrl Pts',(2.36993836421144,0.173790001941277,3.16463012809853));
#42317=CARTESIAN_POINT('Ctrl Pts',(2.35461347417735,0.320336493127514,3.17357490168829));
#42318=CARTESIAN_POINT('Ctrl Pts',(2.3080747450888,0.553345658031935,3.18820349770689));
#42319=CARTESIAN_POINT('Ctrl Pts',(2.2852645916663,0.64106525268589,3.19380458947351));
#42320=CARTESIAN_POINT('Ctrl Pts',(2.24475830558875,0.766801052793803,3.20215724048862));
#42321=CARTESIAN_POINT('Ctrl Pts',(2.23098440894213,0.80599750929483,3.20480803646782));
#42322=CARTESIAN_POINT('Ctrl Pts',(2.20386793164277,0.87713208433436,3.20972197587692));
#42323=CARTESIAN_POINT('Ctrl Pts',(2.19084188433596,0.909178858723863,3.21197515521205));
#42324=CARTESIAN_POINT('Ctrl Pts',(2.16849826684493,0.960877540818893,3.21568121938285));
#42325=CARTESIAN_POINT('Ctrl Pts',(2.15960277024621,0.980706992374399,3.21712010860713));
#42326=CARTESIAN_POINT('Ctrl Pts',(2.14177249127744,1.01903412338137,3.2199367738348));
#42327=CARTESIAN_POINT('Ctrl Pts',(2.13286739554234,1.037543530314,3.22131344970243));
#42328=CARTESIAN_POINT('Ctrl Pts',(2.11112929013862,1.08126378144751,3.22460568461241));
#42329=CARTESIAN_POINT('Ctrl Pts',(2.09808367154296,1.10636478359268,3.2265283514266));
#42330=CARTESIAN_POINT('Ctrl Pts',(2.0519911694297,1.19130283357977,3.23314936028095));
#42331=CARTESIAN_POINT('Ctrl Pts',(2.01681078386904,1.24993716329735,3.23791962013976));
#42332=CARTESIAN_POINT('Ctrl Pts',(1.88089501049086,1.45575565166071,3.25540155615017));
#42333=CARTESIAN_POINT('Ctrl Pts',(1.76617746856635,1.59298341511564,3.2685397477923));
#42334=CARTESIAN_POINT('Ctrl Pts',(1.58817033892526,1.76281122453687,3.28627500219807));
#42335=CARTESIAN_POINT('Ctrl Pts',(1.5371629890109,1.80746232737251,3.29110251065013));
#42336=CARTESIAN_POINT('Ctrl Pts',(1.46958442724663,1.86168635502307,3.29711676999495));
#42337=CARTESIAN_POINT('Ctrl Pts',(1.45471855140829,1.87332550954975,3.29841736731983));
#42338=CARTESIAN_POINT('Ctrl Pts',(1.43018551950645,1.89206533487532,3.30052532236282));
#42339=CARTESIAN_POINT('Ctrl Pts',(1.42060093914961,1.89927218764784,3.30133946905811));
#42340=CARTESIAN_POINT('Ctrl Pts',(1.40231491803986,1.91280596438696,3.30287439882048));
#42341=CARTESIAN_POINT('Ctrl Pts',(1.39362440054565,1.9191469011636,3.3035961662468));
#42342=CARTESIAN_POINT('Ctrl Pts',(1.36977934916997,1.93629777980115,3.30555649570193));
#42343=CARTESIAN_POINT('Ctrl Pts',(1.35453986316615,1.94698905208411,3.30678746743322));
#42344=CARTESIAN_POINT('Ctrl Pts',(1.29027885036009,1.99095164023283,3.31189455206704));
#42345=CARTESIAN_POINT('Ctrl Pts',(1.24014164315954,2.02256220131441,3.3156785327761));
#42346=CARTESIAN_POINT('Ctrl Pts',(0.997432216105636,2.16316286972624,3.33332581258172));
#42347=CARTESIAN_POINT('Ctrl Pts',(0.791423528607317,2.24673135908165,3.34648101948516));
#42348=CARTESIAN_POINT('Ctrl Pts',(0.53181706790111,2.31182183270309,3.36357114111945));
#42349=CARTESIAN_POINT('Ctrl Pts',(0.486506539856596,2.3217796027777,3.36656673318472));
#42350=CARTESIAN_POINT('Ctrl Pts',(0.417288587778491,2.33487633254923,3.37117844049166));
#42351=CARTESIAN_POINT('Ctrl Pts',(0.393575761727071,2.33899023181909,3.37276453461936));
#42352=CARTESIAN_POINT('Ctrl Pts',(0.349933726448231,2.34587918726324,3.37569706552008));
#42353=CARTESIAN_POINT('Ctrl Pts',(0.330023752625998,2.34876287757548,3.37704000932117));
#42354=CARTESIAN_POINT('Ctrl Pts',(0.286046573754407,2.35456218235334,3.38001864168513));
#42355=CARTESIAN_POINT('Ctrl Pts',(0.261966754130693,2.35736273377595,3.38165771728396));
#42356=CARTESIAN_POINT('Ctrl Pts',(0.192236835076011,2.36439097124383,3.38642941922871));
#42357=CARTESIAN_POINT('Ctrl Pts',(0.146503854923845,2.36766462933651,3.3895904387194));
#42358=CARTESIAN_POINT('Ctrl Pts',(-0.0754299931378458,2.37709670728848,
3.40509044877301));
#42359=CARTESIAN_POINT('Ctrl Pts',(-0.251831275948877,2.36491896207247,
3.41795608159483));
#42360=CARTESIAN_POINT('Ctrl Pts',(-0.492245535190987,2.32110616074103,
3.43571979797412));
#42361=CARTESIAN_POINT('Ctrl Pts',(-0.558716006568461,2.30600887242064,
3.44064841396094));
#42362=CARTESIAN_POINT('Ctrl Pts',(-0.652074495569949,2.28052998600842,
3.44752621947062));
#42363=CARTESIAN_POINT('Ctrl Pts',(-0.679563995253629,2.27249006373039,
3.44954564714763));
#42364=CARTESIAN_POINT('Ctrl Pts',(-0.728304607186525,2.25727117947073,
3.45310841482403));
#42365=CARTESIAN_POINT('Ctrl Pts',(-0.749612012442071,2.25028502605011,
3.45465974966162));
#42366=CARTESIAN_POINT('Ctrl Pts',(-0.782870253818592,2.23885565369224,
3.45706813988182));
#42367=CARTESIAN_POINT('Ctrl Pts',(-0.794889216424853,2.234616661659,3.45793578829303));
#42368=CARTESIAN_POINT('Ctrl Pts',(-0.8177333154705,2.22635209533754,3.45957896815401));
#42369=CARTESIAN_POINT('Ctrl Pts',(-0.828564054573966,2.2223440419134,3.4603553781085));
#42370=CARTESIAN_POINT('Ctrl Pts',(-0.852838866431851,2.21315870650631,
3.46209037358421));
#42371=CARTESIAN_POINT('Ctrl Pts',(-0.866266127783814,2.20793763796001,
3.46304650259064));
#42372=CARTESIAN_POINT('Ctrl Pts',(-0.914165292375105,2.18880825164705,
3.46644736992822));
#42373=CARTESIAN_POINT('Ctrl Pts',(-0.948358536649344,2.17421162209463,
3.46885658300752));
#42374=CARTESIAN_POINT('Ctrl Pts',(-1.11062211103469,2.10038656899485,3.48026465218472));
#42375=CARTESIAN_POINT('Ctrl Pts',(-1.23358925492092,2.03060829229769,3.48884781043404));
#42376=CARTESIAN_POINT('Ctrl Pts',(-1.42234393182489,1.89998807652394,3.50298517135967));
#42377=CARTESIAN_POINT('Ctrl Pts',(-1.49218149884534,1.84564618450459,3.50845926883154));
#42378=CARTESIAN_POINT('Ctrl Pts',(-1.60343430999369,1.74862825668671,3.51779831633965));
#42379=CARTESIAN_POINT('Ctrl Pts',(-1.64657454617898,1.70806726050829,3.52159300242642));
#42380=CARTESIAN_POINT('Ctrl Pts',(-1.70660287183484,1.647238555026,3.52716698980351));
#42381=CARTESIAN_POINT('Ctrl Pts',(-1.7247431566068,1.62823498745683,3.5288928961914));
#42382=CARTESIAN_POINT('Ctrl Pts',(-1.7563047318699,1.59405208917849,3.53197315804465));
#42383=CARTESIAN_POINT('Ctrl Pts',(-1.76985439745985,1.57899453563827,3.53332199436456));
#42384=CARTESIAN_POINT('Ctrl Pts',(-1.79810614875913,1.5467782106517,3.53619229919335));
#42385=CARTESIAN_POINT('Ctrl Pts',(-1.81275914635655,1.52957927959192,3.53771556894155));
#42386=CARTESIAN_POINT('Ctrl Pts',(-1.85192700685686,1.48225265582605,3.54188439343084));
#42387=CARTESIAN_POINT('Ctrl Pts',(-1.87595019515784,1.45172901697744,3.54454873509709));
#42388=CARTESIAN_POINT('Ctrl Pts',(-2.01046652038272,1.27189691712276,3.5601162516265));
#42389=CARTESIAN_POINT('Ctrl Pts',(-2.10384784974602,1.11062998564555,3.57364648591392));
#42390=CARTESIAN_POINT('Ctrl Pts',(-2.2053649595544,0.875512551861624,3.59227050289971));
#42391=CARTESIAN_POINT('Ctrl Pts',(-2.23038737330346,0.809648116073871,
3.59736950337685));
#42392=CARTESIAN_POINT('Ctrl Pts',(-2.26570522777612,0.702546289675075,
3.60538969190063));
#42393=CARTESIAN_POINT('Ctrl Pts',(-2.27788901986706,0.661977028589482,
3.6083670451995));
#42394=CARTESIAN_POINT('Ctrl Pts',(-2.29322443061286,0.605460481594743,
3.6124125733104));
#42395=CARTESIAN_POINT('Ctrl Pts',(-2.29730800040423,0.589776797882458,
3.6135244791844));
#42396=CARTESIAN_POINT('Ctrl Pts',(-2.30401647472113,0.562884203400059,
3.61541130790141));
#42397=CARTESIAN_POINT('Ctrl Pts',(-2.3067210592276,0.551696039161641,3.61619044235533));
#42398=CARTESIAN_POINT('Ctrl Pts',(-2.31235796835592,0.527611203434994,
3.61785478453473));
#42399=CARTESIAN_POINT('Ctrl Pts',(-2.31526402920089,0.514709093841059,
3.61873858398443));
#42400=CARTESIAN_POINT('Ctrl Pts',(-2.32315097230029,0.478274171339033,
3.62121423802244));
#42401=CARTESIAN_POINT('Ctrl Pts',(-2.32788215867647,0.454688227809483,
3.62279323670354));
#42402=CARTESIAN_POINT('Ctrl Pts',(-2.34804842952469,0.345571689858489,
3.63000670355621));
#42403=CARTESIAN_POINT('Ctrl Pts',(-2.35912700921337,0.25934211993323,3.63545031325973));
#42404=CARTESIAN_POINT('Ctrl Pts',(-2.3654513605298,0.172736572467239,3.64082947459234));
#42405=CARTESIAN_POINT('Origin',(0.,0.,-1.84858989190501));
#42406=CARTESIAN_POINT('',(-2.36545132791903,0.1727370190379,4.83597583405742));
#42407=CARTESIAN_POINT('',(-2.36545134967025,0.172736721177577,4.63766477577655));
#42408=CARTESIAN_POINT('',(-2.36545134966535,0.172736721244682,-1.84858989190501));
#42409=CARTESIAN_POINT('Ctrl Pts',(-2.36545132791902,0.172737019038084,
4.83597583405741));
#42410=CARTESIAN_POINT('Ctrl Pts',(-2.35533920084846,0.311211936229127,
4.8273804069956));
#42411=CARTESIAN_POINT('Ctrl Pts',(-2.33307831419588,0.448655167420158,
4.81894726446124));
#42412=CARTESIAN_POINT('Ctrl Pts',(-2.27985950504,0.658333687173865,4.80540068318638));
#42413=CARTESIAN_POINT('Ctrl Pts',(-2.25721668224938,0.732211515671099,
4.80049355440317));
#42414=CARTESIAN_POINT('Ctrl Pts',(-2.22143223906243,0.831404766665299,
4.79363876603281));
#42415=CARTESIAN_POINT('Ctrl Pts',(-2.2113788978478,0.857786884880636,4.7917893762288));
#42416=CARTESIAN_POINT('Ctrl Pts',(-2.19338316387111,0.902590994150976,
4.78860002368318));
#42417=CARTESIAN_POINT('Ctrl Pts',(-2.18567344329208,0.921103557966245,
4.78726779366037));
#42418=CARTESIAN_POINT('Ctrl Pts',(-2.17046577729332,0.956353839490573,
4.78470222692556));
#42419=CARTESIAN_POINT('Ctrl Pts',(-2.16300659469204,0.973106775224658,
4.78347026205697));
#42420=CARTESIAN_POINT('Ctrl Pts',(-2.14284622428484,1.01700857704299,4.78020743663232));
#42421=CARTESIAN_POINT('Ctrl Pts',(-2.12982371695856,1.0440053550073,4.7781658990363));
#42422=CARTESIAN_POINT('Ctrl Pts',(-2.07650950324224,1.14937900582047,4.77005409527662));
#42423=CARTESIAN_POINT('Ctrl Pts',(-2.0323785694822,1.22572344466343,4.76385604898489));
#42424=CARTESIAN_POINT('Ctrl Pts',(-1.87704633839646,1.46290141534091,4.7435641143981));
#42425=CARTESIAN_POINT('Ctrl Pts',(-1.75020241730722,1.61250399735342,4.72905819340805));
#42426=CARTESIAN_POINT('Ctrl Pts',(-1.58044458899366,1.7687969978942,4.71273499996434));
#42427=CARTESIAN_POINT('Ctrl Pts',(-1.55390201327748,1.79215980434077,4.71026089624965));
#42428=CARTESIAN_POINT('Ctrl Pts',(-1.51544854352607,1.82450968491369,4.70679695876194));
#42429=CARTESIAN_POINT('Ctrl Pts',(-1.50396125123935,1.83399031123718,4.70577692342823));
#42430=CARTESIAN_POINT('Ctrl Pts',(-1.48378540523275,1.85032466360741,4.70401200215828));
#42431=CARTESIAN_POINT('Ctrl Pts',(-1.47513706944861,1.85722673188737,4.70326389326465));
#42432=CARTESIAN_POINT('Ctrl Pts',(-1.45602765726471,1.87225987622076,4.70162943429373));
#42433=CARTESIAN_POINT('Ctrl Pts',(-1.44554636281364,1.88036414457384,4.70074486556295));
#42434=CARTESIAN_POINT('Ctrl Pts',(-1.41487396139246,1.90367238089014,4.69818888484657));
#42435=CARTESIAN_POINT('Ctrl Pts',(-1.39450639890883,1.91864245907507,4.69653217935403));
#42436=CARTESIAN_POINT('Ctrl Pts',(-1.28574126179139,1.99593717064376,4.68787413960963));
#42437=CARTESIAN_POINT('Ctrl Pts',(-1.19338763413892,2.05249283079977,4.68116688604259));
#42438=CARTESIAN_POINT('Ctrl Pts',(-0.987908459136713,2.15974857313577,
4.66688780324374));
#42439=CARTESIAN_POINT('Ctrl Pts',(-0.874031061820946,2.20829012649557,
4.65934588701707));
#42440=CARTESIAN_POINT('Ctrl Pts',(-0.688842117005726,2.27064978358214,
4.64707531866328));
#42441=CARTESIAN_POINT('Ctrl Pts',(-0.619792511658483,2.29046058541658,
4.6425014300596));
#42442=CARTESIAN_POINT('Ctrl Pts',(-0.523134082372167,2.31350146799972,
4.63603644830036));
#42443=CARTESIAN_POINT('Ctrl Pts',(-0.496204472435919,2.3194265088973,4.63422891156447));
#42444=CARTESIAN_POINT('Ctrl Pts',(-0.449631193469407,2.32882535060369,
4.63108880958931));
#42445=CARTESIAN_POINT('Ctrl Pts',(-0.430035363246038,2.33252336958963,
4.62976335760313));
#42446=CARTESIAN_POINT('Ctrl Pts',(-0.392195173266823,2.33917132610175,
4.62719465345623));
#42447=CARTESIAN_POINT('Ctrl Pts',(-0.373958330635711,2.34215598988121,
4.625952586358));
#42448=CARTESIAN_POINT('Ctrl Pts',(-0.325256456820483,2.34954330502224,
4.62262381879196));
#42449=CARTESIAN_POINT('Ctrl Pts',(-0.294738318932124,2.35356637394792,
4.62052560741231));
#42450=CARTESIAN_POINT('Ctrl Pts',(-0.169110742250879,2.36764563601103,
4.61183388790019));
#42451=CARTESIAN_POINT('Ctrl Pts',(-0.0735242936022879,2.37253755618989,
4.60508789161921));
#42452=CARTESIAN_POINT('Ctrl Pts',(0.172700275231606,2.37024453528281,4.58740801448852));
#42453=CARTESIAN_POINT('Ctrl Pts',(0.322828557722016,2.35449844494837,4.57631970401873));
#42454=CARTESIAN_POINT('Ctrl Pts',(0.532515091441941,2.31206318918483,4.56092360538795));
#42455=CARTESIAN_POINT('Ctrl Pts',(0.594062722750231,2.29701968435132,4.55642056150683));
#42456=CARTESIAN_POINT('Ctrl Pts',(0.672417848373035,2.27450720298909,4.55076583973866));
#42457=CARTESIAN_POINT('Ctrl Pts',(0.689838685459744,2.26928434029901,4.54951371376772));
#42458=CARTESIAN_POINT('Ctrl Pts',(0.718279162576799,2.26039993652056,4.54747981774688));
#42459=CARTESIAN_POINT('Ctrl Pts',(0.72933475775657,2.25685703077833,4.54669175116885));
#42460=CARTESIAN_POINT('Ctrl Pts',(0.751644990510565,2.24952636449015,4.54510724255995));
#42461=CARTESIAN_POINT('Ctrl Pts',(0.762898028898242,2.24573499526698,4.54431101832711));
#42462=CARTESIAN_POINT('Ctrl Pts',(0.792490735548514,2.23551652214644,4.54222385876069));
#42463=CARTESIAN_POINT('Ctrl Pts',(0.810781126820546,2.2289481174238,4.54094068189317));
#42464=CARTESIAN_POINT('Ctrl Pts',(0.898018622680762,2.19640360596706,4.53484400803493));
#42465=CARTESIAN_POINT('Ctrl Pts',(0.965817447190775,2.1674466648487,4.53017623245889));
#42466=CARTESIAN_POINT('Ctrl Pts',(1.17405132807904,2.06679394261757,4.51574101130685));
#42467=CARTESIAN_POINT('Ctrl Pts',(1.30875037884268,1.98424003605602,4.50623148452605));
#42468=CARTESIAN_POINT('Ctrl Pts',(1.49850413438474,1.84015992845678,4.49133614751729));
#42469=CARTESIAN_POINT('Ctrl Pts',(1.56020438685097,1.78814527301783,4.48621940281624));
#42470=CARTESIAN_POINT('Ctrl Pts',(1.64004348709731,1.71355607329565,4.47912052725525));
#42471=CARTESIAN_POINT('Ctrl Pts',(1.6605992909546,1.69364309622624,4.47724658632478));
#42472=CARTESIAN_POINT('Ctrl Pts',(1.69498587280874,1.65910392819048,4.47402814862422));
#42473=CARTESIAN_POINT('Ctrl Pts',(1.70900025333188,1.64466441750671,4.47269175326272));
#42474=CARTESIAN_POINT('Ctrl Pts',(1.73705485203183,1.61501298909412,4.46996456822377));
#42475=CARTESIAN_POINT('Ctrl Pts',(1.75108300152111,1.59979210824652,4.46857343866579));
#42476=CARTESIAN_POINT('Ctrl Pts',(1.78604606314704,1.56084547885679,4.46503465736285));
#42477=CARTESIAN_POINT('Ctrl Pts',(1.80670818861305,1.53688142195913,4.46287617509905));
#42478=CARTESIAN_POINT('Ctrl Pts',(1.89565350540297,1.42944904939384,4.45327699969444));
#42479=CARTESIAN_POINT('Ctrl Pts',(1.95866883423737,1.34180385285562,4.44563829551699));
#42480=CARTESIAN_POINT('Ctrl Pts',(2.07621621608734,1.15229906065967,4.42955787068833));
#42481=CARTESIAN_POINT('Ctrl Pts',(2.12972211315881,1.05011868691001,4.42111709254652));
#42482=CARTESIAN_POINT('Ctrl Pts',(2.19777178096194,0.893364491764287,4.40873801253511));
#42483=CARTESIAN_POINT('Ctrl Pts',(2.21814788009371,0.841499620128731,4.40473098883347));
#42484=CARTESIAN_POINT('Ctrl Pts',(2.24868922244876,0.754916048377608,4.39823211089958));
#42485=CARTESIAN_POINT('Ctrl Pts',(2.25992058240464,0.720597496013535,4.39570423142441));
#42486=CARTESIAN_POINT('Ctrl Pts',(2.2747068023682,0.671663885094339,4.39217958096344));
#42487=CARTESIAN_POINT('Ctrl Pts',(2.27891256197112,0.657252596288559,4.39115122434867));
#42488=CARTESIAN_POINT('Ctrl Pts',(2.28595658141371,0.632234989374813,4.38938386532933));
#42489=CARTESIAN_POINT('Ctrl Pts',(2.28885846343327,0.621647429222014,4.38864145456694));
#42490=CARTESIAN_POINT('Ctrl Pts',(2.29506794827501,0.598358924379397,4.38702078795241));
#42491=CARTESIAN_POINT('Ctrl Pts',(2.29834378645797,0.585650193141942,4.38614426885179));
#42492=CARTESIAN_POINT('Ctrl Pts',(2.30747533593123,0.548966905690562,4.38363517920957));
#42493=CARTESIAN_POINT('Ctrl Pts',(2.31306276024204,0.524926538515636,4.3820165102701));
#42494=CARTESIAN_POINT('Ctrl Pts',(2.35419977880891,0.334498297046135,4.36936506194432));
#42495=CARTESIAN_POINT('Ctrl Pts',(2.37213092636178,0.164789843839533,4.35908533922349));
#42496=CARTESIAN_POINT('Ctrl Pts',(2.37155429665257,-0.0887445981140952,
4.34345590425478));
#42497=CARTESIAN_POINT('Ctrl Pts',(2.36697110684533,-0.172022624026459,
4.33828342413938));
#42498=CARTESIAN_POINT('Ctrl Pts',(2.35192072355321,-0.311259544608725,
4.32940923804492));
#42499=CARTESIAN_POINT('Ctrl Pts',(2.34380731883432,-0.367396344244507,
4.32576943930545));
#42500=CARTESIAN_POINT('Ctrl Pts',(2.32915663570164,-0.448188751199906,
4.32041049142159));
#42501=CARTESIAN_POINT('Ctrl Pts',(2.32422119253587,-0.473116854293194,
4.318740296194));
#42502=CARTESIAN_POINT('Ctrl Pts',(2.31476429381294,-0.517155470210715,
4.31575752318676));
#42503=CARTESIAN_POINT('Ctrl Pts',(2.31040417986393,-0.536298427363922,
4.31445009146337));
#42504=CARTESIAN_POINT('Ctrl Pts',(2.30067656473446,-0.576684862531626,
4.31166765705939));
#42505=CARTESIAN_POINT('Ctrl Pts',(2.29525135705422,-0.597912401069293,
4.31019094430137));
#42506=CARTESIAN_POINT('Ctrl Pts',(2.27972045298151,-0.655351828128441,
4.30615490243695));
#42507=CARTESIAN_POINT('Ctrl Pts',(2.26904695497142,-0.691402201519372,
4.30357793279273));
#42508=CARTESIAN_POINT('Ctrl Pts',(2.20757027202545,-0.882255310364198,
4.28969246087521));
#42509=CARTESIAN_POINT('Ctrl Pts',(2.14178112470122,-1.03174520612798,4.27791140636574));
#42510=CARTESIAN_POINT('Ctrl Pts',(1.99778278893594,-1.28471841436772,4.25670762396453));
#42511=CARTESIAN_POINT('Ctrl Pts',(1.92541768269389,-1.39083082973557,4.24736377186084));
#42512=CARTESIAN_POINT('Ctrl Pts',(1.83171394136996,-1.50680361095169,4.23697994213884));
#42513=CARTESIAN_POINT('Ctrl Pts',(1.81839177303455,-1.52285406975997,4.23553899634747));
#42514=CARTESIAN_POINT('Ctrl Pts',(1.79695756363907,-1.54799544836842,4.23327848894684));
#42515=CARTESIAN_POINT('Ctrl Pts',(1.78898458279312,-1.55720280392728,4.2324498967008));
#42516=CARTESIAN_POINT('Ctrl Pts',(1.77350168266863,-1.57480688581067,4.23086490331018));
#42517=CARTESIAN_POINT('Ctrl Pts',(1.76600233757626,-1.58321214486592,4.23010785608293));
#42518=CARTESIAN_POINT('Ctrl Pts',(1.74702887345391,-1.60417502458731,4.22821818908068));
#42519=CARTESIAN_POINT('Ctrl Pts',(1.73547873112509,-1.61666354223325,4.22709096759598));
#42520=CARTESIAN_POINT('Ctrl Pts',(1.69132911642183,-1.6633815342127,4.22286363577812));
#42521=CARTESIAN_POINT('Ctrl Pts',(1.65784118379842,-1.6967603208233,4.21982150740373));
#42522=CARTESIAN_POINT('Ctrl Pts',(1.52626679361792,-1.82028839641133,4.20837166987277));
#42523=CARTESIAN_POINT('Ctrl Pts',(1.42164366637919,-1.90312231413506,4.20027205452098));
#42524=CARTESIAN_POINT('Ctrl Pts',(1.23891701230126,-2.02427333805394,4.18676585288513));
#42525=CARTESIAN_POINT('Ctrl Pts',(1.16469226662965,-2.06787049484582,4.18143464743203));
#42526=CARTESIAN_POINT('Ctrl Pts',(1.03683565587186,-2.13389797640278,4.17232357454245));
#42527=CARTESIAN_POINT('Ctrl Pts',(0.984452202697774,-2.15856475342659,
4.16861043597579));
#42528=CARTESIAN_POINT('Ctrl Pts',(0.907678919324832,-2.19134030582006,
4.16316385752261));
#42529=CARTESIAN_POINT('Ctrl Pts',(0.883975480973467,-2.20100900114747,
4.16148174551434));
#42530=CARTESIAN_POINT('Ctrl Pts',(0.841804104769304,-2.21741972206334,
4.15848567289322));
#42531=CARTESIAN_POINT('Ctrl Pts',(0.823399875402378,-2.22431944219372,
4.15717702602271));
#42532=CARTESIAN_POINT('Ctrl Pts',(0.784397135021651,-2.2383911322332,4.15440029709406));
#42533=CARTESIAN_POINT('Ctrl Pts',(0.763781285710771,-2.24550925624015,
4.15293060548619));
#42534=CARTESIAN_POINT('Ctrl Pts',(0.707835563669785,-2.26396632606916,
4.14893552860718));
#42535=CARTESIAN_POINT('Ctrl Pts',(0.672334227341257,-2.27476177515535,
4.14639311095681));
#42536=CARTESIAN_POINT('Ctrl Pts',(0.445171119375501,-2.33805667972721,
4.13007036386436));
#42537=CARTESIAN_POINT('Ctrl Pts',(0.247829089144496,-2.36711624780666,
4.11554939457764));
#42538=CARTESIAN_POINT('Ctrl Pts',(-0.0152522898383138,-2.37257761960759,
4.09643317317025));
#42539=CARTESIAN_POINT('Ctrl Pts',(-0.0797612949147726,-2.37128578429372,
4.09177428400151));
#42540=CARTESIAN_POINT('Ctrl Pts',(-0.183878533504297,-2.36494644698234,
4.08436904923799));
#42541=CARTESIAN_POINT('Ctrl Pts',(-0.223551933365702,-2.36152661972962,
4.08157448848722));
#42542=CARTESIAN_POINT('Ctrl Pts',(-0.278594222621748,-2.3553822754953,
4.07775127244517));
#42543=CARTESIAN_POINT('Ctrl Pts',(-0.29404860883251,-2.35350288984531,
4.07668376842345));
#42544=CARTESIAN_POINT('Ctrl Pts',(-0.320529943956432,-2.35001760561564,
4.07486605537547));
#42545=CARTESIAN_POINT('Ctrl Pts',(-0.33156588213832,-2.3484859543524,4.07411200027414));
#42546=CARTESIAN_POINT('Ctrl Pts',(-0.355295073656612,-2.34502202524333,
4.07249843400206));
#42547=CARTESIAN_POINT('Ctrl Pts',(-0.367983973486608,-2.34306438286093,
4.07164028153028));
#42548=CARTESIAN_POINT('Ctrl Pts',(-0.403695745629255,-2.33725750377567,
4.06923671243015));
#42549=CARTESIAN_POINT('Ctrl Pts',(-0.426679263027888,-2.33317118925555,
4.06770346356701));
#42550=CARTESIAN_POINT('Ctrl Pts',(-0.596691244203305,-2.30034779928361,
4.05643827957072));
#42551=CARTESIAN_POINT('Ctrl Pts',(-0.740780913110152,-2.25807344158744,
4.04730166392353));
#42552=CARTESIAN_POINT('Ctrl Pts',(-0.970491859088624,-2.16629950108058,
4.03209070553291));
#42553=CARTESIAN_POINT('Ctrl Pts',(-1.0587290796595,-2.12457031573233,4.02607907387049));
#42554=CARTESIAN_POINT('Ctrl Pts',(-1.19902827893452,-2.04730439715628,
4.01596856749238));
#42555=CARTESIAN_POINT('Ctrl Pts',(-1.25269025191291,-2.0149169286898,4.01195928824721));
#42556=CARTESIAN_POINT('Ctrl Pts',(-1.32698508103623,-1.96596073772651,
4.00616029355871));
#42557=CARTESIAN_POINT('Ctrl Pts',(-1.34872277788352,-1.95111194110456,
4.00443207728883));
#42558=CARTESIAN_POINT('Ctrl Pts',(-1.38632837230736,-1.92449519335386,
4.0013838282368));
#42559=CARTESIAN_POINT('Ctrl Pts',(-1.40230503574717,-1.91288490308539,
4.00006976231903));
#42560=CARTESIAN_POINT('Ctrl Pts',(-1.43534069669859,-1.88824149545334,
3.99731147140708));
#42561=CARTESIAN_POINT('Ctrl Pts',(-1.45237139751333,-1.87517362741355,
3.99586599532996));
#42562=CARTESIAN_POINT('Ctrl Pts',(-1.49702739805236,-1.83993521839389,
3.99201155288803));
#42563=CARTESIAN_POINT('Ctrl Pts',(-1.52433652561458,-1.81737463531964,
3.98958757527384));
#42564=CARTESIAN_POINT('Ctrl Pts',(-1.70746246487127,-1.65905891767343,
3.97285967033546));
#42565=CARTESIAN_POINT('Ctrl Pts',(-1.84543803044489,-1.50407164627297,
3.9577383814089));
#42566=CARTESIAN_POINT('Ctrl Pts',(-1.99608799350086,-1.28242091397494,
3.93828569461351));
#42567=CARTESIAN_POINT('Ctrl Pts',(-2.02863031900023,-1.23029694342907,
3.93385475699824));
#42568=CARTESIAN_POINT('Ctrl Pts',(-2.07824548590066,-1.14349468073653,
3.92676366373243));
#42569=CARTESIAN_POINT('Ctrl Pts',(-2.09655944375571,-1.10955994799909,
3.92405969200348));
#42570=CARTESIAN_POINT('Ctrl Pts',(-2.12101311390812,-1.06147920455946,
3.92033743725976));
#42571=CARTESIAN_POINT('Ctrl Pts',(-2.12785385098453,-1.04769878837094,
3.91928284683628));
#42572=CARTESIAN_POINT('Ctrl Pts',(-2.1394064881051,-1.02384644609176,3.91747967296125));
#42573=CARTESIAN_POINT('Ctrl Pts',(-2.14418242035695,-1.01380640878957,
3.91672741261281));
#42574=CARTESIAN_POINT('Ctrl Pts',(-2.1543642493024,-0.992008163241909,
3.91510897200189));
#42575=CARTESIAN_POINT('Ctrl Pts',(-2.15974475185589,-0.980238818137827,
3.91424425763458));
#42576=CARTESIAN_POINT('Ctrl Pts',(-2.17475319854271,-0.946685681550879,
3.9118032097439));
#42577=CARTESIAN_POINT('Ctrl Pts',(-2.18415003046844,-0.924799438856245,
3.91023964763168));
#42578=CARTESIAN_POINT('Ctrl Pts',(-2.24794313921791,-0.76981933469923,
3.89934320563914));
#42579=CARTESIAN_POINT('Ctrl Pts',(-2.29047421117901,-0.632145921168367,
3.89055388067386));
#42580=CARTESIAN_POINT('Ctrl Pts',(-2.34118487377328,-0.392728065915054,
3.87550826850697));
#42581=CARTESIAN_POINT('Ctrl Pts',(-2.35577248521001,-0.292773319784415,
3.86929636123911));
#42582=CARTESIAN_POINT('Ctrl Pts',(-2.36913414046138,-0.128431366297866,
3.85889647990566));
#42583=CARTESIAN_POINT('Ctrl Pts',(-2.37173602461579,-0.0644852799020278,
3.85480552060976));
#42584=CARTESIAN_POINT('Ctrl Pts',(-2.37175513931822,0.0233609360900335,
3.84908163765761));
#42585=CARTESIAN_POINT('Ctrl Pts',(-2.37139977101542,0.0472359383233294,
3.84751557724493));
#42586=CARTESIAN_POINT('Ctrl Pts',(-2.37008832420336,0.0909629385895274,
3.84462609560508));
#42587=CARTESIAN_POINT('Ctrl Pts',(-2.36924305174823,0.1108162556765,3.84330615667556));
#42588=CARTESIAN_POINT('Ctrl Pts',(-2.36737410016197,0.144691093524926,
3.84103935124155));
#42589=CARTESIAN_POINT('Ctrl Pts',(-2.36647502731241,0.158718511030017,
3.84009638256154));
#42590=CARTESIAN_POINT('Ctrl Pts',(-2.36545134965682,0.17273672136148,3.83914957969666));
#42591=CARTESIAN_POINT('Ctrl Pts',(-2.3654513605298,0.172736572467239,3.64082947459234));
#42592=CARTESIAN_POINT('Ctrl Pts',(-2.36959701486398,0.115966060322647,
3.64435555060821));
#42593=CARTESIAN_POINT('Ctrl Pts',(-2.37169985081302,0.0590339790747697,
3.64785365633938));
#42594=CARTESIAN_POINT('Ctrl Pts',(-2.37186929854398,-0.13697030543108,
3.65990871287198));
#42595=CARTESIAN_POINT('Ctrl Pts',(-2.3597667239314,-0.275718044079579,
3.66848094369881));
#42596=CARTESIAN_POINT('Ctrl Pts',(-2.32885929991368,-0.450674302687589,
3.67990230286747));
#42597=CARTESIAN_POINT('Ctrl Pts',(-2.3212034515273,-0.488576745812499,
3.68241265533684));
#42598=CARTESIAN_POINT('Ctrl Pts',(-2.30761936118775,-0.548269861809052,
3.68643274490679));
#42599=CARTESIAN_POINT('Ctrl Pts',(-2.30230033262587,-0.570193018636082,
3.68792352524549));
#42600=CARTESIAN_POINT('Ctrl Pts',(-2.29161130574658,-0.611658651311513,
3.69077218950729));
#42601=CARTESIAN_POINT('Ctrl Pts',(-2.28630193730051,-0.631214774057751,
3.6921280498678));
#42602=CARTESIAN_POINT('Ctrl Pts',(-2.27351712965478,-0.676026298859747,
3.6952645906173));
#42603=CARTESIAN_POINT('Ctrl Pts',(-2.2658703920914,-0.701229610653536,
3.69705056751702));
#42604=CARTESIAN_POINT('Ctrl Pts',(-2.23954823443694,-0.783055797232476,
3.70292326638485));
#42605=CARTESIAN_POINT('Ctrl Pts',(-2.21915856600873,-0.839098852087853,
3.70706342124196));
#42606=CARTESIAN_POINT('Ctrl Pts',(-2.16296380620328,-0.977129175176385,
3.71756249663213));
#42607=CARTESIAN_POINT('Ctrl Pts',(-2.12459301006574,-1.05796779322785,
3.72398967843638));
#42608=CARTESIAN_POINT('Ctrl Pts',(-2.01284523644896,-1.26266944110875,
3.7409111983272));
#42609=CARTESIAN_POINT('Ctrl Pts',(-1.93259673664931,-1.38237224467905,
3.75147964219424));
#42610=CARTESIAN_POINT('Ctrl Pts',(-1.82048765813362,-1.52058821520228,
3.76406400339948));
#42611=CARTESIAN_POINT('Ctrl Pts',(-1.79840778894284,-1.54663943383508,
3.76645336699156));
#42612=CARTESIAN_POINT('Ctrl Pts',(-1.76653256182472,-1.58264178957273,
3.76977012327999));
#42613=CARTESIAN_POINT('Ctrl Pts',(-1.75720123467197,-1.59299597301356,
3.77072577889181));
#42614=CARTESIAN_POINT('Ctrl Pts',(-1.7399655167019,-1.61178524077673,3.77246226563935));
#42615=CARTESIAN_POINT('Ctrl Pts',(-1.73208974569331,-1.62024590657604,
3.77324503365964));
#42616=CARTESIAN_POINT('Ctrl Pts',(-1.71518447059434,-1.63814249514453,
3.77490217599846));
#42617=CARTESIAN_POINT('Ctrl Pts',(-1.70613844806886,-1.64756190120004,
3.77577532647589));
#42618=CARTESIAN_POINT('Ctrl Pts',(-1.68029427497409,-1.6740316797195,3.77823340594831));
#42619=CARTESIAN_POINT('Ctrl Pts',(-1.66331468424705,-1.69090368781637,
3.77980547565187));
#42620=CARTESIAN_POINT('Ctrl Pts',(-1.62359797152988,-1.7291914337846,3.78339370949207));
#42621=CARTESIAN_POINT('Ctrl Pts',(-1.60068713051918,-1.75042117250121,
3.7853988669567));
#42622=CARTESIAN_POINT('Ctrl Pts',(-1.51847301399674,-1.82363818622084,
3.79239830905289));
#42623=CARTESIAN_POINT('Ctrl Pts',(-1.45700059481048,-1.87311701832676,
3.7972848712947));
#42624=CARTESIAN_POINT('Ctrl Pts',(-1.24941469120838,-2.02378735028783,
3.81309428183043));
#42625=CARTESIAN_POINT('Ctrl Pts',(-1.09440358357304,-2.11164076288625,
3.82390642296878));
#42626=CARTESIAN_POINT('Ctrl Pts',(-0.897525844218545,-2.19567155091186,
3.837697356745));
#42627=CARTESIAN_POINT('Ctrl Pts',(-0.863683849776956,-2.20920261249745,
3.8400676319614));
#42628=CARTESIAN_POINT('Ctrl Pts',(-0.808832466806698,-2.22968089771886,
3.84391655636787));
#42629=CARTESIAN_POINT('Ctrl Pts',(-0.788013490900771,-2.23712349882225,
3.84537902567851));
#42630=CARTESIAN_POINT('Ctrl Pts',(-0.747802481056421,-2.25086764529329,
3.84820835485844));
#42631=CARTESIAN_POINT('Ctrl Pts',(-0.728427195358609,-2.25721232600311,
3.84957367594173));
#42632=CARTESIAN_POINT('Ctrl Pts',(-0.68293297459544,-2.2714632364996,3.85278542883885));
#42633=CARTESIAN_POINT('Ctrl Pts',(-0.656755062654135,-2.27916988498903,
3.85463803161126));
#42634=CARTESIAN_POINT('Ctrl Pts',(-0.566795950278192,-2.30397492198413,
3.86102255758896));
#42635=CARTESIAN_POINT('Ctrl Pts',(-0.502441468264347,-2.3188594720347,
3.86562186567931));
#42636=CARTESIAN_POINT('Ctrl Pts',(-0.333719670755148,-2.35052991440881,
3.87776417190233));
#42637=CARTESIAN_POINT('Ctrl Pts',(-0.228706999775877,-2.36305928100741,
3.88540842552406));
#42638=CARTESIAN_POINT('Ctrl Pts',(0.00999595579355788,-2.37547725565066,
3.90280516817964));
#42639=CARTESIAN_POINT('Ctrl Pts',(0.143567155264895,-2.371157091238,3.912558114431));
#42640=CARTESIAN_POINT('Ctrl Pts',(0.30097034944349,-2.35270976067056,3.9236566697985));
#42641=CARTESIAN_POINT('Ctrl Pts',(0.325819405575156,-2.3493974131832,3.92539645250121));
#42642=CARTESIAN_POINT('Ctrl Pts',(0.363905308127659,-2.34370468220607,
3.9280394695584));
#42643=CARTESIAN_POINT('Ctrl Pts',(0.377181448267994,-2.34160476751479,
3.92895636749114));
#42644=CARTESIAN_POINT('Ctrl Pts',(0.400606678112143,-2.33769514795478,
3.93056555234368));
#42645=CARTESIAN_POINT('Ctrl Pts',(0.410762458876981,-2.33593204598352,
3.93126024206808));
#42646=CARTESIAN_POINT('Ctrl Pts',(0.435726916999368,-2.3314302236727,3.93296097130487));
#42647=CARTESIAN_POINT('Ctrl Pts',(0.450521506849136,-2.32861659253567,
3.93396294336805));
#42648=CARTESIAN_POINT('Ctrl Pts',(0.499353312476416,-2.31884694883676,
3.93725348306805));
#42649=CARTESIAN_POINT('Ctrl Pts',(0.533266098946622,-2.31128372617966,
3.93951191798685));
#42650=CARTESIAN_POINT('Ctrl Pts',(0.617749244398843,-2.29048363245666,
3.94509843053944));
#42651=CARTESIAN_POINT('Ctrl Pts',(0.66807228948704,-2.27631488643149,3.94839018079369));
#42652=CARTESIAN_POINT('Ctrl Pts',(0.810617366573668,-2.2310453514565,3.9577146334586));
#42653=CARTESIAN_POINT('Ctrl Pts',(0.901448439913645,-2.19591795516649,
3.96365956172259));
#42654=CARTESIAN_POINT('Ctrl Pts',(1.10660342129562,-2.10169661411891,3.97757063293859));
#42655=CARTESIAN_POINT('Ctrl Pts',(1.21877781753522,-2.03869441880731,3.98555890524226));
#42656=CARTESIAN_POINT('Ctrl Pts',(1.35253402169478,-1.94857095101678,3.99598943318772));
#42657=CARTESIAN_POINT('Ctrl Pts',(1.37938967441525,-1.92965307488603,3.99813236598012));
#42658=CARTESIAN_POINT('Ctrl Pts',(1.42306457500007,-1.89750955641875,4.00170440222749));
#42659=CARTESIAN_POINT('Ctrl Pts',(1.44011367101772,-1.88460284054043,4.00312145660147));
#42660=CARTESIAN_POINT('Ctrl Pts',(1.47335116914279,-1.85872659814813,4.00593052163419));
#42661=CARTESIAN_POINT('Ctrl Pts',(1.48954857365625,-1.8457717179745,4.00732188311774));
#42662=CARTESIAN_POINT('Ctrl Pts',(1.52834292922249,-1.81390030474475,4.0107104244733));
#42663=CARTESIAN_POINT('Ctrl Pts',(1.55076077025568,-1.79477222105789,4.01271584787354));
#42664=CARTESIAN_POINT('Ctrl Pts',(1.63552406159507,-1.71967385926942,4.02048669602019));
#42665=CARTESIAN_POINT('Ctrl Pts',(1.6952377698661,-1.66083812169591,4.02636636913664));
#42666=CARTESIAN_POINT('Ctrl Pts',(1.86782285883982,-1.47176747154114,4.04464388194149));
#42667=CARTESIAN_POINT('Ctrl Pts',(1.96972502139181,-1.33230558346584,4.05735306779864));
#42668=CARTESIAN_POINT('Ctrl Pts',(2.08386102263331,-1.13398657558563,4.07377303001559));
#42669=CARTESIAN_POINT('Ctrl Pts',(2.11033358798511,-1.08392597799857,4.07778723693651));
#42670=CARTESIAN_POINT('Ctrl Pts',(2.14299417604124,-1.01642101449627,4.082988333703));
#42671=CARTESIAN_POINT('Ctrl Pts',(2.15080496593952,-0.999786860782929,
4.08425336371895));
#42672=CARTESIAN_POINT('Ctrl Pts',(2.16286266366618,-0.973312871353701,
4.08623871421392));
#42673=CARTESIAN_POINT('Ctrl Pts',(2.16723739152076,-0.963532535748515,
4.0869661853375));
#42674=CARTESIAN_POINT('Ctrl Pts',(2.17638962172718,-0.942693681843332,
4.08850302284787));
#42675=CARTESIAN_POINT('Ctrl Pts',(2.18114946461862,-0.931627709978138,
4.0893112886481));
#42676=CARTESIAN_POINT('Ctrl Pts',(2.19325346078083,-0.902886289245861,
4.09139156433872));
#42677=CARTESIAN_POINT('Ctrl Pts',(2.20046851059907,-0.885156926746334,
4.09265631658826));
#42678=CARTESIAN_POINT('Ctrl Pts',(2.23352089112106,-0.801035404537531,
4.09857921752201));
#42679=CARTESIAN_POINT('Ctrl Pts',(2.25657526875353,-0.73358251957858,4.1031011108126));
#42680=CARTESIAN_POINT('Ctrl Pts',(2.33550922792691,-0.463436511503453,
4.120696639232));
#42681=CARTESIAN_POINT('Ctrl Pts',(2.36737862340621,-0.254751785075263,
4.13325968599711));
#42682=CARTESIAN_POINT('Ctrl Pts',(2.37209574148656,-0.00391372846938446,
4.14929610723635));
#42683=CARTESIAN_POINT('Ctrl Pts',(2.37181378855006,0.0367774094967678,
4.15192306620879));
#42684=CARTESIAN_POINT('Ctrl Pts',(2.36966135224321,0.102665293149738,4.15622981959101));
#42685=CARTESIAN_POINT('Ctrl Pts',(2.36843468145974,0.127875593091838,4.1578902756474));
#42686=CARTESIAN_POINT('Ctrl Pts',(2.36550499903268,0.173177798722209,4.1608991172681));
#42687=CARTESIAN_POINT('Ctrl Pts',(2.3639476408708,0.193276899115214,4.16224292907959));
#42688=CARTESIAN_POINT('Ctrl Pts',(2.36004416271809,0.236494154304883,4.1651526980586));
#42689=CARTESIAN_POINT('Ctrl Pts',(2.35761414460571,0.259602417121173,4.16672109542269));
#42690=CARTESIAN_POINT('Ctrl Pts',(2.34983258483826,0.324428294961655,4.17115792094549));
#42691=CARTESIAN_POINT('Ctrl Pts',(2.34371054418482,0.366042893678182,4.17404945855088));
#42692=CARTESIAN_POINT('Ctrl Pts',(2.32721355582752,0.460638622281026,4.18072529803128));
#42693=CARTESIAN_POINT('Ctrl Pts',(2.31612986698481,0.513471128124007,4.18452864575801));
#42694=CARTESIAN_POINT('Ctrl Pts',(2.26701627807338,0.713375339508083,4.19919668728086));
#42695=CARTESIAN_POINT('Ctrl Pts',(2.21669430461229,0.857045569807947,4.21034719239739));
#42696=CARTESIAN_POINT('Ctrl Pts',(2.11995620683581,1.06638891943087,4.22703740811421));
#42697=CARTESIAN_POINT('Ctrl Pts',(2.08337882964004,1.13619306230513,4.23267755211699));
#42698=CARTESIAN_POINT('Ctrl Pts',(2.03321412302157,1.22132729939304,4.239549184619));
#42699=CARTESIAN_POINT('Ctrl Pts',(2.02281669094517,1.23847193850463,4.24093254207919));
#42700=CARTESIAN_POINT('Ctrl Pts',(2.00572370398829,1.2658674068242,4.24313977039542));
#42701=CARTESIAN_POINT('Ctrl Pts',(1.99916426064522,1.27620145118244,4.24397161782834));
#42702=CARTESIAN_POINT('Ctrl Pts',(1.98601190431793,1.29657200142261,4.24560914605082));
#42703=CARTESIAN_POINT('Ctrl Pts',(1.97942222955367,1.30661007518579,4.24641496883988));
#42704=CARTESIAN_POINT('Ctrl Pts',(1.9622337228158,1.33236489217494,4.24848078794539));
#42705=CARTESIAN_POINT('Ctrl Pts',(1.95152193438601,1.34800578023285,4.24973371934177));
#42706=CARTESIAN_POINT('Ctrl Pts',(1.90109730646082,1.41977254243833,4.25548340941102));
#42707=CARTESIAN_POINT('Ctrl Pts',(1.8591399272787,1.47428815574891,4.2598534761862));
#42708=CARTESIAN_POINT('Ctrl Pts',(1.69490179762089,1.66950009505479,4.27582346863329));
#42709=CARTESIAN_POINT('Ctrl Pts',(1.55854950481684,1.79745652873527,4.28700229857499));
#42710=CARTESIAN_POINT('Ctrl Pts',(1.35921490686768,1.94460899715166,4.30264156805711));
#42711=CARTESIAN_POINT('Ctrl Pts',(1.30841409108551,1.97914651727392,4.30656933940486));
#42712=CARTESIAN_POINT('Ctrl Pts',(1.23541347204958,2.02473700818823,4.31217363062635));
#42713=CARTESIAN_POINT('Ctrl Pts',(1.21429166743376,2.03747443490682,4.31379056115342));
#42714=CARTESIAN_POINT('Ctrl Pts',(1.17525730393103,2.06019139944019,4.31677281205536));
#42715=CARTESIAN_POINT('Ctrl Pts',(1.15740646060623,2.07027258447125,4.31813440469737));
#42716=CARTESIAN_POINT('Ctrl Pts',(1.12066957834967,2.09039594355557,4.32093327441707));
#42717=CARTESIAN_POINT('Ctrl Pts',(1.10177393638872,2.10041654132479,4.32237114336336));
#42718=CARTESIAN_POINT('Ctrl Pts',(1.05349951526259,2.12518643361744,4.32604156483767));
#42719=CARTESIAN_POINT('Ctrl Pts',(1.02394566111259,2.13958260078573,4.32828585614312));
#42720=CARTESIAN_POINT('Ctrl Pts',(0.871218946592627,2.2100892463976,4.33987558761203));
#42721=CARTESIAN_POINT('Ctrl Pts',(0.743723233567563,2.25618754713974,4.34954459695592));
#42722=CARTESIAN_POINT('Ctrl Pts',(0.471507779731947,2.32902026419796,4.36999584339015));
#42723=CARTESIAN_POINT('Ctrl Pts',(0.326795493038871,2.35369143786506,4.38076137547229));
#42724=CARTESIAN_POINT('Ctrl Pts',(0.148683895114844,2.36730308969311,4.39335994106292));
#42725=CARTESIAN_POINT('Ctrl Pts',(0.116592428726733,2.36910051809704,4.39560334664939));
#42726=CARTESIAN_POINT('Ctrl Pts',(0.0698627596221165,2.37076590461429,
4.39882252750585));
#42727=CARTESIAN_POINT('Ctrl Pts',(0.0552479967207604,2.37115150625911,
4.39982257121407));
#42728=CARTESIAN_POINT('Ctrl Pts',(0.029259149947314,2.37159678321582,4.40158782058091));
#42729=CARTESIAN_POINT('Ctrl Pts',(0.017887022491942,2.3717098197621,4.40235571844826));
#42730=CARTESIAN_POINT('Ctrl Pts',(-0.0078245996975554,2.37178043420015,
4.4040816972023));
#42731=CARTESIAN_POINT('Ctrl Pts',(-0.0221634587373503,2.37168978977999,
4.40503722022514));
#42732=CARTESIAN_POINT('Ctrl Pts',(-0.0670490634442839,2.37099892187294,
4.40800881262807));
#42733=CARTESIAN_POINT('Ctrl Pts',(-0.0975868348555995,2.36993849707445,
4.41000221612063));
#42734=CARTESIAN_POINT('Ctrl Pts',(-0.171574392440073,2.36593661873287,
4.41478147822842));
#42735=CARTESIAN_POINT('Ctrl Pts',(-0.214981016099167,2.36238807950973,
4.41754316594666));
#42736=CARTESIAN_POINT('Ctrl Pts',(-0.410936050032594,2.34092224864457,
4.42991536637424));
#42737=CARTESIAN_POINT('Ctrl Pts',(-0.561623213991225,2.30940873238947,
4.43918979904656));
#42738=CARTESIAN_POINT('Ctrl Pts',(-0.7955124154501,2.23623026714634,4.45443597512809));
#42739=CARTESIAN_POINT('Ctrl Pts',(-0.88115282773577,2.2038903954872,4.4602079157636));
#42740=CARTESIAN_POINT('Ctrl Pts',(-0.992830350896185,2.15416659808128,
4.46813276762702));
#42741=CARTESIAN_POINT('Ctrl Pts',(-1.02070698939691,2.1410985358678,4.47014510947494));
#42742=CARTESIAN_POINT('Ctrl Pts',(-1.06526228311548,2.11914394261611,4.47342134614995));
#42743=CARTESIAN_POINT('Ctrl Pts',(-1.08210344060334,2.11059396643435,4.47467380449814));
#42744=CARTESIAN_POINT('Ctrl Pts',(-1.11720042389382,2.09224532585545,4.47731467890076));
#42745=CARTESIAN_POINT('Ctrl Pts',(-1.1354334832107,2.08240679262041,4.4787043850232));
#42746=CARTESIAN_POINT('Ctrl Pts',(-1.17917009098673,2.05806140440532,4.48208236233983));
#42747=CARTESIAN_POINT('Ctrl Pts',(-1.20453733373699,2.04331801938028,4.48407875137095));
#42748=CARTESIAN_POINT('Ctrl Pts',(-1.30023322007292,1.98529847663583,4.49175671920609));
#42749=CARTESIAN_POINT('Ctrl Pts',(-1.3685512687438,1.93883501837791,4.49754897289493));
#42750=CARTESIAN_POINT('Ctrl Pts',(-1.56631458050422,1.78866776506741,4.51526812946975));
#42751=CARTESIAN_POINT('Ctrl Pts',(-1.68745208630786,1.67486488031832,4.52748100502024));
#42752=CARTESIAN_POINT('Ctrl Pts',(-1.83706803298036,1.50146089929052,4.54396672173134));
#42753=CARTESIAN_POINT('Ctrl Pts',(-1.87648278969722,1.45190135212583,4.54846951132244));
#42754=CARTESIAN_POINT('Ctrl Pts',(-1.92509118871346,1.38549012627206,4.55418333457826));
#42755=CARTESIAN_POINT('Ctrl Pts',(-1.93612759149335,1.37002517515135,4.55549233038461));
#42756=CARTESIAN_POINT('Ctrl Pts',(-1.95316152532907,1.34553906940437,4.55752928321059));
#42757=CARTESIAN_POINT('Ctrl Pts',(-1.95928485152688,1.33660697792828,4.55826501792636));
#42758=CARTESIAN_POINT('Ctrl Pts',(-1.97201511605928,1.31776187120408,4.55980148729828));
#42759=CARTESIAN_POINT('Ctrl Pts',(-1.97860894145919,1.30784044660455,4.56060128907068));
#42760=CARTESIAN_POINT('Ctrl Pts',(-1.99524735136364,1.28239153280117,4.56263081248285));
#42761=CARTESIAN_POINT('Ctrl Pts',(-2.00518585492076,1.26679508018082,4.56385394851374));
#42762=CARTESIAN_POINT('Ctrl Pts',(-2.04820232339298,1.19751460011362,4.56920416851125));
#42763=CARTESIAN_POINT('Ctrl Pts',(-2.07931696096085,1.14263571858385,4.57322518079343));
#42764=CARTESIAN_POINT('Ctrl Pts',(-2.17164580349763,0.963496528046234,
4.58588154134459));
#42765=CARTESIAN_POINT('Ctrl Pts',(-2.22418404544549,0.835092703635923,
4.5942739590145));
#42766=CARTESIAN_POINT('Ctrl Pts',(-2.29653487403135,0.601907278282683,
4.60939282451259));
#42767=CARTESIAN_POINT('Ctrl Pts',(-2.3210662687693,0.499011514499828,4.61602278866778));
#42768=CARTESIAN_POINT('Ctrl Pts',(-2.34394193075249,0.363514674476526,
4.62492060515917));
#42769=CARTESIAN_POINT('Ctrl Pts',(-2.34859916807399,0.332097107268569,
4.62699459821716));
#42770=CARTESIAN_POINT('Ctrl Pts',(-2.35503908188814,0.281695028335984,
4.63034390390299));
#42771=CARTESIAN_POINT('Ctrl Pts',(-2.35722621796972,0.26276546315654,4.63160674528801));
#42772=CARTESIAN_POINT('Ctrl Pts',(-2.36116115002608,0.224690098143811,
4.63415777395436));
#42773=CARTESIAN_POINT('Ctrl Pts',(-2.36290471661995,0.205545323697977,
4.63544598974069));
#42774=CARTESIAN_POINT('Ctrl Pts',(-2.36477379335609,0.181834475928732,
4.63704878560607));
#42775=CARTESIAN_POINT('Ctrl Pts',(-2.36511913544288,0.177286052594564,
4.63735658114384));
#42776=CARTESIAN_POINT('Ctrl Pts',(-2.36545134967025,0.172736721177577,
4.63766477577655));
#42777=CARTESIAN_POINT('Origin',(0.,0.,-1.84858989190501));
#42778=CARTESIAN_POINT('',(-2.36545133284689,0.172736951556046,5.836583843094));
#42779=CARTESIAN_POINT('',(-2.36545134983051,0.172736718982988,5.64123248379855));
#42780=CARTESIAN_POINT('',(-2.36545134966535,0.172736721244682,-1.84858989190501));
#42781=CARTESIAN_POINT('',(-2.37174965175948,-0.00128525436374919,4.84688602397483));
#42782=CARTESIAN_POINT('Ctrl Pts',(-2.36545133284689,0.172736951556046,
5.836583843094));
#42783=CARTESIAN_POINT('Ctrl Pts',(-2.35983651434252,0.249626000454991,
5.83096966813975));
#42784=CARTESIAN_POINT('Ctrl Pts',(-2.35047365701173,0.326229766732311,
5.8253661914758));
#42785=CARTESIAN_POINT('Ctrl Pts',(-2.32956379880885,0.447724696538534,
5.81657106413305));
#42786=CARTESIAN_POINT('Ctrl Pts',(-2.32041718088337,0.49293978679623,5.81331910439767));
#42787=CARTESIAN_POINT('Ctrl Pts',(-2.30613380496632,0.554282574352545,
5.80896045886768));
#42788=CARTESIAN_POINT('Ctrl Pts',(-2.30213536430365,0.570661986976835,
5.8078019002244));
#42789=CARTESIAN_POINT('Ctrl Pts',(-2.29518143793053,0.59788501570341,5.80588667218263));
#42790=CARTESIAN_POINT('Ctrl Pts',(-2.29232297990814,0.608752578186658,
5.8051248758443));
#42791=CARTESIAN_POINT('Ctrl Pts',(-2.28619197080939,0.631406316164129,
5.80354319707501));
#42792=CARTESIAN_POINT('Ctrl Pts',(-2.28290531676541,0.643188148672387,
5.80272409584545));
#42793=CARTESIAN_POINT('Ctrl Pts',(-2.27370053826859,0.67522529260106,5.80050503703187));
#42794=CARTESIAN_POINT('Ctrl Pts',(-2.26760285882853,0.695428416428523,
5.79911468149373));
#42795=CARTESIAN_POINT('Ctrl Pts',(-2.25320214180448,0.740936764783969,
5.79599767779488));
#42796=CARTESIAN_POINT('Ctrl Pts',(-2.24474082441348,0.76618922871637,5.79427853762823));
#42797=CARTESIAN_POINT('Ctrl Pts',(-2.21543190440487,0.849003506085373,
5.78865906853966));
#42798=CARTESIAN_POINT('Ctrl Pts',(-2.19278025961378,0.905903495369401,
5.78482732084784));
#42799=CARTESIAN_POINT('Ctrl Pts',(-2.0839284368528,1.15124463554459,5.76818287956512));
#42800=CARTESIAN_POINT('Ctrl Pts',(-1.97546316278137,1.32878292144953,5.75572348062973));
#42801=CARTESIAN_POINT('Ctrl Pts',(-1.8231379551919,1.51743603271154,5.74008857939321));
#42802=CARTESIAN_POINT('Ctrl Pts',(-1.80035284539538,1.54440070674248,5.73779121446811));
#42803=CARTESIAN_POINT('Ctrl Pts',(-1.7627743021259,1.58691038309416,5.73406004428108));
#42804=CARTESIAN_POINT('Ctrl Pts',(-1.74835642117146,1.60278120126657,5.7326414452077));
#42805=CARTESIAN_POINT('Ctrl Pts',(-1.72024337623466,1.63289655267585,5.72989843924121));
#42806=CARTESIAN_POINT('Ctrl Pts',(-1.70658144095262,1.64716974556969,5.72857549078604));
#42807=CARTESIAN_POINT('Ctrl Pts',(-1.6742643236744,1.68009911305064,5.72546818068498));
#42808=CARTESIAN_POINT('Ctrl Pts',(-1.65547332016843,1.69861768672768,5.72367806386286));
#42809=CARTESIAN_POINT('Ctrl Pts',(-1.59073712136371,1.76032071365969,5.71756396410465));
#42810=CARTESIAN_POINT('Ctrl Pts',(-1.54338364568856,1.80198204375279,5.71317855851379));
#42811=CARTESIAN_POINT('Ctrl Pts',(-1.41792535371578,1.90378375833569,5.70177148837119));
#42812=CARTESIAN_POINT('Ctrl Pts',(-1.3376331501234,1.96103015710688,5.69466261665056));
#42813=CARTESIAN_POINT('Ctrl Pts',(-1.12843124466399,2.09134749485002,5.6767380436381));
#42814=CARTESIAN_POINT('Ctrl Pts',(-0.995787731911431,2.15766176086079,
5.66587905030475));
#42815=CARTESIAN_POINT('Ctrl Pts',(-0.835893066226128,2.21969233797341,
5.65388825973334));
#42816=CARTESIAN_POINT('Ctrl Pts',(-0.813838179902742,2.22787315887062,
5.65225792753819));
#42817=CARTESIAN_POINT('Ctrl Pts',(-0.779525726150336,2.24002310777201,
5.64976162452941));
#42818=CARTESIAN_POINT('Ctrl Pts',(-0.76735204258696,2.24422252525514,5.64888369492357));
#42819=CARTESIAN_POINT('Ctrl Pts',(-0.744591327685893,2.25186716929118,
5.64725741071244));
#42820=CARTESIAN_POINT('Ctrl Pts',(-0.734013808511635,2.25533716502136,
5.64650778162859));
#42821=CARTESIAN_POINT('Ctrl Pts',(-0.708653554826448,2.26345937517038,
5.64472460991575));
#42822=CARTESIAN_POINT('Ctrl Pts',(-0.693849037172218,2.26804139047526,
5.64369497980043));
#42823=CARTESIAN_POINT('Ctrl Pts',(-0.641325327004928,2.28373509900227,
5.64007849088617));
#42824=CARTESIAN_POINT('Ctrl Pts',(-0.603373807978468,2.29405419213439,
5.63753147455735));
#42825=CARTESIAN_POINT('Ctrl Pts',(-0.503721144162228,2.31850550335701,
5.63097302123838));
#42826=CARTESIAN_POINT('Ctrl Pts',(-0.441678563563814,2.33112071992003,
5.62701714561831));
#42827=CARTESIAN_POINT('Ctrl Pts',(-0.180051174976883,2.37349555920616,
5.61059795370754));
#42828=CARTESIAN_POINT('Ctrl Pts',(0.0223849324246697,2.38020899460828,
5.59844591271183));
#42829=CARTESIAN_POINT('Ctrl Pts',(0.259531218346824,2.35778951913976,5.58310421238673));
#42830=CARTESIAN_POINT('Ctrl Pts',(0.295750228301503,2.35352064921956,5.58073309322422));
#42831=CARTESIAN_POINT('Ctrl Pts',(0.353321685541067,2.34538522878325,5.57691175297781));
#42832=CARTESIAN_POINT('Ctrl Pts',(0.374745204281869,2.3420576563193,5.57547813515316));
#42833=CARTESIAN_POINT('Ctrl Pts',(0.415529824577874,2.33514894557895,5.57272522501834));
#42834=CARTESIAN_POINT('Ctrl Pts',(0.434897919747119,2.33161947862673,5.57140764420607));
#42835=CARTESIAN_POINT('Ctrl Pts',(0.479597990855436,2.32289742070321,5.5683419345559));
#42836=CARTESIAN_POINT('Ctrl Pts',(0.504893055628163,2.31753092151006,5.56658852023571));
#42837=CARTESIAN_POINT('Ctrl Pts',(0.588134927158108,2.29844320973825,5.56075440018524));
#42838=CARTESIAN_POINT('Ctrl Pts',(0.64564882979788,2.28295431792562,5.55661974714181));
#42839=CARTESIAN_POINT('Ctrl Pts',(0.78837678704089,2.23869188423944,5.54609264564333));
#42840=CARTESIAN_POINT('Ctrl Pts',(0.872647787070976,2.20720695701663,5.53962999957555));
#42841=CARTESIAN_POINT('Ctrl Pts',(1.08641916555434,2.11317966515402,5.52268023440513));
#42842=CARTESIAN_POINT('Ctrl Pts',(1.21239308135347,2.04351192242557,5.51211949869314));
#42843=CARTESIAN_POINT('Ctrl Pts',(1.36013008809604,1.9433112025839,5.49949005398249));
#42844=CARTESIAN_POINT('Ctrl Pts',(1.38853582243527,1.9231174832937,5.49705073319995));
#42845=CARTESIAN_POINT('Ctrl Pts',(1.42746342260215,1.89413132947216,5.49370311310393));
#42846=CARTESIAN_POINT('Ctrl Pts',(1.43836835859807,1.88586367563031,5.49276480453541));
#42847=CARTESIAN_POINT('Ctrl Pts',(1.45810390234321,1.87063025350073,5.49106660516452));
#42848=CARTESIAN_POINT('Ctrl Pts',(1.46695766140168,1.86369519410678,5.49030475680871));
#42849=CARTESIAN_POINT('Ctrl Pts',(1.48554969912342,1.84891764761507,5.48870537956168));
#42850=CARTESIAN_POINT('Ctrl Pts',(1.49527578168365,1.84106076226913,5.48786884253952));
#42851=CARTESIAN_POINT('Ctrl Pts',(1.52224234652545,1.81892206299536,5.48554841901247));
#42852=CARTESIAN_POINT('Ctrl Pts',(1.53934391466039,1.8044721202348,5.48407565823806));
#42853=CARTESIAN_POINT('Ctrl Pts',(1.57796207581588,1.77089311184019,5.4807403232036));
#42854=CARTESIAN_POINT('Ctrl Pts',(1.59934040855064,1.7516098689334,5.47888690682706));
#42855=CARTESIAN_POINT('Ctrl Pts',(1.67112545772865,1.68444947713912,5.47261764241429));
#42856=CARTESIAN_POINT('Ctrl Pts',(1.71977848410962,1.63474570818768,5.46828849406543));
#42857=CARTESIAN_POINT('Ctrl Pts',(1.88620036279507,1.44906283626675,5.45288118057935));
#42858=CARTESIAN_POINT('Ctrl Pts',(1.99059346289233,1.30194805649066,5.44199618722029));
#42859=CARTESIAN_POINT('Ctrl Pts',(2.09629805536048,1.11007785770259,5.42797764919269));
#42860=CARTESIAN_POINT('Ctrl Pts',(2.11437904391868,1.0752392174298,5.42544131297186));
#42861=CARTESIAN_POINT('Ctrl Pts',(2.14230512564725,1.0180001713845,5.42127821304472));
#42862=CARTESIAN_POINT('Ctrl Pts',(2.15268301391176,0.995867144617789,5.41966942702183));
#42863=CARTESIAN_POINT('Ctrl Pts',(2.1707385919924,0.95575830222694,5.4167536347155));
#42864=CARTESIAN_POINT('Ctrl Pts',(2.17853977120631,0.937840281716509,5.41545091406078));
#42865=CARTESIAN_POINT('Ctrl Pts',(2.19484969511452,0.899077151868505,5.41263132802331));
#42866=CARTESIAN_POINT('Ctrl Pts',(2.20328476776369,0.878203326015486,5.41111216799049));
#42867=CARTESIAN_POINT('Ctrl Pts',(2.2260950966414,0.819357702511538,5.40682565126848));
#42868=CARTESIAN_POINT('Ctrl Pts',(2.23979375712705,0.781133794847414,5.40403673838727));
#42869=CARTESIAN_POINT('Ctrl Pts',(2.26873040703623,0.693358738045418,5.39761866404703));
#42870=CARTESIAN_POINT('Ctrl Pts',(2.28333809055135,0.643622964301902,5.39397203732664));
#42871=CARTESIAN_POINT('Ctrl Pts',(2.3313110147999,0.457996298894227,5.38033256503023));
#42872=CARTESIAN_POINT('Ctrl Pts',(2.3542613151249,0.319717561064668,5.37009440142709));
#42873=CARTESIAN_POINT('Ctrl Pts',(2.37211308487593,0.0854853880717415,
5.35302706169835));
#42874=CARTESIAN_POINT('Ctrl Pts',(2.37363418225915,-0.00962548594368886,
5.3461787562647));
#42875=CARTESIAN_POINT('Ctrl Pts',(2.36854805337011,-0.12486126208412,5.33815179423761));
#42876=CARTESIAN_POINT('Ctrl Pts',(2.36739246938358,-0.145131593875779,
5.33675015968628));
#42877=CARTESIAN_POINT('Ctrl Pts',(2.36513570838378,-0.1774164502631,5.33453677978305));
#42878=CARTESIAN_POINT('Ctrl Pts',(2.3642029413978,-0.189441240740074,5.33371660195758));
#42879=CARTESIAN_POINT('Ctrl Pts',(2.36220410897676,-0.212888216794355,
5.33212624756636));
#42880=CARTESIAN_POINT('Ctrl Pts',(2.36114683879175,-0.22431062942299,5.33135567438545));
#42881=CARTESIAN_POINT('Ctrl Pts',(2.35826720248799,-0.253140654950356,
5.32942035755941));
#42882=CARTESIAN_POINT('Ctrl Pts',(2.3563348967022,-0.270537036741587,5.32826140518265));
#42883=CARTESIAN_POINT('Ctrl Pts',(2.34742496258216,-0.343392374366385,
5.32343889512857));
#42884=CARTESIAN_POINT('Ctrl Pts',(2.33868005416297,-0.398621292932018,
5.31985880299081));
#42885=CARTESIAN_POINT('Ctrl Pts',(2.30601380863896,-0.56631199619505,5.30908161051705));
#42886=CARTESIAN_POINT('Ctrl Pts',(2.27586364903919,-0.677389577911156,
5.30206656579179));
#42887=CARTESIAN_POINT('Ctrl Pts',(2.19275543315795,-0.914047990051146,
5.28663093986359));
#42888=CARTESIAN_POINT('Ctrl Pts',(2.13680738856947,-1.03812726825105,5.27820758601029));
#42889=CARTESIAN_POINT('Ctrl Pts',(2.05453625263995,-1.18539319646175,5.26730207458688));
#42890=CARTESIAN_POINT('Ctrl Pts',(2.03792904927482,-1.21372207111858,5.26516062861634));
#42891=CARTESIAN_POINT('Ctrl Pts',(2.00977723386111,-1.25953641855663,5.26161969661488));
#42892=CARTESIAN_POINT('Ctrl Pts',(1.99857925015029,-1.27723038403366,5.26023262482767));
#42893=CARTESIAN_POINT('Ctrl Pts',(1.97624494093414,-1.31150788601183,5.25750574510989));
#42894=CARTESIAN_POINT('Ctrl Pts',(1.96513046900119,-1.32810361047556,5.2561668175452));
#42895=CARTESIAN_POINT('Ctrl Pts',(1.93806811730361,-1.36742857516302,5.2529479908486));
#42896=CARTESIAN_POINT('Ctrl Pts',(1.921928421539,-1.39002157048769,5.25106107268301));
#42897=CARTESIAN_POINT('Ctrl Pts',(1.86172555493616,-1.47124246918038,5.24413596563973));
#42898=CARTESIAN_POINT('Ctrl Pts',(1.81534987304086,-1.52809664970729,5.23901170306047));
#42899=CARTESIAN_POINT('Ctrl Pts',(1.68620132630663,-1.672236098016,5.22526610473913));
#42900=CARTESIAN_POINT('Ctrl Pts',(1.59929886448346,-1.75553043511646,5.21651511940835));
#42901=CARTESIAN_POINT('Ctrl Pts',(1.41536576130241,-1.90679047771282,5.19917109576228));
#42902=CARTESIAN_POINT('Ctrl Pts',(1.31879384896392,-1.97481604771594,5.19060384247161));
#42903=CARTESIAN_POINT('Ctrl Pts',(1.19977622159638,-2.04601176707779,5.18094702497339));
#42904=CARTESIAN_POINT('Ctrl Pts',(1.18186066160913,-2.05641255129386,5.17951621115076));
#42905=CARTESIAN_POINT('Ctrl Pts',(1.15322497579121,-2.07253897569914,5.17726784418582));
#42906=CARTESIAN_POINT('Ctrl Pts',(1.1425936073757,-2.07841899413828,5.17644141602583));
#42907=CARTESIAN_POINT('Ctrl Pts',(1.1218852334152,-2.08966550203978,5.17484837771745));
#42908=CARTESIAN_POINT('Ctrl Pts',(1.11181393878483,-2.09504132641319,5.17408126538524));
#42909=CARTESIAN_POINT('Ctrl Pts',(1.08645623726605,-2.10834232782184,5.17216798820957));
#42910=CARTESIAN_POINT('Ctrl Pts',(1.07112123076078,-2.11617434961667,5.17102733755447));
#42911=CARTESIAN_POINT('Ctrl Pts',(1.00811921344539,-2.1474909143601,5.16640219539893));
#42912=CARTESIAN_POINT('Ctrl Pts',(0.959751291244879,-2.16953911145561,
5.16299285209468));
#42913=CARTESIAN_POINT('Ctrl Pts',(0.814335582076024,-2.23000963224693,
5.15303909169019));
#42914=CARTESIAN_POINT('Ctrl Pts',(0.715446723791671,-2.26367489001098,
5.14664629577101));
#42915=CARTESIAN_POINT('Ctrl Pts',(0.479863094888836,-2.32688784537193,
5.13165021929414));
#42916=CARTESIAN_POINT('Ctrl Pts',(0.342154011499422,-2.35108501746986,
5.12304683303129));
#42917=CARTESIAN_POINT('Ctrl Pts',(0.165457461621328,-2.36627368878776,
5.11164422385195));
#42918=CARTESIAN_POINT('Ctrl Pts',(0.127720289175776,-2.36861027186162,
5.10918964455716));
#42919=CARTESIAN_POINT('Ctrl Pts',(0.06780306886953,-2.37088417607716,5.10525320287712));
#42920=CARTESIAN_POINT('Ctrl Pts',(0.0456511166297272,-2.37141412527839,
5.10378941463638));
#42921=CARTESIAN_POINT('Ctrl Pts',(0.00390879856295782,-2.3718276631876,
5.10101361448089));
#42922=CARTESIAN_POINT('Ctrl Pts',(-0.0156791323647055,-2.3717790513836,
5.09970379477545));
#42923=CARTESIAN_POINT('Ctrl Pts',(-0.060242389168304,-2.37111640128047,
5.09670636877949));
#42924=CARTESIAN_POINT('Ctrl Pts',(-0.0852127699032866,-2.37035036152854,
5.09501425371175));
#42925=CARTESIAN_POINT('Ctrl Pts',(-0.164186061918645,-2.36667816136069,
5.08962078494959));
#42926=CARTESIAN_POINT('Ctrl Pts',(-0.218100797522671,-2.36231958651618,
5.08587621475144));
#42927=CARTESIAN_POINT('Ctrl Pts',(-0.348916604859631,-2.34722791523376,
5.07663381456617));
#42928=CARTESIAN_POINT('Ctrl Pts',(-0.425527737333055,-2.33455477371267,
5.07108675024579));
#42929=CARTESIAN_POINT('Ctrl Pts',(-0.652284268152342,-2.28551142151962,
5.05432164901246));
#42930=CARTESIAN_POINT('Ctrl Pts',(-0.799644697274543,-2.23821494534555,
5.04293997512563));
#42931=CARTESIAN_POINT('Ctrl Pts',(-0.979647580033029,-2.16037692293081,
5.02899055876038));
#42932=CARTESIAN_POINT('Ctrl Pts',(-1.01749132139787,-2.14281350661744,
5.02605715399275));
#42933=CARTESIAN_POINT('Ctrl Pts',(-1.06941906810972,-2.1170274799708,5.02204941448369));
#42934=CARTESIAN_POINT('Ctrl Pts',(-1.08390930638961,-2.10964526547953,
5.02093300712275));
#42935=CARTESIAN_POINT('Ctrl Pts',(-1.10828966663745,-2.09690689591035,
5.01905930388239));
#42936=CARTESIAN_POINT('Ctrl Pts',(-1.11821952898874,-2.09162846170564,
5.01829752110859));
#42937=CARTESIAN_POINT('Ctrl Pts',(-1.13911175640631,-2.08033142575201,
5.01669805684348));
#42938=CARTESIAN_POINT('Ctrl Pts',(-1.15006460891892,-2.07429647044581,
5.01586136985217));
#42939=CARTESIAN_POINT('Ctrl Pts',(-1.18050063976755,-2.05721121212241,
5.01354006903425));
#42940=CARTESIAN_POINT('Ctrl Pts',(-1.1998763281987,-2.04597082491982,5.01206659454421));
#42941=CARTESIAN_POINT('Ctrl Pts',(-1.24379966177214,-2.01965101396301,
5.00872935385576));
#42942=CARTESIAN_POINT('Ctrl Pts',(-1.26823795712945,-2.00439528293902,
5.00687476071485));
#42943=CARTESIAN_POINT('Ctrl Pts',(-1.35074439431465,-1.9507768863627,5.00059961628949));
#42944=CARTESIAN_POINT('Ctrl Pts',(-1.40740208496645,-1.91030402855942,
4.99626593753506));
#42945=CARTESIAN_POINT('Ctrl Pts',(-1.60402844081316,-1.75634241355609,
4.98083531419186));
#42946=CARTESIAN_POINT('Ctrl Pts',(-1.73273267552638,-1.62950283785317,
4.96993151329039));
#42947=CARTESIAN_POINT('Ctrl Pts',(-1.87033877347285,-1.45895620246359,
4.95590499940489));
#42948=CARTESIAN_POINT('Ctrl Pts',(-1.89408454084166,-1.42799293199246,
4.953383137315));
#42949=CARTESIAN_POINT('Ctrl Pts',(-1.93140966728029,-1.37675312149897,
4.94923887472202));
#42950=CARTESIAN_POINT('Ctrl Pts',(-1.94545933719025,-1.35682731255793,
4.94763417324986));
#42951=CARTESIAN_POINT('Ctrl Pts',(-1.9702102512868,-1.32054964227576,4.94472272706631));
#42952=CARTESIAN_POINT('Ctrl Pts',(-1.981021435069,-1.30427521156576,4.94342021079128));
#42953=CARTESIAN_POINT('Ctrl Pts',(-2.00388005504848,-1.26892542211526,
4.94059761244707));
#42954=CARTESIAN_POINT('Ctrl Pts',(-2.01585876493428,-1.249808138038,4.93907519211629));
#42955=CARTESIAN_POINT('Ctrl Pts',(-2.04874849083197,-1.1956149578706,4.93476919471659));
#42956=CARTESIAN_POINT('Ctrl Pts',(-2.06902812589879,-1.16016713041531,
4.93196374242355));
#42957=CARTESIAN_POINT('Ctrl Pts',(-2.11313935191103,-1.07822457384409,
4.92549991870341));
#42958=CARTESIAN_POINT('Ctrl Pts',(-2.13636944626691,-1.03143157021321,
4.92182370936814));
#42959=CARTESIAN_POINT('Ctrl Pts',(-2.21583607572108,-0.857135867678792,
4.90819181365658));
#42960=CARTESIAN_POINT('Ctrl Pts',(-2.26234976598788,-0.725519872764137,
4.89799515111079));
#42961=CARTESIAN_POINT('Ctrl Pts',(-2.32060810414617,-0.498932803671791,
4.88099784086205));
#42962=CARTESIAN_POINT('Ctrl Pts',(-2.33867064841662,-0.405929940600503,
4.87417747595414));
#42963=CARTESIAN_POINT('Ctrl Pts',(-2.35380885558994,-0.291885700629591,
4.86617071983084));
#42964=CARTESIAN_POINT('Ctrl Pts',(-2.35623013046204,-0.271648728433522,
4.86476356480965));
#42965=CARTESIAN_POINT('Ctrl Pts',(-2.35967040226515,-0.2393731642305,4.86254356312469));
#42966=CARTESIAN_POINT('Ctrl Pts',(-2.36085874751695,-0.227354149563595,
4.8617222009013));
#42967=CARTESIAN_POINT('Ctrl Pts',(-2.36289841662166,-0.204980625550495,
4.86020378989359));
#42968=CARTESIAN_POINT('Ctrl Pts',(-2.36377359581518,-0.194628818536194,
4.85950549340648));
#42969=CARTESIAN_POINT('Ctrl Pts',(-2.36547442213167,-0.172803726398664,
4.85804159350378));
#42970=CARTESIAN_POINT('Ctrl Pts',(-2.36628468549959,-0.161329382698505,
4.85727680634689));
#42971=CARTESIAN_POINT('Ctrl Pts',(-2.36830893667634,-0.129354424462884,
4.85515797272806));
#42972=CARTESIAN_POINT('Ctrl Pts',(-2.36934022612258,-0.108842750727502,
4.85381289252438));
#42973=CARTESIAN_POINT('Ctrl Pts',(-2.37118557821475,-0.0593216529717983,
4.85059401951231));
#42974=CARTESIAN_POINT('Ctrl Pts',(-2.37173392573361,-0.0303053436508547,
4.84873154878914));
#42975=CARTESIAN_POINT('Ctrl Pts',(-2.37174965175948,-0.00128525436374919,
4.84688602397483));
#42976=CARTESIAN_POINT('Ctrl Pts',(-2.3717496500648,-0.00128837785816269,
4.84688622261268));
#42977=CARTESIAN_POINT('Ctrl Pts',(-2.371781216878,0.056822352373548,4.84319068379912));
#42978=CARTESIAN_POINT('Ctrl Pts',(-2.36967708807495,0.114869689684006,
4.83956777994056));
#42979=CARTESIAN_POINT('Ctrl Pts',(-2.36545132791902,0.172737019038084,
4.83597583405741));
#42980=CARTESIAN_POINT('',(-2.37174912486677,-0.00129108034661244,4.64962605624969));
#42981=CARTESIAN_POINT('Ctrl Pts',(-2.36545134967025,0.172736721177577,
4.63766477577655));
#42982=CARTESIAN_POINT('Ctrl Pts',(-2.36658296888664,0.157240362415775,
4.6387145771999));
#42983=CARTESIAN_POINT('Ctrl Pts',(-2.36756226778942,0.141733467563053,
4.63976901278111));
#42984=CARTESIAN_POINT('Ctrl Pts',(-2.37065240762875,0.0837493591564288,
4.64372701539268));
#42985=CARTESIAN_POINT('Ctrl Pts',(-2.37177284112994,0.041230125981495,
4.64666004539431));
#42986=CARTESIAN_POINT('Ctrl Pts',(-2.37174964720368,-0.00129363410709259,
4.64962532548984));
#42987=CARTESIAN_POINT('Ctrl Pts',(-2.37174964856074,-0.00129114368864713,
4.64962515182724));
#42988=CARTESIAN_POINT('Ctrl Pts',(-2.37165110338696,-0.182312422208469,
4.66224817878405));
#42989=CARTESIAN_POINT('Ctrl Pts',(-2.35082803275891,-0.362713863320744,
4.675471399105));
#42990=CARTESIAN_POINT('Ctrl Pts',(-2.29472645522795,-0.60313390397009,
4.69340839884554));
#42991=CARTESIAN_POINT('Ctrl Pts',(-2.27708403754593,-0.666655278982695,
4.69817091492568));
#42992=CARTESIAN_POINT('Ctrl Pts',(-2.248187994304,-0.756066384117575,4.70484479801763));
#42993=CARTESIAN_POINT('Ctrl Pts',(-2.23908413951427,-0.782616120552576,
4.70682257672485));
#42994=CARTESIAN_POINT('Ctrl Pts',(-2.22197921086113,-0.829755382450694,
4.71031992200118));
#42995=CARTESIAN_POINT('Ctrl Pts',(-2.214157796454,-0.850406341721413,4.71184709082956));
#42996=CARTESIAN_POINT('Ctrl Pts',(-2.20139536674833,-0.882732736820557,
4.71422661614696));
#42997=CARTESIAN_POINT('Ctrl Pts',(-2.19664742706446,-0.894482389346666,
4.71508917241692));
#42998=CARTESIAN_POINT('Ctrl Pts',(-2.18738020811822,-0.916896956367165,
4.71672942425424));
#42999=CARTESIAN_POINT('Ctrl Pts',(-2.18287664792323,-0.927567652135011,
4.71750791612136));
#43000=CARTESIAN_POINT('Ctrl Pts',(-2.17254069258638,-0.95156534707847,
4.71925416987481));
#43001=CARTESIAN_POINT('Ctrl Pts',(-2.16666339030451,-0.964872763365423,
4.72021936711099));
#43002=CARTESIAN_POINT('Ctrl Pts',(-2.14458497625673,-1.01364362465095,
4.72374812597013));
#43003=CARTESIAN_POINT('Ctrl Pts',(-2.12763169684756,-1.0487620689161,4.72627219296531));
#43004=CARTESIAN_POINT('Ctrl Pts',(-2.03829367049038,-1.22273160849175,
4.73876847555801));
#43005=CARTESIAN_POINT('Ctrl Pts',(-1.95314563859356,-1.35460126906985,
4.74823774858585));
#43006=CARTESIAN_POINT('Ctrl Pts',(-1.79764613744162,-1.54994499577224,
4.76365949818677));
#43007=CARTESIAN_POINT('Ctrl Pts',(-1.73544703424529,-1.61928457174219,
4.769461707163));
#43008=CARTESIAN_POINT('Ctrl Pts',(-1.63765290788172,-1.71618199961081,
4.77826530960326));
#43009=CARTESIAN_POINT('Ctrl Pts',(-1.60508956957666,-1.74667535022641,
4.78114933774708));
#43010=CARTESIAN_POINT('Ctrl Pts',(-1.55391613248898,-1.79195585995192,
4.78562539877054));
#43011=CARTESIAN_POINT('Ctrl Pts',(-1.53591040487013,-1.80741260168723,
4.78719015760944));
#43012=CARTESIAN_POINT('Ctrl Pts',(-1.50221084466508,-1.83547423480581,
4.79010217698707));
#43013=CARTESIAN_POINT('Ctrl Pts',(-1.48658250753474,-1.84815461877676,
4.79144626087941));
#43014=CARTESIAN_POINT('Ctrl Pts',(-1.45148886169345,-1.87589546122685,
4.79445152143152));
#43015=CARTESIAN_POINT('Ctrl Pts',(-1.43194692010397,-1.89085473730379,
4.79611642288232));
#43016=CARTESIAN_POINT('Ctrl Pts',(-1.37383487442656,-1.93392173579044,
4.80104440013107));
#43017=CARTESIAN_POINT('Ctrl Pts',(-1.33464701784071,-1.96117116287171,
4.80433880445198));
#43018=CARTESIAN_POINT('Ctrl Pts',(-1.14880685008554,-2.08224540972875,
4.81983898563114));
#43019=CARTESIAN_POINT('Ctrl Pts',(-0.992945463331488,-2.16091317060829,
4.83254805105607));
#43020=CARTESIAN_POINT('Ctrl Pts',(-0.766607802552961,-2.2454569982077,
4.85010899360453));
#43021=CARTESIAN_POINT('Ctrl Pts',(-0.702318041090329,-2.26638810199638,
4.85499661336951));
#43022=CARTESIAN_POINT('Ctrl Pts',(-0.597488569635666,-2.29562775342633,
4.86273019202159));
#43023=CARTESIAN_POINT('Ctrl Pts',(-0.557473020839824,-2.30567206577461,
4.86562807191041));
#43024=CARTESIAN_POINT('Ctrl Pts',(-0.501547974343546,-2.3181685323608,
4.86958560992966));
#43025=CARTESIAN_POINT('Ctrl Pts',(-0.485847064565066,-2.32150993536767,
4.87068665295815));
#43026=CARTESIAN_POINT('Ctrl Pts',(-0.458851539734028,-2.32696912997076,
4.87256120100941));
#43027=CARTESIAN_POINT('Ctrl Pts',(-0.44757351532359,-2.32916466523366,
4.8733387713707));
#43028=CARTESIAN_POINT('Ctrl Pts',(-0.42319904605979,-2.33372614390257,
4.87500695287501));
#43029=CARTESIAN_POINT('Ctrl Pts',(-0.410098048240426,-2.33606394580354,
4.87589606556439));
#43030=CARTESIAN_POINT('Ctrl Pts',(-0.372883612360168,-2.34238193530011,
4.87840215368309));
#43031=CARTESIAN_POINT('Ctrl Pts',(-0.348726629173498,-2.34609999108689,
4.88000577168433));
#43032=CARTESIAN_POINT('Ctrl Pts',(-0.187920195213922,-2.368311271314,4.89055288782546));
#43033=CARTESIAN_POINT('Ctrl Pts',(-0.0499225087589769,-2.37523247260828,
4.89900353008266));
#43034=CARTESIAN_POINT('Ctrl Pts',(0.191198713584041,-2.36628922170586,
4.91384228154988));
#43035=CARTESIAN_POINT('Ctrl Pts',(0.294124070915623,-2.35571028587255,
4.92019896519204));
#43036=CARTESIAN_POINT('Ctrl Pts',(0.440152342953531,-2.33097982454859,
4.92953465697416));
#43037=CARTESIAN_POINT('Ctrl Pts',(0.484056076565638,-2.3222597603063,4.93238241454375));
#43038=CARTESIAN_POINT('Ctrl Pts',(0.563359202703935,-2.30416218942303,
4.9376221174143));
#43039=CARTESIAN_POINT('Ctrl Pts',(0.59883856704674,-2.29519696962475,4.94000171672073));
#43040=CARTESIAN_POINT('Ctrl Pts',(0.655427892318291,-2.27949610006659,
4.94386202939001));
#43041=CARTESIAN_POINT('Ctrl Pts',(0.676676344311584,-2.27327896724064,
4.94532638364013));
#43042=CARTESIAN_POINT('Ctrl Pts',(0.717309449702917,-2.26076988060579,
4.94815687727492));
#43043=CARTESIAN_POINT('Ctrl Pts',(0.736706215216213,-2.25452372099153,
4.94952144438719));
#43044=CARTESIAN_POINT('Ctrl Pts',(0.781368425072409,-2.2395036691234,4.95269568387034));
#43045=CARTESIAN_POINT('Ctrl Pts',(0.806570330594091,-2.23055094138072,
4.95451097405464));
#43046=CARTESIAN_POINT('Ctrl Pts',(0.887170580026883,-2.2003739553889,4.96039718478683));
#43047=CARTESIAN_POINT('Ctrl Pts',(0.941922140556682,-2.17749829641362,
4.96452032493413));
#43048=CARTESIAN_POINT('Ctrl Pts',(1.16134654918115,-2.07599623855053,4.98156450553382));
#43049=CARTESIAN_POINT('Ctrl Pts',(1.31753445314707,-1.98054897154749,4.99498604056335));
#43050=CARTESIAN_POINT('Ctrl Pts',(1.50118294470875,-1.83690574075698,5.01183579483194));
#43051=CARTESIAN_POINT('Ctrl Pts',(1.54014085461459,-1.80436683146923,5.01547568107742));
#43052=CARTESIAN_POINT('Ctrl Pts',(1.60343686299302,-1.74795503832035,5.02146584641049));
#43053=CARTESIAN_POINT('Ctrl Pts',(1.62835801764578,-1.72476289289692,5.02384537098807));
#43054=CARTESIAN_POINT('Ctrl Pts',(1.66348981771552,-1.69062798247203,5.02722026216105));
#43055=CARTESIAN_POINT('Ctrl Pts',(1.67410860957276,-1.68011360953002,5.02824312855876));
#43056=CARTESIAN_POINT('Ctrl Pts',(1.69187424080273,-1.66218699243977,5.02995808389872));
#43057=CARTESIAN_POINT('Ctrl Pts',(1.69907319907929,-1.65482758101297,5.03065400987143));
#43058=CARTESIAN_POINT('Ctrl Pts',(1.71561581946345,-1.63769448541001,5.03225537496554));
#43059=CARTESIAN_POINT('Ctrl Pts',(1.72492414200704,-1.62788746340444,5.03315820950765));
#43060=CARTESIAN_POINT('Ctrl Pts',(1.75150759098343,-1.59939573685941,5.03574363077265));
#43061=CARTESIAN_POINT('Ctrl Pts',(1.76856711081288,-1.5805113295587,5.0374115114201));
#43062=CARTESIAN_POINT('Ctrl Pts',(1.85194715336425,-1.48517102486712,5.04562938953061));
#43063=CARTESIAN_POINT('Ctrl Pts',(1.91363662188265,-1.40479193998499,5.05192546535555));
#43064=CARTESIAN_POINT('Ctrl Pts',(2.01778352495627,-1.24944354097062,5.06346468403217));
#43065=CARTESIAN_POINT('Ctrl Pts',(2.06165808021096,-1.17563830349169,5.06871334819673));
#43066=CARTESIAN_POINT('Ctrl Pts',(2.13482061768018,-1.03582027923389,5.0784820183481));
#43067=CARTESIAN_POINT('Ctrl Pts',(2.16527966060376,-0.970538851958767,
5.08297784731948));
#43068=CARTESIAN_POINT('Ctrl Pts',(2.21240472916112,-0.856230396023313,
5.09084107249904));
#43069=CARTESIAN_POINT('Ctrl Pts',(2.23052259857101,-0.807857362597834,
5.09416561744907));
#43070=CARTESIAN_POINT('Ctrl Pts',(2.25505218039733,-0.735230363445715,
5.0991755035198));
#43071=CARTESIAN_POINT('Ctrl Pts',(2.26268222692542,-0.711402197407416,
5.10082199721662));
#43072=CARTESIAN_POINT('Ctrl Pts',(2.27577265455452,-0.668178639355362,
5.10381604699735));
#43073=CARTESIAN_POINT('Ctrl Pts',(2.28136561259387,-0.64882568471274,5.10515923091088));
#43074=CARTESIAN_POINT('Ctrl Pts',(2.29292035873469,-0.606845725485791,
5.10807962909838));
#43075=CARTESIAN_POINT('Ctrl Pts',(2.29879513492063,-0.584197198847938,
5.10965943980867));
#43076=CARTESIAN_POINT('Ctrl Pts',(2.31420011263372,-0.520973066361815,
5.11408294913696));
#43077=CARTESIAN_POINT('Ctrl Pts',(2.32299689316245,-0.480229280151128,
5.11694899654504));
#43078=CARTESIAN_POINT('Ctrl Pts',(2.36431719483691,-0.260992070817214,
5.13246099549679));
#43079=CARTESIAN_POINT('Ctrl Pts',(2.37734679262253,-0.0794641915102049,
5.14568820799574));
#43080=CARTESIAN_POINT('Ctrl Pts',(2.36659072666646,0.171057333192036,5.16392008314734));
#43081=CARTESIAN_POINT('Ctrl Pts',(2.3605737986665,0.240217961819762,5.16894215865201));
#43082=CARTESIAN_POINT('Ctrl Pts',(2.34606670065391,0.350612346769363,5.1768583145386));
#43083=CARTESIAN_POINT('Ctrl Pts',(2.33949779738781,0.392056794425747,5.1798070040956));
#43084=CARTESIAN_POINT('Ctrl Pts',(2.32888177577863,0.449186570935638,5.18382083543816));
#43085=CARTESIAN_POINT('Ctrl Pts',(2.32576893887404,0.465035245760649,5.18492885552106));
#43086=CARTESIAN_POINT('Ctrl Pts',(2.32016232005791,0.492115004611031,5.18681128264761));
#43087=CARTESIAN_POINT('Ctrl Pts',(2.31774833507715,0.503361745429486,5.18758984898347));
#43088=CARTESIAN_POINT('Ctrl Pts',(2.31237683771739,0.527529227465505,5.18925552445166));
#43089=CARTESIAN_POINT('Ctrl Pts',(2.3093927205057,0.540443344324526,5.19014119344737));
#43090=CARTESIAN_POINT('Ctrl Pts',(2.30065716648568,0.576853323694828,5.19262753914778));
#43091=CARTESIAN_POINT('Ctrl Pts',(2.29465415994562,0.600287888253987,5.19421518475187));
#43092=CARTESIAN_POINT('Ctrl Pts',(2.25124025447184,0.759587698018044,5.20494643553421));
#43093=CARTESIAN_POINT('Ctrl Pts',(2.20213883935107,0.891992437052478,5.2135727046943));
#43094=CARTESIAN_POINT('Ctrl Pts',(2.07668361361566,1.15558442530973,5.23152603669983));
#43095=CARTESIAN_POINT('Ctrl Pts',(1.99894431816741,1.28538123317038,5.24082935445429));
#43096=CARTESIAN_POINT('Ctrl Pts',(1.88933054733923,1.4341454558541,5.25276667180737));
#43097=CARTESIAN_POINT('Ctrl Pts',(1.8686779708433,1.46095364898792,5.25497230353333));
#43098=CARTESIAN_POINT('Ctrl Pts',(1.83392627778115,1.50412041442188,5.2586204864492));
#43099=CARTESIAN_POINT('Ctrl Pts',(1.82016436689223,1.52074502804192,5.26004989434407));
#43100=CARTESIAN_POINT('Ctrl Pts',(1.79296456102121,1.55270466626286,5.26284724608678));
#43101=CARTESIAN_POINT('Ctrl Pts',(1.77955197594444,1.56805880592934,5.26421409831973));
#43102=CARTESIAN_POINT('Ctrl Pts',(1.74685277984816,1.60453149123839,5.26751785476558));
#43103=CARTESIAN_POINT('Ctrl Pts',(1.72737926010606,1.62547737945573,5.26946232587143));
#43104=CARTESIAN_POINT('Ctrl Pts',(1.65864419332484,1.69677914344971,5.27625053930209));
#43105=CARTESIAN_POINT('Ctrl Pts',(1.60752552256837,1.74528508462493,5.28117120312147));
#43106=CARTESIAN_POINT('Ctrl Pts',(1.39025754495403,1.933795816761,5.30158376068989));
#43107=CARTESIAN_POINT('Ctrl Pts',(1.20743280282681,2.05291818166336,5.31775448736565));
#43108=CARTESIAN_POINT('Ctrl Pts',(0.979494169096872,2.16032398550873,5.33556845606557));
#43109=CARTESIAN_POINT('Ctrl Pts',(0.947696643084033,2.17446083439009,5.3380021090852));
#43110=CARTESIAN_POINT('Ctrl Pts',(0.9016981795616,2.19371043807433,5.3414385918448));
#43111=CARTESIAN_POINT('Ctrl Pts',(0.887743097695399,2.19939476109261,5.34247025485715));
#43112=CARTESIAN_POINT('Ctrl Pts',(0.864150742059678,2.20874349456479,5.34419497424904));
#43113=CARTESIAN_POINT('Ctrl Pts',(0.854542378580899,2.21247862536741,5.34489198165544));
#43114=CARTESIAN_POINT('Ctrl Pts',(0.832356030646821,2.22093718812977,5.34648881934817));
#43115=CARTESIAN_POINT('Ctrl Pts',(0.819761846707342,2.22561656431074,5.3473861326129));
#43116=CARTESIAN_POINT('Ctrl Pts',(0.783583980828815,2.23870970515927,5.34993949957969));
#43117=CARTESIAN_POINT('Ctrl Pts',(0.759905173631907,2.24685763782029,5.35158139935531));
#43118=CARTESIAN_POINT('Ctrl Pts',(0.609758667198756,2.29587808563206,5.36183503662984));
#43119=CARTESIAN_POINT('Ctrl Pts',(0.480157420582651,2.32643913705813,5.36999430703003));
#43120=CARTESIAN_POINT('Ctrl Pts',(0.243819935023265,2.3615641471679,5.38468873245931));
#43121=CARTESIAN_POINT('Ctrl Pts',(0.138051933709894,2.37009985653739,5.39120050065762));
#43122=CARTESIAN_POINT('Ctrl Pts',(-0.0340796963843198,2.37242778751211,
5.40204530382957));
#43123=CARTESIAN_POINT('Ctrl Pts',(-0.100235773192517,2.37055408272223,
5.40627102428342));
#43124=CARTESIAN_POINT('Ctrl Pts',(-0.193461720510762,2.36400427995252,
5.41235713792293));
#43125=CARTESIAN_POINT('Ctrl Pts',(-0.220664413446217,2.36162037392588,
5.41414873359078));
#43126=CARTESIAN_POINT('Ctrl Pts',(-0.268097355340189,2.35663693022035,
5.41730325899755));
#43127=CARTESIAN_POINT('Ctrl Pts',(-0.288346836832517,2.35424507461221,
5.41865971031016));
#43128=CARTESIAN_POINT('Ctrl Pts',(-0.330475866091216,2.34871714557575,
5.42150337084423));
#43129=CARTESIAN_POINT('Ctrl Pts',(-0.352347367323676,2.34553571806251,
5.42299185353294));
#43130=CARTESIAN_POINT('Ctrl Pts',(-0.41012085590314,2.3363057065339,5.42695743813941));
#43131=CARTESIAN_POINT('Ctrl Pts',(-0.445932304636449,2.32973552186478,
5.42945030421442));
#43132=CARTESIAN_POINT('Ctrl Pts',(-0.655821475485251,2.28621150450753,
5.44427414732502));
#43133=CARTESIAN_POINT('Ctrl Pts',(-0.825419083931088,2.23058899133352,
5.45718409978112));
#43134=CARTESIAN_POINT('Ctrl Pts',(-1.05873146646179,2.12378900845944,5.47586369815742));
#43135=CARTESIAN_POINT('Ctrl Pts',(-1.12862122409183,2.08748831090851,5.48157964825219));
#43136=CARTESIAN_POINT('Ctrl Pts',(-1.22351292835331,2.03204017152364,5.4894119693805));
#43137=CARTESIAN_POINT('Ctrl Pts',(-1.25013437683699,2.01577165594001,5.49161731552381));
#43138=CARTESIAN_POINT('Ctrl Pts',(-1.29658348095563,1.98611208212418,5.49547003381992));
#43139=CARTESIAN_POINT('Ctrl Pts',(-1.31654379186555,1.97293752473937,5.49712725662053));
#43140=CARTESIAN_POINT('Ctrl Pts',(-1.34708781085225,1.95210730270141,5.49966173970242));
#43141=CARTESIAN_POINT('Ctrl Pts',(-1.35781269977561,1.94466274288617,5.50055138332652));
#43142=CARTESIAN_POINT('Ctrl Pts',(-1.37791785696558,1.93045955279906,5.50221777364405));
#43143=CARTESIAN_POINT('Ctrl Pts',(-1.38731059142363,1.92372062260659,5.50299561104756));
#43144=CARTESIAN_POINT('Ctrl Pts',(-1.40792455599873,1.90870137966437,5.50470191185869));
#43145=CARTESIAN_POINT('Ctrl Pts',(-1.41912258964514,1.90039038371628,5.50562833468664));
#43146=CARTESIAN_POINT('Ctrl Pts',(-1.45751559345723,1.87136711004092,5.50880543138979));
#43147=CARTESIAN_POINT('Ctrl Pts',(-1.48433698533777,1.85016500788029,5.51102638857135));
#43148=CARTESIAN_POINT('Ctrl Pts',(-1.62152198039556,1.73681698897707,5.5224485253824));
#43149=CARTESIAN_POINT('Ctrl Pts',(-1.72380705779316,1.63534832659884,5.5311948392174));
#43150=CARTESIAN_POINT('Ctrl Pts',(-1.87377211965941,1.45676660934416,5.54555460638491));
#43151=CARTESIAN_POINT('Ctrl Pts',(-1.92734549629563,1.38510964880787,5.55108670487353));
#43152=CARTESIAN_POINT('Ctrl Pts',(-2.00968597081519,1.26091800275511,5.56051148598884));
#43153=CARTESIAN_POINT('Ctrl Pts',(-2.04074085321657,1.21001148773585,5.56433205257));
#43154=CARTESIAN_POINT('Ctrl Pts',(-2.0827018671235,1.13500862488954,5.56993692251447));
#43155=CARTESIAN_POINT('Ctrl Pts',(-2.09517610034106,1.11181323303174,5.57166696263946));
#43156=CARTESIAN_POINT('Ctrl Pts',(-2.1165602725007,1.07041173891797,5.57475183190208));
#43157=CARTESIAN_POINT('Ctrl Pts',(-2.12562806533239,1.05228986660156,5.57610108195207));
#43158=CARTESIAN_POINT('Ctrl Pts',(-2.14429785436192,1.01375228318112,5.57896937725715));
#43159=CARTESIAN_POINT('Ctrl Pts',(-2.15384293249525,0.993311402531853,
5.5804901876685));
#43160=CARTESIAN_POINT('Ctrl Pts',(-2.17895320975329,0.937473238005745,
5.58464457123343));
#43161=CARTESIAN_POINT('Ctrl Pts',(-2.19394611875703,0.901827751408585,
5.5872967094198));
#43162=CARTESIAN_POINT('Ctrl Pts',(-2.25868233697933,0.736736555146988,
5.59958715013205));
#43163=CARTESIAN_POINT('Ctrl Pts',(-2.29787792279577,0.603467666674163,
5.60955064411162));
#43164=CARTESIAN_POINT('Ctrl Pts',(-2.34477954047919,0.370222179973078,
5.62685247337639));
#43165=CARTESIAN_POINT('Ctrl Pts',(-2.35822058487779,0.27175459322788,5.6341098994282));
#43166=CARTESIAN_POINT('Ctrl Pts',(-2.36545134983051,0.172736718982988,
5.64123248379855));
#43167=CARTESIAN_POINT('Origin',(0.,0.,-1.84858989190501));
#43168=CARTESIAN_POINT('',(-2.36545134966528,0.172736721245734,6.83902895557492));
#43169=CARTESIAN_POINT('',(-2.36545136499511,0.172736511319393,6.6396530072276));
#43170=CARTESIAN_POINT('',(-2.36545134966535,0.172736721244682,-1.84858989190501));
#43171=CARTESIAN_POINT('Ctrl Pts',(-2.36545134966532,0.172736721245143,
6.83902895557496));
#43172=CARTESIAN_POINT('Ctrl Pts',(-2.36542532467499,0.173093106662592,
6.83900560678643));
#43173=CARTESIAN_POINT('Ctrl Pts',(-2.36539921913017,0.173449486382915,
6.83898225563025));
#43174=CARTESIAN_POINT('Ctrl Pts',(-2.3639291327463,0.193456307102682,6.8376711896765));
#43175=CARTESIAN_POINT('Ctrl Pts',(-2.36224045459217,0.213087504274731,
6.83637638238029));
#43176=CARTESIAN_POINT('Ctrl Pts',(-2.35849122463444,0.251117278926783,
6.8338505940092));
#43177=CARTESIAN_POINT('Ctrl Pts',(-2.35645945002291,0.269517295416842,
6.83262057564433));
#43178=CARTESIAN_POINT('Ctrl Pts',(-2.35170092552846,0.308429833699506,
6.83000150861523));
#43179=CARTESIAN_POINT('Ctrl Pts',(-2.34892070930324,0.328934128388039,
6.82861090973337));
#43180=CARTESIAN_POINT('Ctrl Pts',(-2.3412170627432,0.380656599659059,6.82507524540553));
#43181=CARTESIAN_POINT('Ctrl Pts',(-2.33593740339763,0.411816785893085,
6.82291938843814));
#43182=CARTESIAN_POINT('Ctrl Pts',(-2.30897578139668,0.553670738115659,
6.81298205457405));
#43183=CARTESIAN_POINT('Ctrl Pts',(-2.28003987291106,0.662821430618337,
6.80498159700965));
#43184=CARTESIAN_POINT('Ctrl Pts',(-2.19825955134394,0.901253604394254,
6.78678097333404));
#43185=CARTESIAN_POINT('Ctrl Pts',(-2.14154523272019,1.02877910230439,6.7765348047321));
#43186=CARTESIAN_POINT('Ctrl Pts',(-2.04634395039736,1.2003819879763,6.76245446212597));
#43187=CARTESIAN_POINT('Ctrl Pts',(-2.0169333247234,1.24916834045662,6.75841815581534));
#43188=CARTESIAN_POINT('Ctrl Pts',(-1.9761659607068,1.31159296812389,6.75325176968593));
#43189=CARTESIAN_POINT('Ctrl Pts',(-1.96637520310589,1.32622646045377,6.75204057795236));
#43190=CARTESIAN_POINT('Ctrl Pts',(-1.94992614204335,1.35022892431204,6.75005550178593));
#43191=CARTESIAN_POINT('Ctrl Pts',(-1.94336120026763,1.35966075649119,6.74927587419132));
#43192=CARTESIAN_POINT('Ctrl Pts',(-1.92978363109161,1.37886834775541,6.74768961917059));
#43193=CARTESIAN_POINT('Ctrl Pts',(-1.92276473136573,1.3886391132304,6.74688341655464));
#43194=CARTESIAN_POINT('Ctrl Pts',(-1.90378576072101,1.4146392640734,6.74473877917064));
#43195=CARTESIAN_POINT('Ctrl Pts',(-1.89169231926433,1.43077066814459,6.74340888745887));
#43196=CARTESIAN_POINT('Ctrl Pts',(-1.82412853727094,1.51853930910172,6.73616513714645));
#43197=CARTESIAN_POINT('Ctrl Pts',(-1.76478817211058,1.58711464082255,6.7304743645058));
#43198=CARTESIAN_POINT('Ctrl Pts',(-1.60174843662205,1.75504226204715,6.71596463527191));
#43199=CARTESIAN_POINT('Ctrl Pts',(-1.49270676434456,1.84867466489829,6.70727132185702));
#43200=CARTESIAN_POINT('Ctrl Pts',(-1.31286736355104,1.97675510243706,6.6934462843553));
#43201=CARTESIAN_POINT('Ctrl Pts',(-1.24770883019535,2.01851489099284,6.68853168445244));
#43202=CARTESIAN_POINT('Ctrl Pts',(-1.15613376662309,2.07107474300824,6.68166818213167));
#43203=CARTESIAN_POINT('Ctrl Pts',(-1.1313880620436,2.08469585822529,6.67981789415524));
#43204=CARTESIAN_POINT('Ctrl Pts',(-1.08866580632776,2.10722734119433,6.6766274799188));
#43205=CARTESIAN_POINT('Ctrl Pts',(-1.07080829587183,2.11635768662975,6.67529509979448));
#43206=CARTESIAN_POINT('Ctrl Pts',(-1.03640761869444,2.1333995177124,6.67272957969641));
#43207=CARTESIAN_POINT('Ctrl Pts',(-1.01988422210213,2.14134779887459,6.67149781545816));
#43208=CARTESIAN_POINT('Ctrl Pts',(-0.976126976102489,2.16177509015727,
6.66823631177346));
#43209=CARTESIAN_POINT('Ctrl Pts',(-0.948746719658261,2.17393075693665,
6.66619591181752));
#43210=CARTESIAN_POINT('Ctrl Pts',(-0.840110769079175,2.21971729761167,
6.65809819071309));
#43211=CARTESIAN_POINT('Ctrl Pts',(-0.757249583070241,2.24933342793609,
6.65191368241777));
#43212=CARTESIAN_POINT('Ctrl Pts',(-0.485410935009481,2.32976865411779,
6.63162530989638));
#43213=CARTESIAN_POINT('Ctrl Pts',(-0.291750328215603,2.36184706564075,
6.61710725986489));
#43214=CARTESIAN_POINT('Ctrl Pts',(-0.0609873882252387,2.37122998970069,
6.60076898323319));
#43215=CARTESIAN_POINT('Ctrl Pts',(-0.0255879450803394,2.37187619749758,
6.59829162742651));
#43216=CARTESIAN_POINT('Ctrl Pts',(0.0247153748751761,2.37166802974491,
6.59482401331062));
#43217=CARTESIAN_POINT('Ctrl Pts',(0.0396155094544078,2.37146594600062,
6.5938034705129));
#43218=CARTESIAN_POINT('Ctrl Pts',(0.06557563217951,2.37086911080748,6.59203799528834));
#43219=CARTESIAN_POINT('Ctrl Pts',(0.076636230171716,2.37053736737872,6.59128983321678));
#43220=CARTESIAN_POINT('Ctrl Pts',(0.100929210243043,2.36963852652243,6.58965564475329));
#43221=CARTESIAN_POINT('Ctrl Pts',(0.114159670552405,2.36903799924672,6.58877139473487));
#43222=CARTESIAN_POINT('Ctrl Pts',(0.152599071684038,2.36697046562635,6.58621727861332));
#43223=CARTESIAN_POINT('Ctrl Pts',(0.177791298605128,2.36521162639432,6.58456208658935));
#43224=CARTESIAN_POINT('Ctrl Pts',(0.317055483434422,2.35325085106747,6.57549211726679));
#43225=CARTESIAN_POINT('Ctrl Pts',(0.430312859504358,2.33519815961538,6.56840918207765));
#43226=CARTESIAN_POINT('Ctrl Pts',(0.655496726036591,2.28235689072448,6.55417236284696));
#43227=CARTESIAN_POINT('Ctrl Pts',(0.767031136827342,2.24732968264644,6.54703643569882));
#43228=CARTESIAN_POINT('Ctrl Pts',(0.921178344166718,2.18610178183194,6.53662333564196));
#43229=CARTESIAN_POINT('Ctrl Pts',(0.96624966207171,2.16655756696394,6.53350948154794));
#43230=CARTESIAN_POINT('Ctrl Pts',(1.04597382433044,2.12900419839743,6.52784744369699));
#43231=CARTESIAN_POINT('Ctrl Pts',(1.08085055314369,2.11151176322449,6.52531558436485));
#43232=CARTESIAN_POINT('Ctrl Pts',(1.13486771600584,2.08273042119615,6.52129767930024));
#43233=CARTESIAN_POINT('Ctrl Pts',(1.15430885891841,2.07201876045021,6.51983145696891));
#43234=CARTESIAN_POINT('Ctrl Pts',(1.19061274640348,2.05134658162497,6.51705366765181));
#43235=CARTESIAN_POINT('Ctrl Pts',(1.20750812261734,2.04144693903642,6.51574433042117));
#43236=CARTESIAN_POINT('Ctrl Pts',(1.24562112562161,2.01847641479658,6.51275169187655));
#43237=CARTESIAN_POINT('Ctrl Pts',(1.26675891460345,2.00527823437122,6.51106393679386));
#43238=CARTESIAN_POINT('Ctrl Pts',(1.33278573402331,1.96259130330786,6.50570066036345));
#43239=CARTESIAN_POINT('Ctrl Pts',(1.37688056729968,1.93191137482338,6.50198261237318));
#43240=CARTESIAN_POINT('Ctrl Pts',(1.57952985708404,1.78045020609046,6.48423034828215));
#43241=CARTESIAN_POINT('Ctrl Pts',(1.72347801509004,1.64149924780821,6.46953611437609));
#43242=CARTESIAN_POINT('Ctrl Pts',(1.89215701684174,1.43172312985216,6.45011264262666));
#43243=CARTESIAN_POINT('Ctrl Pts',(1.93355444575195,1.37530299678486,6.44512450608028));
#43244=CARTESIAN_POINT('Ctrl Pts',(1.98278763930992,1.30157637529536,6.43897014364482));
#43245=CARTESIAN_POINT('Ctrl Pts',(1.99299051498817,1.2858991968201,6.43768145326722));
#43246=CARTESIAN_POINT('Ctrl Pts',(2.00928231419232,1.26020631356106,6.43560372108651));
#43247=CARTESIAN_POINT('Ctrl Pts',(2.0154841308751,1.25026361392333,6.43480788113702));
#43248=CARTESIAN_POINT('Ctrl Pts',(2.02775841297569,1.23025689250392,6.43322348315045));
#43249=CARTESIAN_POINT('Ctrl Pts',(2.03383026413275,1.22019288409894,6.43243497279787));
#43250=CARTESIAN_POINT('Ctrl Pts',(2.04945443853848,1.19385535786401,6.4303923388121));
#43251=CARTESIAN_POINT('Ctrl Pts',(2.05888802490903,1.17751189652115,6.42914538505867));
#43252=CARTESIAN_POINT('Ctrl Pts',(2.10013455670182,1.10404175409316,6.4236231282517));
#43253=CARTESIAN_POINT('Ctrl Pts',(2.12977480253932,1.0457218620721,6.41946172680066));
#43254=CARTESIAN_POINT('Ctrl Pts',(2.22561266703555,0.836119767353759,6.40501562865975));
#43255=CARTESIAN_POINT('Ctrl Pts',(2.27839686035632,0.679234708973688,6.39507692935581));
#43256=CARTESIAN_POINT('Ctrl Pts',(2.33241831302828,0.437925538951538,6.37962819857534));
#43257=CARTESIAN_POINT('Ctrl Pts',(2.34619134424461,0.356844627523759,6.37441735047596));
#43258=CARTESIAN_POINT('Ctrl Pts',(2.35906792130351,0.246627599565111,6.36720915662877));
#43259=CARTESIAN_POINT('Ctrl Pts',(2.3618872360025,0.217979814007121,6.36532462449572));
#43260=CARTESIAN_POINT('Ctrl Pts',(2.36579270835301,0.169201134070067,6.36209360071417));
#43261=CARTESIAN_POINT('Ctrl Pts',(2.36714490439128,0.14909434144515,6.36075537079677));
#43262=CARTESIAN_POINT('Ctrl Pts',(2.36936399731871,0.108346778454531,6.35802928724783));
#43263=CARTESIAN_POINT('Ctrl Pts',(2.37021775364071,0.0877070733611477,
6.35664115069178));
#43264=CARTESIAN_POINT('Ctrl Pts',(2.37169040373146,0.0356433515391833,
6.35311996733857));
#43265=CARTESIAN_POINT('Ctrl Pts',(2.37195444720267,0.00421410901337383,
6.35097630965169));
#43266=CARTESIAN_POINT('Ctrl Pts',(2.3703997750263,-0.131290118411623,6.341651980117));
#43267=CARTESIAN_POINT('Ctrl Pts',(2.36235569961672,-0.235165147250278,
6.33428800792809));
#43268=CARTESIAN_POINT('Ctrl Pts',(2.32719970021587,-0.47921597985295,6.31652958673824));
#43269=CARTESIAN_POINT('Ctrl Pts',(2.29421094254769,-0.618142938735001,
6.30604590380047));
#43270=CARTESIAN_POINT('Ctrl Pts',(2.22930560262247,-0.811924538389362,
6.29134842433696));
#43271=CARTESIAN_POINT('Ctrl Pts',(2.20736911906492,-0.869797592671791,
6.28695273727277));
#43272=CARTESIAN_POINT('Ctrl Pts',(2.17613591017555,-0.943375172592391,
6.28140964945651));
#43273=CARTESIAN_POINT('Ctrl Pts',(2.1688892407961,-0.95991860375963,6.2801664102373));
#43274=CARTESIAN_POINT('Ctrl Pts',(2.15668571918784,-0.986934108320738,
6.27814313877535));
#43275=CARTESIAN_POINT('Ctrl Pts',(2.15183997357075,-0.997455248131422,
6.27735693083482));
#43276=CARTESIAN_POINT('Ctrl Pts',(2.14185741769152,-1.01871812390797,6.27577220072896));
#43277=CARTESIAN_POINT('Ctrl Pts',(2.13671644670183,-1.02945745680394,6.27497393971008));
#43278=CARTESIAN_POINT('Ctrl Pts',(2.12290721246118,-1.05775538073396,6.27287504344825));
#43279=CARTESIAN_POINT('Ctrl Pts',(2.11410180617813,-1.07524652597635,6.27158232457971));
#43280=CARTESIAN_POINT('Ctrl Pts',(2.07003500371878,-1.16014662388675,6.26532057805561));
#43281=CARTESIAN_POINT('Ctrl Pts',(2.03175772002092,-1.22594779437349,6.26050716376725));
#43282=CARTESIAN_POINT('Ctrl Pts',(1.90582494383209,-1.42028324048335,6.24607016420576));
#43283=CARTESIAN_POINT('Ctrl Pts',(1.80864460958961,-1.54213482558072,6.23668192429487));
#43284=CARTESIAN_POINT('Ctrl Pts',(1.64432334523634,-1.71109031693999,6.22194410999281));
#43285=CARTESIAN_POINT('Ctrl Pts',(1.58553583781208,-1.7657019891943,6.21685544961642));
#43286=CARTESIAN_POINT('Ctrl Pts',(1.50221137590773,-1.83558577721047,6.20978922977191));
#43287=CARTESIAN_POINT('Ctrl Pts',(1.47999396530646,-1.85354576777793,6.20791850088244));
#43288=CARTESIAN_POINT('Ctrl Pts',(1.44159107126498,-1.88345899155765,6.20470387574747));
#43289=CARTESIAN_POINT('Ctrl Pts',(1.42556766372122,-1.89561583248758,6.2033680324422));
#43290=CARTESIAN_POINT('Ctrl Pts',(1.39273351113588,-1.91987510553488,6.20064048857699));
#43291=CARTESIAN_POINT('Ctrl Pts',(1.37591499233533,-1.93196401146227,6.19924843066712));
#43292=CARTESIAN_POINT('Ctrl Pts',(1.33295577146983,-1.96199699389624,6.19570419980298));
#43293=CARTESIAN_POINT('Ctrl Pts',(1.3066102739149,-1.97963954275863,6.19354112804837));
#43294=CARTESIAN_POINT('Ctrl Pts',(1.18798153421953,-2.05568084013864,6.18384253785017));
#43295=CARTESIAN_POINT('Ctrl Pts',(1.09209513517765,-2.10818553320995,6.17610347514817));
#43296=CARTESIAN_POINT('Ctrl Pts',(0.889233005668803,-2.2017049855788,6.1599888998064));
#43297=CARTESIAN_POINT('Ctrl Pts',(0.782204118916242,-2.24196245435948,
6.15162074190443));
#43298=CARTESIAN_POINT('Ctrl Pts',(0.619587887031015,-2.29006031654228,
6.13933794723494));
#43299=CARTESIAN_POINT('Ctrl Pts',(0.565941583773536,-2.30390456202802,
6.13535459203533));
#43300=CARTESIAN_POINT('Ctrl Pts',(0.476743005521254,-2.3236194590524,6.12888910013483));
#43301=CARTESIAN_POINT('Ctrl Pts',(0.441454813231906,-2.33058131352853,
6.12637135719678));
#43302=CARTESIAN_POINT('Ctrl Pts',(0.391251564421225,-2.33930437553239,
6.12285813748782));
#43303=CARTESIAN_POINT('Ctrl Pts',(0.376458848129943,-2.34173045262465,
6.12183133806096));
#43304=CARTESIAN_POINT('Ctrl Pts',(0.35069936955868,-2.34570472207914,6.1200590123873));
#43305=CARTESIAN_POINT('Ctrl Pts',(0.339743269926519,-2.34731659980889,
6.11931017410947));
#43306=CARTESIAN_POINT('Ctrl Pts',(0.315719261384868,-2.35067930993816,
6.11767922811137));
#43307=CARTESIAN_POINT('Ctrl Pts',(0.302647540104854,-2.35239800135795,
6.11679883634816));
#43308=CARTESIAN_POINT('Ctrl Pts',(0.264020877357473,-2.35714939016802,
6.11421620555426));
#43309=CARTESIAN_POINT('Ctrl Pts',(0.238429275463149,-2.35987539513475,
6.11252949050779));
#43310=CARTESIAN_POINT('Ctrl Pts',(0.107097806058428,-2.37170637756908,
6.1039750688423));
#43311=CARTESIAN_POINT('Ctrl Pts',(0.000866616818803647,-2.37412408417339,
6.09738870717227));
#43312=CARTESIAN_POINT('Ctrl Pts',(-0.227511513130802,-2.36398631128562,
6.08330183214533));
#43313=CARTESIAN_POINT('Ctrl Pts',(-0.349235020293758,-2.34909054807512,
6.0758325011141));
#43314=CARTESIAN_POINT('Ctrl Pts',(-0.541849729439626,-2.31021223325413,
6.06350784294496));
#43315=CARTESIAN_POINT('Ctrl Pts',(-0.613705324291566,-2.29217056406882,
6.05879578316037));
#43316=CARTESIAN_POINT('Ctrl Pts',(-0.711261791736611,-2.26275948565538,
6.05216890181641));
#43317=CARTESIAN_POINT('Ctrl Pts',(-0.737784179258192,-2.25425114532952,
6.05034358157497));
#43318=CARTESIAN_POINT('Ctrl Pts',(-0.783072163553667,-2.23883799811418,
6.04718260831492));
#43319=CARTESIAN_POINT('Ctrl Pts',(-0.801911945278698,-2.23215922067777,
6.04585433041541));
#43320=CARTESIAN_POINT('Ctrl Pts',(-0.84028527334229,-2.21800722577292,
6.0431203689425));
#43321=CARTESIAN_POINT('Ctrl Pts',(-0.859808837423326,-2.21051218266549,
6.04171407037881));
#43322=CARTESIAN_POINT('Ctrl Pts',(-0.909602896822906,-2.19063691761851,
6.03808666325165));
#43323=CARTESIAN_POINT('Ctrl Pts',(-0.93972021886839,-2.17788733947459,
6.03585359748941));
#43324=CARTESIAN_POINT('Ctrl Pts',(-1.09486508333506,-2.10839259934208,
6.02413972769836));
#43325=CARTESIAN_POINT('Ctrl Pts',(-1.21503704678675,-2.04150017996007,
6.01432371358579));
#43326=CARTESIAN_POINT('Ctrl Pts',(-1.423215504033,-1.90070146021737,5.99607237790804));
#43327=CARTESIAN_POINT('Ctrl Pts',(-1.51296612243999,-1.8300663650977,5.9877132809889));
#43328=CARTESIAN_POINT('Ctrl Pts',(-1.63844391685033,-1.71575039899171,
5.9755420935242));
#43329=CARTESIAN_POINT('Ctrl Pts',(-1.67827141089234,-1.67681364774516,
5.97159808391528));
#43330=CARTESIAN_POINT('Ctrl Pts',(-1.72875584480334,-1.62385555182175,
5.96652922454154));
#43331=CARTESIAN_POINT('Ctrl Pts',(-1.74067747001173,-1.61106971113231,
5.96532686819106));
#43332=CARTESIAN_POINT('Ctrl Pts',(-1.76018344541345,-1.58968040151759,
5.96335228483598));
#43333=CARTESIAN_POINT('Ctrl Pts',(-1.76784855976269,-1.58115180502976,
5.96257443309881));
#43334=CARTESIAN_POINT('Ctrl Pts',(-1.7834527168597,-1.56353448334302,5.96098753857058));
#43335=CARTESIAN_POINT('Ctrl Pts',(-1.79138476577734,-1.55444019204796,
5.96017896790289));
#43336=CARTESIAN_POINT('Ctrl Pts',(-1.81249444659139,-1.52986121594332,
5.9580206872017));
#43337=CARTESIAN_POINT('Ctrl Pts',(-1.82554326987668,-1.51426658675174,
5.95667971067277));
#43338=CARTESIAN_POINT('Ctrl Pts',(-1.89923366372438,-1.42386203317637,
5.94905412357267));
#43339=CARTESIAN_POINT('Ctrl Pts',(-1.95548155277556,-1.34557337778903,
5.94302230431289));
#43340=CARTESIAN_POINT('Ctrl Pts',(-2.08084801854272,-1.14654397330121,
5.92846612325855));
#43341=CARTESIAN_POINT('Ctrl Pts',(-2.14440897219707,-1.02274206232494,
5.92003520173132));
#43342=CARTESIAN_POINT('Ctrl Pts',(-2.22548945135277,-0.823528089592046,
5.9065595876468));
#43343=CARTESIAN_POINT('Ctrl Pts',(-2.25078946237846,-0.751629507688478,
5.90171672577152));
#43344=CARTESIAN_POINT('Ctrl Pts',(-2.28062770994385,-0.651709605948943,
5.89493693985247));
#43345=CARTESIAN_POINT('Ctrl Pts',(-2.28819089818765,-0.624636268233069,
5.89309534782173));
#43346=CARTESIAN_POINT('Ctrl Pts',(-2.30031694357159,-0.578049574094697,
5.88991520475524));
#43347=CARTESIAN_POINT('Ctrl Pts',(-2.30511703895668,-0.558600704225646,
5.88858427017787));
#43348=CARTESIAN_POINT('Ctrl Pts',(-2.31440630517847,-0.51880217886128,
5.88585291106844));
#43349=CARTESIAN_POINT('Ctrl Pts',(-2.31887478124092,-0.498449544221166,
5.88445196627546));
#43350=CARTESIAN_POINT('Ctrl Pts',(-2.32959051049132,-0.446375715583181,
5.88085574884813));
#43351=CARTESIAN_POINT('Ctrl Pts',(-2.33545821234231,-0.414581703621275,
5.87864891951459));
#43352=CARTESIAN_POINT('Ctrl Pts',(-2.3614719843078,-0.255467243426252,
5.86754402908281));
#43353=CARTESIAN_POINT('Ctrl Pts',(-2.37186176843005,-0.126791202973871,
5.85835348480349));
#43354=CARTESIAN_POINT('Ctrl Pts',(-2.37169928118365,0.0590433526103015,
5.84488022648407));
#43355=CARTESIAN_POINT('Ctrl Pts',(-2.36959688997047,0.11596789586163,5.84072892506888));
#43356=CARTESIAN_POINT('Ctrl Pts',(-2.36545133284689,0.172736951556046,
5.836583843094));
#43357=CARTESIAN_POINT('Ctrl Pts',(-2.36545134983051,0.172736718982988,
5.64123248379855));
#43358=CARTESIAN_POINT('Ctrl Pts',(-2.36578023953226,0.168232913460231,
5.64155645293107));
#43359=CARTESIAN_POINT('Ctrl Pts',(-2.36609628100516,0.163727968708386,
5.64188013254837));
#43360=CARTESIAN_POINT('Ctrl Pts',(-2.36997300544558,0.106111042944931,
5.64601495739026));
#43361=CARTESIAN_POINT('Ctrl Pts',(-2.37175781277497,0.0528904143435972,
5.64978090317875));
#43362=CARTESIAN_POINT('Ctrl Pts',(-2.37174739206271,-0.0178879215464695,
5.6546827610044));
#43363=CARTESIAN_POINT('Ctrl Pts',(-2.37155026538341,-0.0354267308714001,
5.65588871844607));
#43364=CARTESIAN_POINT('Ctrl Pts',(-2.37089929323082,-0.0645711640244984,
5.65787646073038));
#43365=CARTESIAN_POINT('Ctrl Pts',(-2.37055474079148,-0.0761783255766588,
5.65866381833403));
#43366=CARTESIAN_POINT('Ctrl Pts',(-2.36965812363536,-0.100386816681599,
5.66029646047557));
#43367=CARTESIAN_POINT('Ctrl Pts',(-2.36909077150643,-0.112987035396042,
5.66114093693192));
#43368=CARTESIAN_POINT('Ctrl Pts',(-2.36726870980262,-0.147350209519865,
5.66343099269311));
#43369=CARTESIAN_POINT('Ctrl Pts',(-2.36581441562608,-0.169101923713969,
5.66486636017696));
#43370=CARTESIAN_POINT('Ctrl Pts',(-2.36184033382696,-0.218333699791606,
5.66808907103359));
#43371=CARTESIAN_POINT('Ctrl Pts',(-2.35914044609461,-0.245796370245136,
5.66986835907773));
#43372=CARTESIAN_POINT('Ctrl Pts',(-2.34857920697284,-0.336869771363608,
5.67572596145446));
#43373=CARTESIAN_POINT('Ctrl Pts',(-2.33861869041828,-0.400211415621115,
5.67973041794787));
#43374=CARTESIAN_POINT('Ctrl Pts',(-2.28741722256558,-0.65740483951979,
5.69597340927771));
#43375=CARTESIAN_POINT('Ctrl Pts',(-2.22453614031546,-0.846105073321273,
5.70792513214723));
#43376=CARTESIAN_POINT('Ctrl Pts',(-2.12278265817708,-1.05848374713708,
5.72308321076931));
#43377=CARTESIAN_POINT('Ctrl Pts',(-2.10584559360362,-1.0917912580745,5.72551151576248));
#43378=CARTESIAN_POINT('Ctrl Pts',(-2.07755706944244,-1.14431279608638,
5.72943133345789));
#43379=CARTESIAN_POINT('Ctrl Pts',(-2.0667085910341,-1.16379151755075,5.73090553787557));
#43380=CARTESIAN_POINT('Ctrl Pts',(-2.04544631841972,-1.20073340531113,
5.73374242287402));
#43381=CARTESIAN_POINT('Ctrl Pts',(-2.03507937768889,-1.21822134087508,
5.73510335925646));
#43382=CARTESIAN_POINT('Ctrl Pts',(-2.01049313543848,-1.25850594175691,
5.73828157647416));
#43383=CARTESIAN_POINT('Ctrl Pts',(-1.99610896212891,-1.2811981749897,5.74010463891316));
#43384=CARTESIAN_POINT('Ctrl Pts',(-1.94665401431654,-1.35636246888808,
5.74625678965326));
#43385=CARTESIAN_POINT('Ctrl Pts',(-1.90987758691654,-1.40767445204668,
5.75064671376742));
#43386=CARTESIAN_POINT('Ctrl Pts',(-1.81090534128857,-1.53473642310342,
5.7620184417255));
#43387=CARTESIAN_POINT('Ctrl Pts',(-1.74598405672104,-1.60820726509411,
5.76908503403594));
#43388=CARTESIAN_POINT('Ctrl Pts',(-1.57254212223241,-1.78157311921658,
5.78691360739987));
#43389=CARTESIAN_POINT('Ctrl Pts',(-1.45889240237088,-1.87577461744847,
5.79771824808407));
#43390=CARTESIAN_POINT('Ctrl Pts',(-1.31757944812477,-1.9722445697237,5.8096820714659));
#43391=CARTESIAN_POINT('Ctrl Pts',(-1.29772579011068,-1.9853644812301,5.81133147976303));
#43392=CARTESIAN_POINT('Ctrl Pts',(-1.26658234576733,-2.00527819683184,
5.81386652601018));
#43393=CARTESIAN_POINT('Ctrl Pts',(-1.25542832057329,-2.0122801091089,5.81476424061711));
#43394=CARTESIAN_POINT('Ctrl Pts',(-1.23440383249583,-2.02523531532749,
5.81643648125875));
#43395=CARTESIAN_POINT('Ctrl Pts',(-1.22454786762937,-2.03120984382484,
5.81721222245939));
#43396=CARTESIAN_POINT('Ctrl Pts',(-1.2006359027733,-2.04546758464899,5.81907530223929));
#43397=CARTESIAN_POINT('Ctrl Pts',(-1.18653733726933,-2.05367801626033,
5.82015817910857));
#43398=CARTESIAN_POINT('Ctrl Pts',(-1.13485255696043,-2.08306718206789,
5.8240756579843));
#43399=CARTESIAN_POINT('Ctrl Pts',(-1.09677287852343,-2.10336610922076,
5.82686221126415));
#43400=CARTESIAN_POINT('Ctrl Pts',(-0.993262452344374,-2.15496770666979,
5.83423000112154));
#43401=CARTESIAN_POINT('Ctrl Pts',(-0.92691311317928,-2.18432816279766,
5.83873849797822));
#43402=CARTESIAN_POINT('Ctrl Pts',(-0.681791379413475,-2.27961332944921,
5.8549758357128));
#43403=CARTESIAN_POINT('Ctrl Pts',(-0.496615512133596,-2.32698157941617,
5.86652307955466));
#43404=CARTESIAN_POINT('Ctrl Pts',(-0.273401907431081,-2.35619419560885,
5.88105293264485));
#43405=CARTESIAN_POINT('Ctrl Pts',(-0.238937509337316,-2.35993821141071,
5.88331080145762));
#43406=CARTESIAN_POINT('Ctrl Pts',(-0.182737798023221,-2.36479976554458,
5.88702257907744));
#43407=CARTESIAN_POINT('Ctrl Pts',(-0.16104667010228,-2.36637591102542,
5.88846240713598));
#43408=CARTESIAN_POINT('Ctrl Pts',(-0.118840285173875,-2.36885977646934,
5.89127949944095));
#43409=CARTESIAN_POINT('Ctrl Pts',(-0.0983288208485738,-2.36979979159629,
5.89265564526774));
#43410=CARTESIAN_POINT('Ctrl Pts',(-0.049580496321132,-2.37139990353691,
5.89594427208569));
#43411=CARTESIAN_POINT('Ctrl Pts',(-0.0213395146880917,-2.37182213418319,
5.89786381868385));
#43412=CARTESIAN_POINT('Ctrl Pts',(0.0800890165780273,-2.37152699831633,
5.9048126218662));
#43413=CARTESIAN_POINT('Ctrl Pts',(0.153220490005098,-2.36792654937597,
5.90992669463199));
#43414=CARTESIAN_POINT('Ctrl Pts',(0.344371412835014,-2.34962374146219,
5.92356411964682));
#43415=CARTESIAN_POINT('Ctrl Pts',(0.461652738406823,-2.3294196266039,5.93221180444539));
#43416=CARTESIAN_POINT('Ctrl Pts',(0.691479882900604,-2.27178433819866,
5.94946333371919));
#43417=CARTESIAN_POINT('Ctrl Pts',(0.803749709636661,-2.23453358046326,
5.9580418122213));
#43418=CARTESIAN_POINT('Ctrl Pts',(0.932245340392641,-2.18095419918627,
5.96773783947919));
#43419=CARTESIAN_POINT('Ctrl Pts',(0.951597052417868,-2.17258042857045,
5.969194410356));
#43420=CARTESIAN_POINT('Ctrl Pts',(0.982204145092333,-2.15884884725206,
5.97148945065426));
#43421=CARTESIAN_POINT('Ctrl Pts',(0.993532919795582,-2.15365867366831,
5.97233700354946));
#43422=CARTESIAN_POINT('Ctrl Pts',(1.01554654926933,-2.14336265761326,5.97397943526246));
#43423=CARTESIAN_POINT('Ctrl Pts',(1.02623492847852,-2.13826568871588,5.97477474167052));
#43424=CARTESIAN_POINT('Ctrl Pts',(1.05319463069071,-2.12516069872611,5.9767763780805));
#43425=CARTESIAN_POINT('Ctrl Pts',(1.06941353060286,-2.11704550607595,5.97797648681104));
#43426=CARTESIAN_POINT('Ctrl Pts',(1.13809299574232,-2.08169073307758,5.98304770001403));
#43427=CARTESIAN_POINT('Ctrl Pts',(1.1896225859989,-2.05267905187098,5.98682596277798));
#43428=CARTESIAN_POINT('Ctrl Pts',(1.34886869654328,-1.95500813275285,5.99858631979095));
#43429=CARTESIAN_POINT('Ctrl Pts',(1.4521548723051,-1.87956196080577,6.00635029065062));
#43430=CARTESIAN_POINT('Ctrl Pts',(1.6393249270639,-1.71816137194626,6.02160326949658));
#43431=CARTESIAN_POINT('Ctrl Pts',(1.72374965589472,-1.6334463780326,6.02905635080786));
#43432=CARTESIAN_POINT('Ctrl Pts',(1.82260905504624,-1.51801001942559,6.03888845338173));
#43433=CARTESIAN_POINT('Ctrl Pts',(1.84327554027202,-1.4928473819201,6.04101314710745));
#43434=CARTESIAN_POINT('Ctrl Pts',(1.87660997110012,-1.45051297104119,6.04456308041927));
#43435=CARTESIAN_POINT('Ctrl Pts',(1.88957624011359,-1.43358098713145,6.04597658301143));
#43436=CARTESIAN_POINT('Ctrl Pts',(1.91472281446972,-1.39980942889336,6.04878491875366));
#43437=CARTESIAN_POINT('Ctrl Pts',(1.92691361402352,-1.38298003281408,6.05017918180063));
#43438=CARTESIAN_POINT('Ctrl Pts',(1.95598218358289,-1.34172030039274,6.05358610134248));
#43439=CARTESIAN_POINT('Ctrl Pts',(1.97262498039105,-1.31712953724282,6.05560722078294));
#43440=CARTESIAN_POINT('Ctrl Pts',(2.03562316987075,-1.22017271995127,6.06354366745498));
#43441=CARTESIAN_POINT('Ctrl Pts',(2.07848883169563,-1.14562836532599,6.06957977513489));
#43442=CARTESIAN_POINT('Ctrl Pts',(2.20075018980182,-0.903467327831151,
6.08896743849208));
#43443=CARTESIAN_POINT('Ctrl Pts',(2.2645975261339,-0.728797575729085,6.10268820066702));
#43444=CARTESIAN_POINT('Ctrl Pts',(2.31765368782206,-0.505591909030072,
6.1190323471743));
#43445=CARTESIAN_POINT('Ctrl Pts',(2.32665210039277,-0.462420106924175,
6.12213736251942));
#43446=CARTESIAN_POINT('Ctrl Pts',(2.33742399838102,-0.402407704592652,
6.12635494040289));
#43447=CARTESIAN_POINT('Ctrl Pts',(2.34022845188182,-0.385763842731493,
6.12751423091057));
#43448=CARTESIAN_POINT('Ctrl Pts',(2.34466216184429,-0.357620259491832,
6.12945540294883));
#43449=CARTESIAN_POINT('Ctrl Pts',(2.34638502772495,-0.346136141516994,
6.13024213465479));
#43450=CARTESIAN_POINT('Ctrl Pts',(2.34984485052009,-0.321860009875625,
6.13189338091179));
#43451=CARTESIAN_POINT('Ctrl Pts',(2.35156183072193,-0.309065790492221,
6.13275684437723));
#43452=CARTESIAN_POINT('Ctrl Pts',(2.35607302652082,-0.273233386574049,
6.13515774469181));
#43453=CARTESIAN_POINT('Ctrl Pts',(2.35863378989579,-0.250166607445443,
6.13668325287829));
#43454=CARTESIAN_POINT('Ctrl Pts',(2.36372520486561,-0.197229787110296,
6.14014593105574));
#43455=CARTESIAN_POINT('Ctrl Pts',(2.36602903818142,-0.167341531977288,
6.14207316375314));
#43456=CARTESIAN_POINT('Ctrl Pts',(2.3720253511006,-0.0640214471063062,
6.1486638558142));
#43457=CARTESIAN_POINT('Ctrl Pts',(2.37287029338955,0.0095365984689538,
6.15323237955966));
#43458=CARTESIAN_POINT('Ctrl Pts',(2.36370367440257,0.271254507750847,6.16939603012114));
#43459=CARTESIAN_POINT('Ctrl Pts',(2.33471398869007,0.458015739130436,6.18082237169589));
#43460=CARTESIAN_POINT('Ctrl Pts',(2.27451404202174,0.673058116066307,6.19523085799782));
#43461=CARTESIAN_POINT('Ctrl Pts',(2.26434185218677,0.706524685358358,6.19750839231698));
#43462=CARTESIAN_POINT('Ctrl Pts',(2.2466309445949,0.760475625057775,6.20124413888627));
#43463=CARTESIAN_POINT('Ctrl Pts',(2.23954275452551,0.781103050839649,6.20268791127723));
#43464=CARTESIAN_POINT('Ctrl Pts',(2.22524124113493,0.820926233492554,6.20550687672391));
#43465=CARTESIAN_POINT('Ctrl Pts',(2.21806145041506,0.840132025201788,6.20688087539652));
#43466=CARTESIAN_POINT('Ctrl Pts',(2.20046784449994,0.885396371048065,6.21015475619988));
#43467=CARTESIAN_POINT('Ctrl Pts',(2.18983897349617,0.911367447255657,6.21206153180158));
#43468=CARTESIAN_POINT('Ctrl Pts',(2.15039853163296,1.00306205236417,6.21889821077395));
#43469=CARTESIAN_POINT('Ctrl Pts',(2.11907061418222,1.06765409603407,6.22390929128145));
#43470=CARTESIAN_POINT('Ctrl Pts',(2.02643388872319,1.2384610813929,6.2376982681088));
#43471=CARTESIAN_POINT('Ctrl Pts',(1.95974261250118,1.3415007431432,6.24661906463699));
#43472=CARTESIAN_POINT('Ctrl Pts',(1.8201674945745,1.5243844138546,6.2633680955525));
#43473=CARTESIAN_POINT('Ctrl Pts',(1.74919737943121,1.60532551075475,6.2711738241074));
#43474=CARTESIAN_POINT('Ctrl Pts',(1.6546643992218,1.6993972515994,6.28052183685177));
#43475=CARTESIAN_POINT('Ctrl Pts',(1.63605729532713,1.71731824382338,6.28231603270985));
#43476=CARTESIAN_POINT('Ctrl Pts',(1.60721113372758,1.74420624372959,6.28502379709278));
#43477=CARTESIAN_POINT('Ctrl Pts',(1.59718214650736,1.75339449700382,6.2859520226483));
#43478=CARTESIAN_POINT('Ctrl Pts',(1.57865939725611,1.77007367058003,6.28764151114012));
#43479=CARTESIAN_POINT('Ctrl Pts',(1.57019055350955,1.77759048295065,6.28840453490789));
#43480=CARTESIAN_POINT('Ctrl Pts',(1.55001067157273,1.79524507238569,6.29020096571449));
#43481=CARTESIAN_POINT('Ctrl Pts',(1.53825368606332,1.80532921670585,6.29123062253935));
#43482=CARTESIAN_POINT('Ctrl Pts',(1.49774405497266,1.83939185665732,6.29472429450027));
#43483=CARTESIAN_POINT('Ctrl Pts',(1.46852141247816,1.86280564631288,6.29715284943029));
#43484=CARTESIAN_POINT('Ctrl Pts',(1.39238493534334,1.92090196670928,6.30328552197746));
#43485=CARTESIAN_POINT('Ctrl Pts',(1.34472263082007,1.95456441453259,6.30694355982376));
#43486=CARTESIAN_POINT('Ctrl Pts',(1.13865851763053,2.08899165612909,6.32222644741322));
#43487=CARTESIAN_POINT('Ctrl Pts',(0.969842481153402,2.17251792697489,6.33352967809068));
#43488=CARTESIAN_POINT('Ctrl Pts',(0.746912031149507,2.25160081181676,6.34860470527262));
#43489=CARTESIAN_POINT('Ctrl Pts',(0.700387945400513,2.26650391863106,6.35175428550142));
#43490=CARTESIAN_POINT('Ctrl Pts',(0.629868117452508,2.28671499231276,6.35655273269274));
#43491=CARTESIAN_POINT('Ctrl Pts',(0.606194315205028,2.29310437635411,6.35816758295036));
#43492=CARTESIAN_POINT('Ctrl Pts',(0.562920112567481,2.30406682250814,6.36112884622699));
#43493=CARTESIAN_POINT('Ctrl Pts',(0.543352245829095,2.30875968236557,6.36247134559364));
#43494=CARTESIAN_POINT('Ctrl Pts',(0.500507481816747,2.31846007770791,6.36541948990815));
#43495=CARTESIAN_POINT('Ctrl Pts',(0.477210342804884,2.32336718791008,6.367028119285));
#43496=CARTESIAN_POINT('Ctrl Pts',(0.409660330319795,2.33653651174923,6.37171015517303));
#43497=CARTESIAN_POINT('Ctrl Pts',(0.365243127551471,2.34389023856262,6.37481097677845));
#43498=CARTESIAN_POINT('Ctrl Pts',(0.0987837685891144,2.38024769832461,
6.39355490890545));
#43499=CARTESIAN_POINT('Ctrl Pts',(-0.126231365591026,2.37894307121585,
6.41011984683565));
#43500=CARTESIAN_POINT('Ctrl Pts',(-0.405926009450226,2.33749691633769,
6.43043225221606));
#43501=CARTESIAN_POINT('Ctrl Pts',(-0.463857150945083,2.32669410936557,
6.43461410323573));
#43502=CARTESIAN_POINT('Ctrl Pts',(-0.53946059936844,2.30965922075857,6.43999100972916));
#43503=CARTESIAN_POINT('Ctrl Pts',(-0.557542855714967,2.30536102839415,
6.44127082646511));
#43504=CARTESIAN_POINT('Ctrl Pts',(-0.586004036519302,2.29824127069845,
6.4432735024244));
#43505=CARTESIAN_POINT('Ctrl Pts',(-0.596417069123826,2.29556101207306,
6.4440037214249));
#43506=CARTESIAN_POINT('Ctrl Pts',(-0.618410323064428,2.28974030932096,
6.44554020519186));
#43507=CARTESIAN_POINT('Ctrl Pts',(-0.629985659677364,2.2865826231699,6.44634542696884));
#43508=CARTESIAN_POINT('Ctrl Pts',(-0.659742191036129,2.27822209291788,
6.4484076679363));
#43509=CARTESIAN_POINT('Ctrl Pts',(-0.677886469452383,2.27288927414737,
6.44965766974099));
#43510=CARTESIAN_POINT('Ctrl Pts',(-0.761123500867893,2.24733945605914,
6.45536584572576));
#43511=CARTESIAN_POINT('Ctrl Pts',(-0.825395227103285,2.22453772459901,
6.45969956387093));
#43512=CARTESIAN_POINT('Ctrl Pts',(-1.05685522379626,2.13100617379443,6.47533223031337));
#43513=CARTESIAN_POINT('Ctrl Pts',(-1.21675038561398,2.04393069876013,6.48622809597149));
#43514=CARTESIAN_POINT('Ctrl Pts',(-1.41897166053197,1.90159103785509,6.50180018988613));
#43515=CARTESIAN_POINT('Ctrl Pts',(-1.47118327011399,1.86149071875855,6.50600114561125));
#43516=CARTESIAN_POINT('Ctrl Pts',(-1.54088922189402,1.80318803933655,6.51191467227363));
#43517=CARTESIAN_POINT('Ctrl Pts',(-1.55986453326166,1.78679860672471,6.51355747045079));
#43518=CARTESIAN_POINT('Ctrl Pts',(-1.59394938573373,1.75640192619069,6.51657187867528));
#43519=CARTESIAN_POINT('Ctrl Pts',(-1.60914319962626,1.74249260813757,6.51793945006947));
#43520=CARTESIAN_POINT('Ctrl Pts',(-1.63963690349021,1.7138378900879,6.52073442165589));
#43521=CARTESIAN_POINT('Ctrl Pts',(-1.65492362770187,1.69908128869193,6.52216221998327));
#43522=CARTESIAN_POINT('Ctrl Pts',(-1.69284366259746,1.66147900421524,6.52577315716763));
#43523=CARTESIAN_POINT('Ctrl Pts',(-1.71521383316145,1.63837525670508,6.52796727161902));
#43524=CARTESIAN_POINT('Ctrl Pts',(-1.81766149058534,1.52816980820141,6.53832586627115));
#43525=CARTESIAN_POINT('Ctrl Pts',(-1.8916079551903,1.43562124678482,6.54673204854011));
#43526=CARTESIAN_POINT('Ctrl Pts',(-2.05124613376433,1.20196260382582,6.56719200454078));
#43527=CARTESIAN_POINT('Ctrl Pts',(-2.12974029781669,1.05666139043118,6.57934505506317));
#43528=CARTESIAN_POINT('Ctrl Pts',(-2.20370183449107,0.877355121311782,
6.59302765788477));
#43529=CARTESIAN_POINT('Ctrl Pts',(-2.21435584019639,0.850107155447432,
6.5950721369387));
#43530=CARTESIAN_POINT('Ctrl Pts',(-2.22946695725954,0.809246509110479,
6.5980797211005));
#43531=CARTESIAN_POINT('Ctrl Pts',(-2.23430897500204,0.795780280657911,
6.59906161154154));
#43532=CARTESIAN_POINT('Ctrl Pts',(-2.24283046609485,0.771389917398216,
6.60082227597204));
#43533=CARTESIAN_POINT('Ctrl Pts',(-2.24655273910661,0.760481240816587,
6.60160335985199));
#43534=CARTESIAN_POINT('Ctrl Pts',(-2.25423928076437,0.737405621940138,
6.60324168706354));
#43535=CARTESIAN_POINT('Ctrl Pts',(-2.2581848446999,0.725233074271705,6.60409790349739));
#43536=CARTESIAN_POINT('Ctrl Pts',(-2.26884603345972,0.691411233443826,
6.60645632720292));
#43537=CARTESIAN_POINT('Ctrl Pts',(-2.27535031370248,0.669696093468538,
6.60794727717495));
#43538=CARTESIAN_POINT('Ctrl Pts',(-2.28947863487125,0.619943263563181,
6.61131748002293));
#43539=CARTESIAN_POINT('Ctrl Pts',(-2.29690091104665,0.591851692970257,
6.61318754583698));
#43540=CARTESIAN_POINT('Ctrl Pts',(-2.33523019469976,0.435182823143709,
6.62347137079951));
#43541=CARTESIAN_POINT('Ctrl Pts',(-2.35583463309604,0.304427903160431,
6.63152390776219));
#43542=CARTESIAN_POINT('Ctrl Pts',(-2.36545136499509,0.172736511319546,
6.63965300722759));
#43543=CARTESIAN_POINT('Origin',(0.,0.,-1.84858989190501));
#43544=CARTESIAN_POINT('',(-2.36545134965667,0.17273672136364,7.83525515262476));
#43545=CARTESIAN_POINT('',(-2.36545135498545,0.17273664839138,7.63805096494753));
#43546=CARTESIAN_POINT('',(-2.36545134966535,0.172736721244682,-1.84858989190501));
#43547=CARTESIAN_POINT('',(-2.37174965797748,-0.00127372827735513,6.85023264105921));
#43548=CARTESIAN_POINT('Ctrl Pts',(-2.36545134965667,0.17273672136364,7.83525515262476));
#43549=CARTESIAN_POINT('Ctrl Pts',(-2.36502652455963,0.178554263176551,
7.83488542092976));
#43550=CARTESIAN_POINT('Ctrl Pts',(-2.36458022850928,0.18437036980467,7.83451633788331));
#43551=CARTESIAN_POINT('Ctrl Pts',(-2.35550714366389,0.297154247534622,
7.82736904092432));
#43552=CARTESIAN_POINT('Ctrl Pts',(-2.33965115124067,0.40342258231143,7.82080147884784));
#43553=CARTESIAN_POINT('Ctrl Pts',(-2.28759914925481,0.640677282685825,
7.80586554411087));
#43554=CARTESIAN_POINT('Ctrl Pts',(-2.24725031471078,0.770349262957642,
7.79749654101737));
#43555=CARTESIAN_POINT('Ctrl Pts',(-2.18176354461517,0.930879425497304,
7.78634965453539));
#43556=CARTESIAN_POINT('Ctrl Pts',(-2.16664185855844,0.965552420234006,
7.78389396821056));
#43557=CARTESIAN_POINT('Ctrl Pts',(-2.14135567965776,1.01994365098656,7.77995616145276));
#43558=CARTESIAN_POINT('Ctrl Pts',(-2.13173219075743,1.03990721237562,7.77849213719076));
#43559=CARTESIAN_POINT('Ctrl Pts',(-2.11307879457354,1.07725564628182,7.77571614500148));
#43560=CARTESIAN_POINT('Ctrl Pts',(-2.10411045567512,1.09466929757376,7.77440637293124));
#43561=CARTESIAN_POINT('Ctrl Pts',(-2.08321827336733,1.13402974176567,7.77140941538428));
#43562=CARTESIAN_POINT('Ctrl Pts',(-2.07116153442144,1.15590295733346,7.76971772650803));
#43563=CARTESIAN_POINT('Ctrl Pts',(-2.03192983396312,1.2244916439511,7.76432721529079));
#43564=CARTESIAN_POINT('Ctrl Pts',(-2.00350414842023,1.2704680119567,7.7605852442756));
#43565=CARTESIAN_POINT('Ctrl Pts',(-1.93053267203484,1.37994681545583,7.7513511037216));
#43566=CARTESIAN_POINT('Ctrl Pts',(-1.88439616626324,1.44231025367349,7.74580982055011));
#43567=CARTESIAN_POINT('Ctrl Pts',(-1.73778474911568,1.62141906489628,7.72908408716959));
#43568=CARTESIAN_POINT('Ctrl Pts',(-1.62891287360248,1.73076254010812,7.71773699370195));
#43569=CARTESIAN_POINT('Ctrl Pts',(-1.47771302094563,1.85562357425548,7.70378464303611));
#43570=CARTESIAN_POINT('Ctrl Pts',(-1.44450099422281,1.88159294108815,7.70081955550987));
#43571=CARTESIAN_POINT('Ctrl Pts',(-1.39748614446874,1.91637604276122,7.69677637242602));
#43572=CARTESIAN_POINT('Ctrl Pts',(-1.38425969005128,1.92595166310529,7.69565527838919));
#43573=CARTESIAN_POINT('Ctrl Pts',(-1.36174978660769,1.94189656793928,7.69377614437337));
#43574=CARTESIAN_POINT('Ctrl Pts',(-1.35251812426689,1.94833762654464,7.69301355595475));
#43575=CARTESIAN_POINT('Ctrl Pts',(-1.33295763944737,1.96177920802411,7.69141513230602));
#43576=CARTESIAN_POINT('Ctrl Pts',(-1.32261892901348,1.96876431183186,7.69058025965388));
#43577=CARTESIAN_POINT('Ctrl Pts',(-1.29367996658551,1.98798537743181,7.68826956531754));
#43578=CARTESIAN_POINT('Ctrl Pts',(-1.27496131501434,2.00004186161467,7.68680471895894));
#43579=CARTESIAN_POINT('Ctrl Pts',(-1.23183460711029,2.02696773499214,7.68349049866248));
#43580=CARTESIAN_POINT('Ctrl Pts',(-1.20732170416249,2.04166332849617,7.68165011538188));
#43581=CARTESIAN_POINT('Ctrl Pts',(-1.12301494123781,2.09015604542276,7.67544574871097));
#43582=CARTESIAN_POINT('Ctrl Pts',(-1.06201855043906,2.12179938929066,7.67116656782923));
#43583=CARTESIAN_POINT('Ctrl Pts',(-0.839718853935663,2.22513064609199,
7.65601442700783));
#43584=CARTESIAN_POINT('Ctrl Pts',(-0.671917555688727,2.28141571668127,
7.64533474098238));
#43585=CARTESIAN_POINT('Ctrl Pts',(-0.454635120436417,2.32821918001872,
7.63114425278071));
#43586=CARTESIAN_POINT('Ctrl Pts',(-0.409573633211008,2.33656728002393,
7.62818576568138));
#43587=CARTESIAN_POINT('Ctrl Pts',(-0.340779987955371,2.34726088445391,
7.62362989651485));
#43588=CARTESIAN_POINT('Ctrl Pts',(-0.317206170593052,2.35056266419589,
7.6220618304207));
#43589=CARTESIAN_POINT('Ctrl Pts',(-0.274228745217447,2.35592386214044,
7.61918860047817));
#43590=CARTESIAN_POINT('Ctrl Pts',(-0.254841606014832,2.35809973635284,
7.61788715058258));
#43591=CARTESIAN_POINT('Ctrl Pts',(-0.212524061570712,2.36232121086805,
7.61503374652679));
#43592=CARTESIAN_POINT('Ctrl Pts',(-0.189586479206702,2.36427259074841,
7.61347902896167));
#43593=CARTESIAN_POINT('Ctrl Pts',(-0.123543484042322,2.36892386445819,
7.6089777725126));
#43594=CARTESIAN_POINT('Ctrl Pts',(-0.0803898966371576,2.3707805297001,
7.60600604212888));
#43595=CARTESIAN_POINT('Ctrl Pts',(0.0951811649743621,2.3735355199686,7.59378483158364));
#43596=CARTESIAN_POINT('Ctrl Pts',(0.227498054114296,2.36452238703567,7.58425457583065));
#43597=CARTESIAN_POINT('Ctrl Pts',(0.500002728637081,2.32287071039141,7.56419731460912));
#43598=CARTESIAN_POINT('Ctrl Pts',(0.639407217365449,2.2884264054405,7.55369336343553));
#43599=CARTESIAN_POINT('Ctrl Pts',(0.797386034651848,2.23381775534014,7.54200242891027));
#43600=CARTESIAN_POINT('Ctrl Pts',(0.819797161344559,2.22569067304343,7.54034966757875));
#43601=CARTESIAN_POINT('Ctrl Pts',(0.854184397856357,2.21263070689497,7.53782653875786));
#43602=CARTESIAN_POINT('Ctrl Pts',(0.866248355835281,2.2079355597409,7.5369438273306));
#43603=CARTESIAN_POINT('Ctrl Pts',(0.888600472627781,2.19902497811122,7.53531372767464));
#43604=CARTESIAN_POINT('Ctrl Pts',(0.898897885530266,2.19483581427227,7.53456499503793));
#43605=CARTESIAN_POINT('Ctrl Pts',(0.923367744427714,2.18467995360969,7.53279059130465));
#43606=CARTESIAN_POINT('Ctrl Pts',(0.937512212813359,2.17864760178998,7.53176872099825));
#43607=CARTESIAN_POINT('Ctrl Pts',(0.986862817021009,2.15703085268392,7.52821335089255));
#43608=CARTESIAN_POINT('Ctrl Pts',(1.02174915284601,2.14072636644534,7.5257179311656));
#43609=CARTESIAN_POINT('Ctrl Pts',(1.11110614338163,2.09628199944897,7.51933411173979));
#43610=CARTESIAN_POINT('Ctrl Pts',(1.16491179486983,2.06686635498482,7.51549765071626));
#43611=CARTESIAN_POINT('Ctrl Pts',(1.39513820214338,1.92915106693704,7.4988621003276));
#43612=CARTESIAN_POINT('Ctrl Pts',(1.55807184632938,1.80012315219386,7.486414631567));
#43613=CARTESIAN_POINT('Ctrl Pts',(1.72680459033591,1.62622055048095,7.47079111774733));
#43614=CARTESIAN_POINT('Ctrl Pts',(1.75084654811235,1.60030732363766,7.46849083972407));
#43615=CARTESIAN_POINT('Ctrl Pts',(1.78853420159905,1.55782014943282,7.46475610930128));
#43616=CARTESIAN_POINT('Ctrl Pts',(1.80255009508627,1.54158078389952,7.46333691732641));
#43617=CARTESIAN_POINT('Ctrl Pts',(1.82904653956851,1.5100255156513,7.46059354316046));
#43618=CARTESIAN_POINT('Ctrl Pts',(1.84155981555945,1.49473934438962,7.45927082961816));
#43619=CARTESIAN_POINT('Ctrl Pts',(1.87032128859955,1.45869502252313,7.45616527904333));
#43620=CARTESIAN_POINT('Ctrl Pts',(1.88641698018401,1.43781910290772,7.45437670669));
#43621=CARTESIAN_POINT('Ctrl Pts',(1.93973224032869,1.36623327951279,7.44827465914509));
#43622=CARTESIAN_POINT('Ctrl Pts',(1.97527871842204,1.31431628266825,7.44390009380195));
#43623=CARTESIAN_POINT('Ctrl Pts',(2.06089650031195,1.17793654025632,7.43253206979626));
#43624=CARTESIAN_POINT('Ctrl Pts',(2.10786203055443,1.09166999551216,7.42545220692885));
#43625=CARTESIAN_POINT('Ctrl Pts',(2.21220364138674,0.868018848592198,7.4075054997557));
#43626=CARTESIAN_POINT('Ctrl Pts',(2.2622573509093,0.727667117731736,7.39659262622969));
#43627=CARTESIAN_POINT('Ctrl Pts',(2.30461273177817,0.560810456796328,7.38455785794993));
#43628=CARTESIAN_POINT('Ctrl Pts',(2.31004636646847,0.537990796917997,7.38293218271559));
#43629=CARTESIAN_POINT('Ctrl Pts',(2.31793436907612,0.502537340288836,7.38044145371097));
#43630=CARTESIAN_POINT('Ctrl Pts',(2.32062581485954,0.489958533062745,7.3795645204982));
#43631=CARTESIAN_POINT('Ctrl Pts',(2.3254561461057,0.466450191074961,7.37793901921239));
#43632=CARTESIAN_POINT('Ctrl Pts',(2.32762049887429,0.455527043098023,7.37718919129556));
#43633=CARTESIAN_POINT('Ctrl Pts',(2.33261762788357,0.42934135973239,7.37540413838447));
#43634=CARTESIAN_POINT('Ctrl Pts',(2.33537763532172,0.414065614550607,7.37437284979324));
#43635=CARTESIAN_POINT('Ctrl Pts',(2.3446283891367,0.359827566007707,7.37074316731238));
#43636=CARTESIAN_POINT('Ctrl Pts',(2.35029600013696,0.320729306923126,7.36818500186079));
#43637=CARTESIAN_POINT('Ctrl Pts',(2.36254740546877,0.218237873021053,7.3615884837741));
#43638=CARTESIAN_POINT('Ctrl Pts',(2.36755799393233,0.154687352375816,7.35760649938418));
#43639=CARTESIAN_POINT('Ctrl Pts',(2.37770207794855,-0.109480267277751,
7.34123238647913));
#43640=CARTESIAN_POINT('Ctrl Pts',(2.35993123053883,-0.310119249543331,
7.32914322231165));
#43641=CARTESIAN_POINT('Ctrl Pts',(2.30928631048834,-0.541979388920817,
7.31386149591503));
#43642=CARTESIAN_POINT('Ctrl Pts',(2.30062394135968,-0.577645368834535,
7.31147565560392));
#43643=CARTESIAN_POINT('Ctrl Pts',(2.28552141397073,-0.63408360184742,7.30763631237744));
#43644=CARTESIAN_POINT('Ctrl Pts',(2.2796168797703,-0.654993876142164,7.30619969757301));
#43645=CARTESIAN_POINT('Ctrl Pts',(2.26781986744159,-0.694678487705738,
7.30344467837641));
#43646=CARTESIAN_POINT('Ctrl Pts',(2.26197937924298,-0.713466468001206,
7.30212803471927));
#43647=CARTESIAN_POINT('Ctrl Pts',(2.24795348540473,-0.756681435072762,
7.29906994611166));
#43648=CARTESIAN_POINT('Ctrl Pts',(2.23960261226199,-0.781051673525601,
7.2973233018715));
#43649=CARTESIAN_POINT('Ctrl Pts',(2.21085153094412,-0.860700394717117,
7.29153942721779));
#43650=CARTESIAN_POINT('Ctrl Pts',(2.1887897464905,-0.915351346143952,7.28744953641931));
#43651=CARTESIAN_POINT('Ctrl Pts',(2.12858840463606,-1.04982267197795,7.27707473340755));
#43652=CARTESIAN_POINT('Ctrl Pts',(2.08797742180165,-1.12843432337487,7.27072234248427));
#43653=CARTESIAN_POINT('Ctrl Pts',(1.97214517912684,-1.32489475388003,7.25417675618632));
#43654=CARTESIAN_POINT('Ctrl Pts',(1.89072500883904,-1.43870216521157,7.2439116346261));
#43655=CARTESIAN_POINT('Ctrl Pts',(1.77406184532892,-1.57463003708838,7.2311918316787));
#43656=CARTESIAN_POINT('Ctrl Pts',(1.74761680341099,-1.60392989561684,7.22842079782599));
#43657=CARTESIAN_POINT('Ctrl Pts',(1.70950746875328,-1.64409094963024,7.2245963900735));
#43658=CARTESIAN_POINT('Ctrl Pts',(1.69844766447122,-1.65551393882935,7.22350552779009));
#43659=CARTESIAN_POINT('Ctrl Pts',(1.67941050553304,-1.67478464129566,7.22166123813357));
#43660=CARTESIAN_POINT('Ctrl Pts',(1.67149111330934,-1.68268853921893,7.2209036587945));
#43661=CARTESIAN_POINT('Ctrl Pts',(1.65448497387235,-1.69942285885851,7.21929761758497));
#43662=CARTESIAN_POINT('Ctrl Pts',(1.64538299935255,-1.70823692311428,7.21845033289346));
#43663=CARTESIAN_POINT('Ctrl Pts',(1.61942281726809,-1.73297592829163,7.21606675039528));
#43664=CARTESIAN_POINT('Ctrl Pts',(1.60240057334283,-1.74872763121118,7.21454257657119));
#43665=CARTESIAN_POINT('Ctrl Pts',(1.48916451222402,-1.85046962749401,7.20463260142641));
#43666=CARTESIAN_POINT('Ctrl Pts',(1.38628928050044,-1.92874545377028,7.19668854330215));
#43667=CARTESIAN_POINT('Ctrl Pts',(1.14495016434149,-2.08303973603129,7.179073930088));
#43668=CARTESIAN_POINT('Ctrl Pts',(1.00426198499473,-2.15439482266694,7.16943299927251));
#43669=CARTESIAN_POINT('Ctrl Pts',(0.822214251241414,-2.22499399662373,
7.15687471378871));
#43670=CARTESIAN_POINT('Ctrl Pts',(0.786555542845042,-2.23784822674097,
7.1544130174151));
#43671=CARTESIAN_POINT('Ctrl Pts',(0.729763237336152,-2.2567956129927,7.15048090220939));
#43672=CARTESIAN_POINT('Ctrl Pts',(0.708825789978955,-2.26345902716322,
7.14902887132021));
#43673=CARTESIAN_POINT('Ctrl Pts',(0.669022042889277,-2.27552027687866,
7.14626240193886));
#43674=CARTESIAN_POINT('Ctrl Pts',(0.650175345426807,-2.28097676567459,
7.14494997195391));
#43675=CARTESIAN_POINT('Ctrl Pts',(0.60687759104082,-2.29293211152929,7.14192801984534));
#43676=CARTESIAN_POINT('Ctrl Pts',(0.582386263141423,-2.29927471926238,
7.1402137085369));
#43677=CARTESIAN_POINT('Ctrl Pts',(0.503362477921157,-2.31839623701822,
7.13466426577325));
#43678=CARTESIAN_POINT('Ctrl Pts',(0.44848069450325,-2.3296349675031,7.13078226199609));
#43679=CARTESIAN_POINT('Ctrl Pts',(0.312590049861713,-2.3524830526908,7.12109774144653));
#43680=CARTESIAN_POINT('Ctrl Pts',(0.231283038478646,-2.36186263858594,
7.11523927237148));
#43681=CARTESIAN_POINT('Ctrl Pts',(-0.0238050714686189,-2.3779911496083,
7.09673771199558));
#43682=CARTESIAN_POINT('Ctrl Pts',(-0.1979536189631,-2.36985809530594,7.08389502069377));
#43683=CARTESIAN_POINT('Ctrl Pts',(-0.39339543047754,-2.33902026264831,
7.07005285486293));
#43684=CARTESIAN_POINT('Ctrl Pts',(-0.417079734285967,-2.33491335106683,
7.06838599657265));
#43685=CARTESIAN_POINT('Ctrl Pts',(-0.4534596149512,-2.32803374274299,7.06584602458951));
#43686=CARTESIAN_POINT('Ctrl Pts',(-0.466200978853671,-2.32551572700607,
7.06496032236766));
#43687=CARTESIAN_POINT('Ctrl Pts',(-0.488706542044473,-2.32087565323569,
7.06340349336342));
#43688=CARTESIAN_POINT('Ctrl Pts',(-0.498478558587589,-2.31879645804281,
7.06273013286214));
#43689=CARTESIAN_POINT('Ctrl Pts',(-0.52247188885008,-2.31353269949699,
7.06108294523542));
#43690=CARTESIAN_POINT('Ctrl Pts',(-0.536677441331674,-2.3102787227508,
7.0601129327441));
#43691=CARTESIAN_POINT('Ctrl Pts',(-0.58332129217467,-2.29914085311653,
7.05694242168998));
#43692=CARTESIAN_POINT('Ctrl Pts',(-0.615624681335829,-2.29070271038756,
7.05476986066242));
#43693=CARTESIAN_POINT('Ctrl Pts',(-0.695569750735475,-2.2680063381689,
7.04942670692641));
#43694=CARTESIAN_POINT('Ctrl Pts',(-0.742962582434193,-2.25292636570427,
7.0462891462356));
#43695=CARTESIAN_POINT('Ctrl Pts',(-0.902053865927786,-2.19673787518309,
7.03575278108852));
#43696=CARTESIAN_POINT('Ctrl Pts',(-1.01112019036126,-2.14871967439778,
7.02851515494955));
#43697=CARTESIAN_POINT('Ctrl Pts',(-1.2162681898329,-2.03930654329121,7.01415073348884));
#43698=CARTESIAN_POINT('Ctrl Pts',(-1.31243809561989,-1.97878280750758,
7.00705239116125));
#43699=CARTESIAN_POINT('Ctrl Pts',(-1.42954271130414,-1.89278046901822,
6.99764872658452));
#43700=CARTESIAN_POINT('Ctrl Pts',(-1.4548029416123,-1.87343495083563,6.99557194117343));
#43701=CARTESIAN_POINT('Ctrl Pts',(-1.49586970238984,-1.84065254625775,
6.99210959383941));
#43702=CARTESIAN_POINT('Ctrl Pts',(-1.5119031578588,-1.82750561113263,6.99073535058864));
#43703=CARTESIAN_POINT('Ctrl Pts',(-1.54313467557989,-1.80120441992518,
6.98801249400454));
#43704=CARTESIAN_POINT('Ctrl Pts',(-1.55834198242689,-1.78806381682842,
6.98666449887356));
#43705=CARTESIAN_POINT('Ctrl Pts',(-1.59469381131914,-1.75583627649624,
6.98338692998539));
#43706=CARTESIAN_POINT('Ctrl Pts',(-1.61566460230753,-1.73655899818807,
6.98144966235478));
#43707=CARTESIAN_POINT('Ctrl Pts',(-1.69379104523058,-1.66210141715531,
6.97405011895024));
#43708=CARTESIAN_POINT('Ctrl Pts',(-1.74850357869881,-1.60444447094203,
6.96848520026739));
#43709=CARTESIAN_POINT('Ctrl Pts',(-1.89926682210155,-1.4286809857887,6.95198649834393));
#43710=CARTESIAN_POINT('Ctrl Pts',(-1.98697214206719,-1.3039474333246,6.94081496752217));
#43711=CARTESIAN_POINT('Ctrl Pts',(-2.10167674345068,-1.10207271876522,
6.92400195498985));
#43712=CARTESIAN_POINT('Ctrl Pts',(-2.13768650193864,-1.03048936230543,
6.91826418302858));
#43713=CARTESIAN_POINT('Ctrl Pts',(-2.17797508272193,-0.939155061384799,
6.91132318639994));
#43714=CARTESIAN_POINT('Ctrl Pts',(-2.18571610268048,-0.920995587069111,
6.90996133191355));
#43715=CARTESIAN_POINT('Ctrl Pts',(-2.19777437034843,-0.891699747116969,
6.90779569794099));
#43716=CARTESIAN_POINT('Ctrl Pts',(-2.20223561929945,-0.880624161910472,
6.90698407590782));
#43717=CARTESIAN_POINT('Ctrl Pts',(-2.21084994231891,-0.858763150688833,
6.90539671412672));
#43718=CARTESIAN_POINT('Ctrl Pts',(-2.21500815750429,-0.847980240364823,
6.90462072703593));
#43719=CARTESIAN_POINT('Ctrl Pts',(-2.22541634180217,-0.820391161040172,
6.90265201305297));
#43720=CARTESIAN_POINT('Ctrl Pts',(-2.23155500676116,-0.803543309651698,
6.90146550077109));
#43721=CARTESIAN_POINT('Ctrl Pts',(-2.25753518886798,-0.729644591788346,
6.89632288177082));
#43722=CARTESIAN_POINT('Ctrl Pts',(-2.27538590249599,-0.671912676666023,
6.89246473897535));
#43723=CARTESIAN_POINT('Ctrl Pts',(-2.34449771414989,-0.413850179482464,
6.87566109412968));
#43724=CARTESIAN_POINT('Ctrl Pts',(-2.37163862822805,-0.208017014815944,
6.86333732876224));
#43725=CARTESIAN_POINT('Ctrl Pts',(-2.37174965797748,-0.00127372827735513,
6.85023264105921));
#43726=CARTESIAN_POINT('Ctrl Pts',(-2.37174965943354,-0.00127101411488308,
6.85023246901852));
#43727=CARTESIAN_POINT('Ctrl Pts',(-2.37176696530802,0.0310222558120081,
6.84818551792834));
#43728=CARTESIAN_POINT('Ctrl Pts',(-2.37112472272847,0.0633116873235132,
6.84612333680678));
#43729=CARTESIAN_POINT('Ctrl Pts',(-2.36878519694936,0.121319892465059,
6.84238328321564));
#43730=CARTESIAN_POINT('Ctrl Pts',(-2.36732762140969,0.147043113666593,
6.84071228654366));
#43731=CARTESIAN_POINT('Ctrl Pts',(-2.36545134966532,0.172736721245143,
6.83902895557496));
#43732=CARTESIAN_POINT('',(-2.37174939424271,0.00169511337750838,6.6502503165247));
#43733=CARTESIAN_POINT('Ctrl Pts',(-2.36545136499509,0.172736511319545,
6.6396530072276));
#43734=CARTESIAN_POINT('Ctrl Pts',(-2.36960469570264,0.115860858821994,
6.64316385049418));
#43735=CARTESIAN_POINT('Ctrl Pts',(-2.37170857335039,0.0588104238426276,
6.64668720588036));
#43736=CARTESIAN_POINT('Ctrl Pts',(-2.37174939424271,0.00169511337380844,
6.65025031652493));
#43737=CARTESIAN_POINT('Ctrl Pts',(-2.37174939604129,0.00169259498356675,
6.65025047363349));
#43738=CARTESIAN_POINT('Ctrl Pts',(-2.37180198521626,-0.0719980074205978,
6.65484762707334));
#43739=CARTESIAN_POINT('Ctrl Pts',(-2.36842022635197,-0.145646969305529,
6.65950247976216));
#43740=CARTESIAN_POINT('Ctrl Pts',(-2.35920558020346,-0.245006984224481,
6.66593854475818));
#43741=CARTESIAN_POINT('Ctrl Pts',(-2.3563663772406,-0.270955358027443,
6.6676336889454));
#43742=CARTESIAN_POINT('Ctrl Pts',(-2.35061731969685,-0.316527421877923,
6.6706392077535));
#43743=CARTESIAN_POINT('Ctrl Pts',(-2.34788841388856,-0.336171607927287,
6.6719440911275));
#43744=CARTESIAN_POINT('Ctrl Pts',(-2.34186715063314,-0.375857339753646,
6.67460047600724));
#43745=CARTESIAN_POINT('Ctrl Pts',(-2.3385630816661,-0.395895392017766,
6.67595223138285));
#43746=CARTESIAN_POINT('Ctrl Pts',(-2.33107903663843,-0.437914541218356,
6.67881010480298));
#43747=CARTESIAN_POINT('Ctrl Pts',(-2.32684453395074,-0.459883764824666,
6.68031779259894));
#43748=CARTESIAN_POINT('Ctrl Pts',(-2.31463236085752,-0.518748369904315,
6.68439533682385));
#43749=CARTESIAN_POINT('Ctrl Pts',(-2.30608391989405,-0.555517339905188,
6.68698259608619));
#43750=CARTESIAN_POINT('Ctrl Pts',(-2.25656111397816,-0.74761983246704,
6.70072008158761));
#43751=CARTESIAN_POINT('Ctrl Pts',(-2.20076624756007,-0.898674411720307,
6.71232638877071));
#43752=CARTESIAN_POINT('Ctrl Pts',(-2.08388196602773,-1.13741193789532,
6.73168224039077));
#43753=CARTESIAN_POINT('Ctrl Pts',(-2.031372598892,-1.22873838423062,6.73934972224757));
#43754=CARTESIAN_POINT('Ctrl Pts',(-1.95263335928461,-1.34676040707862,
6.74939565463265));
#43755=CARTESIAN_POINT('Ctrl Pts',(-1.93159326687341,-1.37676738192395,
6.75196203189213));
#43756=CARTESIAN_POINT('Ctrl Pts',(-1.90075508417639,-1.41864873502436,
6.75554877399874));
#43757=CARTESIAN_POINT('Ctrl Pts',(-1.89152486940883,-1.43093250118447,
6.75660135769242));
#43758=CARTESIAN_POINT('Ctrl Pts',(-1.8752308407721,-1.45218374436709,6.75842218244956));
#43759=CARTESIAN_POINT('Ctrl Pts',(-1.86822069960764,-1.46119121621274,
6.75919383448859));
#43760=CARTESIAN_POINT('Ctrl Pts',(-1.85263232830738,-1.48092543239047,
6.76088400285217));
#43761=CARTESIAN_POINT('Ctrl Pts',(-1.84402560900503,-1.4916287259647,6.76180057017437));
#43762=CARTESIAN_POINT('Ctrl Pts',(-1.81802606981801,-1.52339268839907,
6.7645223098142));
#43763=CARTESIAN_POINT('Ctrl Pts',(-1.80036130275517,-1.54422906475486,
6.7663099200441));
#43764=CARTESIAN_POINT('Ctrl Pts',(-1.68255144531188,-1.67842065160567,
6.77787258430705));
#43765=CARTESIAN_POINT('Ctrl Pts',(-1.57210708097827,-1.7822921917115,6.78707690287077));
#43766=CARTESIAN_POINT('Ctrl Pts',(-1.37976973431109,-1.93129489222645,
6.8020523833101));
#43767=CARTESIAN_POINT('Ctrl Pts',(-1.30381632331299,-1.9833622745904,6.80773911319795));
#43768=CARTESIAN_POINT('Ctrl Pts',(-1.17305019504164,-2.06224075702158,
6.81739152855389));
#43769=CARTESIAN_POINT('Ctrl Pts',(-1.1198847529526,-2.09158813233912,6.82128003510613));
#43770=CARTESIAN_POINT('Ctrl Pts',(-1.0419762392597,-2.13077124550669,6.82696589349813));
#43771=CARTESIAN_POINT('Ctrl Pts',(-1.01810006535693,-2.14228213590605,
6.8287066685625));
#43772=CARTESIAN_POINT('Ctrl Pts',(-0.975620461835801,-2.1618913496205,
6.83180354819913));
#43773=CARTESIAN_POINT('Ctrl Pts',(-0.957096369004242,-2.17015575270161,
6.83315391779767));
#43774=CARTESIAN_POINT('Ctrl Pts',(-0.917831749074079,-2.18707290686811,
6.83601722267429));
#43775=CARTESIAN_POINT('Ctrl Pts',(-0.897069778186781,-2.19567046109229,
6.83753183138862));
#43776=CARTESIAN_POINT('Ctrl Pts',(-0.840662867369621,-2.218095041622,6.84164985841201));
#43777=CARTESIAN_POINT('Ctrl Pts',(-0.804801929362138,-2.2313568153584,
6.84427128799778));
#43778=CARTESIAN_POINT('Ctrl Pts',(-0.618462371374257,-2.2951909874728,
6.85791729898134));
#43779=CARTESIAN_POINT('Ctrl Pts',(-0.463524097536502,-2.33142181138276,
6.86938432423666));
#43780=CARTESIAN_POINT('Ctrl Pts',(-0.181278161257841,-2.36816282244178,
6.89010962258279));
#43781=CARTESIAN_POINT('Ctrl Pts',(-0.0552927285863765,-2.37444836370118,
6.89929122107597));
#43782=CARTESIAN_POINT('Ctrl Pts',(0.0943690088880997,-2.36999109482885,
6.90975666730572));
#43783=CARTESIAN_POINT('Ctrl Pts',(0.11812231988628,-2.36892602708971,6.91140402418232));
#43784=CARTESIAN_POINT('Ctrl Pts',(0.154859543466095,-2.36672479727579,
6.9139267869522));
#43785=CARTESIAN_POINT('Ctrl Pts',(0.167856158971682,-2.36583855616849,
6.91481440474648));
#43786=CARTESIAN_POINT('Ctrl Pts',(0.192381409982752,-2.36396305350721,
6.91647937823283));
#43787=CARTESIAN_POINT('Ctrl Pts',(0.203910598789635,-2.36299648715318,
6.91725779312367));
#43788=CARTESIAN_POINT('Ctrl Pts',(0.231974714817298,-2.36043676085089,
6.91914293124431));
#43789=CARTESIAN_POINT('Ctrl Pts',(0.248500788826079,-2.35875419796759,
6.92024490765104));
#43790=CARTESIAN_POINT('Ctrl Pts',(0.306983653290963,-2.35217841528138,
6.9241201202622));
#43791=CARTESIAN_POINT('Ctrl Pts',(0.34882828697458,-2.34633790810091,6.92684813995306));
#43792=CARTESIAN_POINT('Ctrl Pts',(0.575351928240905,-2.3085258416957,6.94147992913852));
#43793=CARTESIAN_POINT('Ctrl Pts',(0.755909757123629,-2.25586650789915,
6.95269558792164));
#43794=CARTESIAN_POINT('Ctrl Pts',(1.00775729147412,-2.1487347731389,6.96976494623298));
#43795=CARTESIAN_POINT('Ctrl Pts',(1.08521054818543,-2.1106756387633,6.97522233134478));
#43796=CARTESIAN_POINT('Ctrl Pts',(1.18633683261385,-2.05394411854507,6.98274902332448));
#43797=CARTESIAN_POINT('Ctrl Pts',(1.21198271470016,-2.03891620613159,6.9846939781063));
#43798=CARTESIAN_POINT('Ctrl Pts',(1.25507182883062,-2.01256672723371,6.98802793674009));
#43799=CARTESIAN_POINT('Ctrl Pts',(1.27266131727835,-2.00149025805052,6.98940813735224));
#43800=CARTESIAN_POINT('Ctrl Pts',(1.30799110614294,-1.97858833461649,6.99222093674746));
#43801=CARTESIAN_POINT('Ctrl Pts',(1.32572204509235,-1.96675202824174,6.993653840464));
#43802=CARTESIAN_POINT('Ctrl Pts',(1.37009215329695,-1.93626008666731,6.9972949959974));
#43803=CARTESIAN_POINT('Ctrl Pts',(1.39651091487895,-1.9172930705407,6.99951460923388));
#43804=CARTESIAN_POINT('Ctrl Pts',(1.51670479841012,-1.82719908155595,7.00985978346458));
#43805=CARTESIAN_POINT('Ctrl Pts',(1.60548089632023,-1.74970680780491,7.01822344438646));
#43806=CARTESIAN_POINT('Ctrl Pts',(1.77885265421624,-1.57402765574,7.03606937157826));
#43807=CARTESIAN_POINT('Ctrl Pts',(1.86191309703049,-1.47484210491552,7.04555326479193));
#43808=CARTESIAN_POINT('Ctrl Pts',(1.97079570438408,-1.32086854337817,7.05909895334066));
#43809=CARTESIAN_POINT('Ctrl Pts',(2.00327374292448,-1.27107235959096,7.06331648460182));
#43810=CARTESIAN_POINT('Ctrl Pts',(2.04319360101439,-1.20452808898838,7.06869661625635));
#43811=CARTESIAN_POINT('Ctrl Pts',(2.05235906457722,-1.18884411428124,7.06994674663879));
#43812=CARTESIAN_POINT('Ctrl Pts',(2.06720310304069,-1.16275953589027,7.07199457110828));
#43813=CARTESIAN_POINT('Ctrl Pts',(2.07298542874829,-1.15241912595429,7.07279835290198));
#43814=CARTESIAN_POINT('Ctrl Pts',(2.08468595348291,-1.13112226675523,7.07443680397979));
#43815=CARTESIAN_POINT('Ctrl Pts',(2.09059577249829,-1.12016179203454,7.07527098408579));
#43816=CARTESIAN_POINT('Ctrl Pts',(2.10625965468208,-1.0905554129311,7.07750140193677));
#43817=CARTESIAN_POINT('Ctrl Pts',(2.11585259812095,-1.07182493823015,7.07888830523962));
#43818=CARTESIAN_POINT('Ctrl Pts',(2.17727687734194,-0.947852954328027,
7.0879262831967));
#43819=CARTESIAN_POINT('Ctrl Pts',(2.22149455582226,-0.839004508869037,
7.09520168162207));
#43820=CARTESIAN_POINT('Ctrl Pts',(2.29411099697318,-0.613614930047822,
7.10979214429349));
#43821=CARTESIAN_POINT('Ctrl Pts',(2.32210018457666,-0.497310733101545,
7.11708789160099));
#43822=CARTESIAN_POINT('Ctrl Pts',(2.3492019533226,-0.330068581422661,7.12771874318987));
#43823=CARTESIAN_POINT('Ctrl Pts',(2.35563412103115,-0.280504037258696,
7.13088485540283));
#43824=CARTESIAN_POINT('Ctrl Pts',(2.36436205228061,-0.191230062449223,
7.13664548924809));
#43825=CARTESIAN_POINT('Ctrl Pts',(2.3672336850891,-0.151595659633722,7.13922326185328));
#43826=CARTESIAN_POINT('Ctrl Pts',(2.37018290714522,-0.0891610743582391,
7.14332574169825));
#43827=CARTESIAN_POINT('Ctrl Pts',(2.37092973915779,-0.0663989722919966,
7.14483009044519));
#43828=CARTESIAN_POINT('Ctrl Pts',(2.371720650477,-0.0234121593118154,7.14768920420574));
#43829=CARTESIAN_POINT('Ctrl Pts',(2.3718340477862,-0.00319065843857204,
7.14904172448005));
#43830=CARTESIAN_POINT('Ctrl Pts',(2.37150252947546,0.0429802358461522,
7.1521482748376));
#43831=CARTESIAN_POINT('Ctrl Pts',(2.37089028436428,0.0689254424510486,
7.15390725021403));
#43832=CARTESIAN_POINT('Ctrl Pts',(2.36765349567127,0.149793606831992,7.15943350070163));
#43833=CARTESIAN_POINT('Ctrl Pts',(2.36354494104859,0.204635484961782,7.16324466725661));
#43834=CARTESIAN_POINT('Ctrl Pts',(2.33667004538567,0.44899732504346,7.18051768991606));
#43835=CARTESIAN_POINT('Ctrl Pts',(2.29298155620036,0.635486233604201,7.1945638618519));
#43836=CARTESIAN_POINT('Ctrl Pts',(2.2102367491011,0.861718859319863,7.21196711979585));
#43837=CARTESIAN_POINT('Ctrl Pts',(2.19154884742905,0.908196065474832,7.21555789822041));
#43838=CARTESIAN_POINT('Ctrl Pts',(2.15783587409957,0.984926319749766,7.22147746198748));
#43839=CARTESIAN_POINT('Ctrl Pts',(2.14361145098473,1.01551254839014,7.22383469733135));
#43840=CARTESIAN_POINT('Ctrl Pts',(2.12217279471738,1.05915174836047,7.2271841724712));
#43841=CARTESIAN_POINT('Ctrl Pts',(2.11548101709301,1.07245507670386,7.22820337096737));
#43842=CARTESIAN_POINT('Ctrl Pts',(2.10345418748732,1.09581388985866,7.22998848121508));
#43843=CARTESIAN_POINT('Ctrl Pts',(2.09817145079525,1.10589519377805,7.2307573489492));
#43844=CARTESIAN_POINT('Ctrl Pts',(2.08618319772416,1.12837779655447,7.2324684956133));
#43845=CARTESIAN_POINT('Ctrl Pts',(2.07943943523042,1.14075783832828,7.23340845672332));
#43846=CARTESIAN_POINT('Ctrl Pts',(2.0583741778565,1.17862133910602,7.23627850810315));
#43847=CARTESIAN_POINT('Ctrl Pts',(2.04369108887535,1.20390175373111,7.23818808431925));
#43848=CARTESIAN_POINT('Ctrl Pts',(1.9227208720392,1.40358622631312,7.25327031806348));
#43849=CARTESIAN_POINT('Ctrl Pts',(1.79476796198041,1.56388570780492,7.26543469150203));
#43850=CARTESIAN_POINT('Ctrl Pts',(1.58424896289906,1.76724955621327,7.28367356558749));
#43851=CARTESIAN_POINT('Ctrl Pts',(1.51727742858009,1.82507055542942,7.28926329330823));
#43852=CARTESIAN_POINT('Ctrl Pts',(1.42352014445897,1.89728353834959,7.29694308398936));
#43853=CARTESIAN_POINT('Ctrl Pts',(1.39945786377047,1.91510103788407,7.29890175394842));
#43854=CARTESIAN_POINT('Ctrl Pts',(1.35809752047,1.94453153258822,7.30225203436734));
#43855=CARTESIAN_POINT('Ctrl Pts',(1.34097161861238,1.95638105405066,7.30363462632279));
#43856=CARTESIAN_POINT('Ctrl Pts',(1.30604659163203,1.97987186461351,7.30644614922014));
#43857=CARTESIAN_POINT('Ctrl Pts',(1.2882425193718,1.99150231264457,7.30787531068201));
#43858=CARTESIAN_POINT('Ctrl Pts',(1.24304684877533,2.02016656164038,7.31149433004567));
#43859=CARTESIAN_POINT('Ctrl Pts',(1.2154603996522,2.03688346454973,7.31369526636055));
#43860=CARTESIAN_POINT('Ctrl Pts',(1.09267511731122,2.1079066026822,7.32346140793998));
#43861=CARTESIAN_POINT('Ctrl Pts',(0.994131036750746,2.15613237182062,7.33123018050427));
#43862=CARTESIAN_POINT('Ctrl Pts',(0.766529143583916,2.24858914800888,7.3489531170373));
#43863=CARTESIAN_POINT('Ctrl Pts',(0.636269155954512,2.2888601143306,7.35895459966368));
#43864=CARTESIAN_POINT('Ctrl Pts',(0.44379539544784,2.33065409868693,7.37311151533002));
#43865=CARTESIAN_POINT('Ctrl Pts',(0.383833733594456,2.34127653985938,7.37743444396681));
#43866=CARTESIAN_POINT('Ctrl Pts',(0.305397991580051,2.3520767304602,7.38292507937804));
#43867=CARTESIAN_POINT('Ctrl Pts',(0.287242056744769,2.35436295645328,7.38418464375798));
#43868=CARTESIAN_POINT('Ctrl Pts',(0.257264310327961,2.35778584878636,7.38624367247878));
#43869=CARTESIAN_POINT('Ctrl Pts',(0.245457431606833,2.3590442355135,7.38704935472446));
#43870=CARTESIAN_POINT('Ctrl Pts',(0.222825498280978,2.36128460459393,7.38858302410748));
#43871=CARTESIAN_POINT('Ctrl Pts',(0.212002374865882,2.36228092978478,7.38931183003946));
#43872=CARTESIAN_POINT('Ctrl Pts',(0.182036159217526,2.36483186575039,7.39131782995691));
#43873=CARTESIAN_POINT('Ctrl Pts',(0.162879974216491,2.36622845212401,7.39258680935211));
#43874=CARTESIAN_POINT('Ctrl Pts',(0.078392821779802,2.37135708978973,7.39813296952163));
#43875=CARTESIAN_POINT('Ctrl Pts',(0.0129351781399842,2.37261756846035,
7.40229709889186));
#43876=CARTESIAN_POINT('Ctrl Pts',(-0.216141432622983,2.3675459414839,7.41665978937104));
#43877=CARTESIAN_POINT('Ctrl Pts',(-0.378974394102621,2.34699236951005,
7.42652249433897));
#43878=CARTESIAN_POINT('Ctrl Pts',(-0.618419801082092,2.29118013842813,
7.44188401620058));
#43879=CARTESIAN_POINT('Ctrl Pts',(-0.697411234680339,2.26838378804286,
7.44709285580397));
#43880=CARTESIAN_POINT('Ctrl Pts',(-0.802742258754739,2.23196351633728,
7.4543312233458));
#43881=CARTESIAN_POINT('Ctrl Pts',(-0.830248340535593,2.22187844947369,
7.45624904365158));
#43882=CARTESIAN_POINT('Ctrl Pts',(-0.876868581217198,2.2037986438129,7.45955081676203));
#43883=CARTESIAN_POINT('Ctrl Pts',(-0.896078093182024,2.19605805411751,
7.46092638835456));
#43884=CARTESIAN_POINT('Ctrl Pts',(-0.932615286225015,2.1807759687145,7.46357298923735));
#43885=CARTESIAN_POINT('Ctrl Pts',(-0.949959095499659,2.17327696802719,
7.46484252469831));
#43886=CARTESIAN_POINT('Ctrl Pts',(-0.995365651144746,2.15299700157365,
7.46820214049723));
#43887=CARTESIAN_POINT('Ctrl Pts',(-1.02327117354341,2.13987495467771,7.47030345822871));
#43888=CARTESIAN_POINT('Ctrl Pts',(-1.13335386894207,2.08546497570741,7.47874385890637));
#43889=CARTESIAN_POINT('Ctrl Pts',(-1.21334634119102,2.03996132895333,7.48522199544609));
#43890=CARTESIAN_POINT('Ctrl Pts',(-1.41894074867014,1.90663176628679,7.50278828029663));
#43891=CARTESIAN_POINT('Ctrl Pts',(-1.5390172086522,1.81109347798263,7.5140561621131));
#43892=CARTESIAN_POINT('Ctrl Pts',(-1.69504775177748,1.66015293673796,7.52968179971005));
#43893=CARTESIAN_POINT('Ctrl Pts',(-1.73923401380762,1.61380332180321,7.53423438264327));
#43894=CARTESIAN_POINT('Ctrl Pts',(-1.79375612377239,1.55176738751399,7.53996441974279));
#43895=CARTESIAN_POINT('Ctrl Pts',(-1.80585398661713,1.53767177523308,7.5412434802507));
#43896=CARTESIAN_POINT('Ctrl Pts',(-1.82544752818523,1.51429246742133,7.54332571911559));
#43897=CARTESIAN_POINT('Ctrl Pts',(-1.83304078757346,1.50509197289964,7.54413538570502));
#43898=CARTESIAN_POINT('Ctrl Pts',(-1.84834513663975,1.48626057949663,7.54577220607711));
#43899=CARTESIAN_POINT('Ctrl Pts',(-1.85605108658666,1.47662609864,7.54659902476091));
#43900=CARTESIAN_POINT('Ctrl Pts',(-1.87636310386161,1.45082044162099,7.54878689925829));
#43901=CARTESIAN_POINT('Ctrl Pts',(-1.88883555220949,1.43454479767433,7.55013922732561));
#43902=CARTESIAN_POINT('Ctrl Pts',(-1.95508579336583,1.34573069567163,7.55738359929408));
#43903=CARTESIAN_POINT('Ctrl Pts',(-2.00490446456094,1.27032012268282,7.56305592137044));
#43904=CARTESIAN_POINT('Ctrl Pts',(-2.12187220143662,1.06917043995233,7.5774847273837));
#43905=CARTESIAN_POINT('Ctrl Pts',(-2.18221118109443,0.939905061466952,
7.58611883632595));
#43906=CARTESIAN_POINT('Ctrl Pts',(-2.25688000149102,0.733262381041774,
7.59987803540204));
#43907=CARTESIAN_POINT('Ctrl Pts',(-2.27958971348356,0.659279948761734,
7.60479220512656));
#43908=CARTESIAN_POINT('Ctrl Pts',(-2.30572665257823,0.556461351126819,
7.61168729140122));
#43909=CARTESIAN_POINT('Ctrl Pts',(-2.31230229604116,0.528471956392537,
7.61357053296406));
#43910=CARTESIAN_POINT('Ctrl Pts',(-2.32271676591039,0.480218616516357,
7.61683152153846));
#43911=CARTESIAN_POINT('Ctrl Pts',(-2.32680314934294,0.460011036823562,
7.61820141802409));
#43912=CARTESIAN_POINT('Ctrl Pts',(-2.33414954083864,0.421076278769923,
7.62085017904811));
#43913=CARTESIAN_POINT('Ctrl Pts',(-2.33744887736892,0.402358076404976,
7.62212770554261));
#43914=CARTESIAN_POINT('Ctrl Pts',(-2.34561434226197,0.352537110139717,
7.62553989138193));
#43915=CARTESIAN_POINT('Ctrl Pts',(-2.35008665308357,0.321374575849296,
7.62768646840528));
#43916=CARTESIAN_POINT('Ctrl Pts',(-2.3587493140946,0.251091891849367,7.63255767963198));
#43917=CARTESIAN_POINT('Ctrl Pts',(-2.36258799030857,0.21194749286373,7.63529150187935));
#43918=CARTESIAN_POINT('Ctrl Pts',(-2.36545135498545,0.17273664839138,7.63805096494753));
#43919=CARTESIAN_POINT('Origin',(0.,0.,-1.84858989190501));
#43920=CARTESIAN_POINT('',(-2.36545132340078,0.172737080910542,8.8374806621729));
#43921=CARTESIAN_POINT('',(-2.36545134966571,0.172736721239843,8.64191454572571));
#43922=CARTESIAN_POINT('',(-2.36545134966535,0.172736721244682,-1.84858989190501));
#43923=CARTESIAN_POINT('Ctrl Pts',(-2.36545132340079,0.172737080910402,
8.8374806621729));
#43924=CARTESIAN_POINT('Ctrl Pts',(-2.3549239636921,0.31689811931398,8.82699267314082));
#43925=CARTESIAN_POINT('Ctrl Pts',(-2.33123218326878,0.459910024350676,
8.81635530687031));
#43926=CARTESIAN_POINT('Ctrl Pts',(-2.28553067457795,0.634692462460707,
8.80356992920104));
#43927=CARTESIAN_POINT('Ctrl Pts',(-2.2756687819126,0.669191233137263,8.8010584792055));
#43928=CARTESIAN_POINT('Ctrl Pts',(-2.26058560740237,0.717756955937051,
8.79755235779571));
#43929=CARTESIAN_POINT('Ctrl Pts',(-2.25600832838802,0.732016931087265,
8.79652652657968));
#43930=CARTESIAN_POINT('Ctrl Pts',(-2.24784333586149,0.756649740162565,
8.79476195436269));
#43931=CARTESIAN_POINT('Ctrl Pts',(-2.24431823953607,0.767042469089523,
8.79401983804858));
#43932=CARTESIAN_POINT('Ctrl Pts',(-2.23641162508261,0.789831593948998,
8.79239793566709));
#43933=CARTESIAN_POINT('Ctrl Pts',(-2.23199901587458,0.802216502404582,
8.79151991009927));
#43934=CARTESIAN_POINT('Ctrl Pts',(-2.2189697023577,0.837846073199519,8.78900207671265));
#43935=CARTESIAN_POINT('Ctrl Pts',(-2.21009099287284,0.860993903107094,
8.78737631896165));
#43936=CARTESIAN_POINT('Ctrl Pts',(-2.1376765042439,1.04128076720594,8.77476147587883));
#43937=CARTESIAN_POINT('Ctrl Pts',(-2.05781649567719,1.19135749774416,8.76451846399258));
#43938=CARTESIAN_POINT('Ctrl Pts',(-1.91567153528225,1.40085495720134,8.74891279280651));
#43939=CARTESIAN_POINT('Ctrl Pts',(-1.86509141385393,1.46752331187729,8.74372370211467));
#43940=CARTESIAN_POINT('Ctrl Pts',(-1.77440518435404,1.57477426443807,8.73482465831089));
#43941=CARTESIAN_POINT('Ctrl Pts',(-1.73616592633438,1.61683482192931,8.73117710804433));
#43942=CARTESIAN_POINT('Ctrl Pts',(-1.67868294991811,1.67566952560035,8.72580889181701));
#43943=CARTESIAN_POINT('Ctrl Pts',(-1.66061975758213,1.69357218483052,8.72413742800565));
#43944=CARTESIAN_POINT('Ctrl Pts',(-1.62810622060584,1.72477643174437,8.72115324375087));
#43945=CARTESIAN_POINT('Ctrl Pts',(-1.61377178187576,1.73819567435074,8.71984568720397));
#43946=CARTESIAN_POINT('Ctrl Pts',(-1.58310158214334,1.76620128826421,8.71706388210865));
#43947=CARTESIAN_POINT('Ctrl Pts',(-1.56672717869249,1.78074240217377,8.71558793436397));
#43948=CARTESIAN_POINT('Ctrl Pts',(-1.52174187602038,1.8195903398038,8.71155635937749));
#43949=CARTESIAN_POINT('Ctrl Pts',(-1.49275245705256,1.84344708923602,8.70898315832546));
#43950=CARTESIAN_POINT('Ctrl Pts',(-1.33413554991997,1.96778509864692,8.69502692453214));
#43951=CARTESIAN_POINT('Ctrl Pts',(-1.19493382305038,2.05528886884725,8.6831640713442));
#43952=CARTESIAN_POINT('Ctrl Pts',(-0.934262530268304,2.18366260055691,
8.66199792930429));
#43953=CARTESIAN_POINT('Ctrl Pts',(-0.816369126214726,2.23042064923685,
8.65277380803439));
#43954=CARTESIAN_POINT('Ctrl Pts',(-0.675033431480264,2.27375837176499,
8.64247333794866));
#43955=CARTESIAN_POINT('Ctrl Pts',(-0.654686938590233,2.27970005825391,
8.64100852100713));
#43956=CARTESIAN_POINT('Ctrl Pts',(-0.622457960550302,2.28864462833137,
8.63871942921143));
#43957=CARTESIAN_POINT('Ctrl Pts',(-0.610627699683309,2.29182939513999,
8.63788575307213));
#43958=CARTESIAN_POINT('Ctrl Pts',(-0.587909569632947,2.29775682953183,
8.63629808038055));
#43959=CARTESIAN_POINT('Ctrl Pts',(-0.577026128529414,2.30051406476027,
8.63554335624783));
#43960=CARTESIAN_POINT('Ctrl Pts',(-0.549805271056664,2.30720493100135,
8.63366948628896));
#43961=CARTESIAN_POINT('Ctrl Pts',(-0.533444466712569,2.31104250719786,
8.63255554070836));
#43962=CARTESIAN_POINT('Ctrl Pts',(-0.472441950473886,2.3246688451108,8.62844313687188));
#43963=CARTESIAN_POINT('Ctrl Pts',(-0.427558243811104,2.33334120847606,
8.62549868628831));
#43964=CARTESIAN_POINT('Ctrl Pts',(-0.234070547347241,2.36495515761656,
8.61304479302822));
#43965=CARTESIAN_POINT('Ctrl Pts',(-0.0837129401427739,2.37503703492672,
8.60394898112043));
#43966=CARTESIAN_POINT('Ctrl Pts',(0.143484614799508,2.36865503969153,8.58990906930768));
#43967=CARTESIAN_POINT('Ctrl Pts',(0.220218085022321,2.36275629812587,8.58511970448396));
#43968=CARTESIAN_POINT('Ctrl Pts',(0.349856788706824,2.34642018651598,8.57682335268715));
#43969=CARTESIAN_POINT('Ctrl Pts',(0.402940885513851,2.33788909908419,8.57336742155193));
#43970=CARTESIAN_POINT('Ctrl Pts',(0.480149098939338,2.32277339864573,8.56822880630346));
#43971=CARTESIAN_POINT('Ctrl Pts',(0.504533898614867,2.31759894879552,8.56658937387015));
#43972=CARTESIAN_POINT('Ctrl Pts',(0.547921447470655,2.30767493946582,8.56364051039771));
#43973=CARTESIAN_POINT('Ctrl Pts',(0.566955703985426,2.30307245436562,8.56233579394326));
#43974=CARTESIAN_POINT('Ctrl Pts',(0.60743389508692,2.2927526218239,8.55953651715485));
#43975=CARTESIAN_POINT('Ctrl Pts',(0.62885882114427,2.28696896522647,8.55803996922111));
#43976=CARTESIAN_POINT('Ctrl Pts',(0.686708241039703,2.27047816717114,8.55395714302827));
#43977=CARTESIAN_POINT('Ctrl Pts',(0.722960594875283,2.25919609863791,8.55135294905878));
#43978=CARTESIAN_POINT('Ctrl Pts',(0.881296621431954,2.20571923768995,8.53977058932203));
#43979=CARTESIAN_POINT('Ctrl Pts',(1.00007044574214,2.15446779905382,8.53051346576622));
#43980=CARTESIAN_POINT('Ctrl Pts',(1.21293423404048,2.04120810170904,8.51299556497496));
#43981=CARTESIAN_POINT('Ctrl Pts',(1.30795261672392,1.98166621610205,8.50479141178066));
#43982=CARTESIAN_POINT('Ctrl Pts',(1.44295753867741,1.88311274959956,8.49280944908056));
#43983=CARTESIAN_POINT('Ctrl Pts',(1.48636111024231,1.84904617275752,8.4889034448089));
#43984=CARTESIAN_POINT('Ctrl Pts',(1.54186615601031,1.80226261772794,8.48387484124514));
#43985=CARTESIAN_POINT('Ctrl Pts',(1.55506804389848,1.79088391845794,8.48267619875846));
#43986=CARTESIAN_POINT('Ctrl Pts',(1.57673849069261,1.7717858325653,8.48070602054185));
#43987=CARTESIAN_POINT('Ctrl Pts',(1.58527852375643,1.76414889595256,8.47992890976153));
#43988=CARTESIAN_POINT('Ctrl Pts',(1.60271146803955,1.74833063479896,8.47834171563353));
#43989=CARTESIAN_POINT('Ctrl Pts',(1.61159776495678,1.74014272927273,8.4775321246025));
#43990=CARTESIAN_POINT('Ctrl Pts',(1.63532250405768,1.71794493434399,8.47536796377216));
#43991=CARTESIAN_POINT('Ctrl Pts',(1.65004371824213,1.7038105191779,8.47402221006071));
#43992=CARTESIAN_POINT('Ctrl Pts',(1.73789322719995,1.61725606757282,8.4659600169087));
#43993=CARTESIAN_POINT('Ctrl Pts',(1.80643500266684,1.54032062372601,8.4595336504411));
#43994=CARTESIAN_POINT('Ctrl Pts',(1.95213913459416,1.35361620638187,8.44490343944075));
#43995=CARTESIAN_POINT('Ctrl Pts',(2.025422849414,1.24128380287203,8.43676329805829));
#43996=CARTESIAN_POINT('Ctrl Pts',(2.12427582032535,1.05747273986883,8.42367815060364));
#43997=CARTESIAN_POINT('Ctrl Pts',(2.15657378134703,0.989941547357563,8.41891878753288));
#43998=CARTESIAN_POINT('Ctrl Pts',(2.19647657751588,0.895248398487564,8.41223656984106));
#43999=CARTESIAN_POINT('Ctrl Pts',(2.20687226907676,0.869306466451068,8.41040530223374));
#44000=CARTESIAN_POINT('Ctrl Pts',(2.22391858549152,0.824490362279526,8.40723732987511));
#44001=CARTESIAN_POINT('Ctrl Pts',(2.23079332975739,0.805704233271185,8.40590808825291));
#44002=CARTESIAN_POINT('Ctrl Pts',(2.24435791059479,0.767132186225706,8.40317511875583));
#44003=CARTESIAN_POINT('Ctrl Pts',(2.25102565022031,0.747340415529887,8.40177081084249));
#44004=CARTESIAN_POINT('Ctrl Pts',(2.26741899436637,0.696469364474807,8.39815499235762));
#44005=CARTESIAN_POINT('Ctrl Pts',(2.27676718014668,0.665274003552024,8.39593167391743));
#44006=CARTESIAN_POINT('Ctrl Pts',(2.32161157723521,0.503590861911816,8.38437194764615));
#44007=CARTESIAN_POINT('Ctrl Pts',(2.34653754531588,0.370452639471144,8.37471104340073));
#44008=CARTESIAN_POINT('Ctrl Pts',(2.37151250747135,0.120636910462846,8.35648580319882));
#44009=CARTESIAN_POINT('Ctrl Pts',(2.37457451519073,0.00464695727427692,
8.34799130147554));
#44010=CARTESIAN_POINT('Ctrl Pts',(2.36651718712373,-0.167165538839918,
8.33565535932213));
#44011=CARTESIAN_POINT('Ctrl Pts',(2.36189877342919,-0.223121396098586,
8.3316787461218));
#44012=CARTESIAN_POINT('Ctrl Pts',(2.35323823682515,-0.296268439618266,
8.32657539763777));
#44013=CARTESIAN_POINT('Ctrl Pts',(2.35098478340419,-0.313649136299329,
8.3253698905354));
#44014=CARTESIAN_POINT('Ctrl Pts',(2.34693731432067,-0.342366739715257,
8.32339156730443));
#44015=CARTESIAN_POINT('Ctrl Pts',(2.34525332783633,-0.353718235736791,
8.32261308425144));
#44016=CARTESIAN_POINT('Ctrl Pts',(2.34163166304584,-0.376967514673342,
8.32102642918691));
#44017=CARTESIAN_POINT('Ctrl Pts',(2.3396855633769,-0.388863514376001,8.32021871231131));
#44018=CARTESIAN_POINT('Ctrl Pts',(2.33422388136751,-0.420722953448914,
8.31806535125519));
#44019=CARTESIAN_POINT('Ctrl Pts',(2.33054284642996,-0.440657507894412,
8.31672837171676));
#44020=CARTESIAN_POINT('Ctrl Pts',(2.30838064065158,-0.552618191179682,
8.30926548353026));
#44021=CARTESIAN_POINT('Ctrl Pts',(2.28470285653747,-0.643540877982558,
8.30337939804438));
#44022=CARTESIAN_POINT('Ctrl Pts',(2.2121850261031,-0.866755244311674,8.28884503313311));
#44023=CARTESIAN_POINT('Ctrl Pts',(2.15683586539921,-0.996537053381276,
8.28030319476529));
#44024=CARTESIAN_POINT('Ctrl Pts',(2.05406847825948,-1.18822603650397,8.26667954228969));
#44025=CARTESIAN_POINT('Ctrl Pts',(2.01458260883726,-1.25400702508516,8.26180594314104));
#44026=CARTESIAN_POINT('Ctrl Pts',(1.95633299401079,-1.34117586354337,8.25499027545934));
#44027=CARTESIAN_POINT('Ctrl Pts',(1.94026748779738,-1.36431427752057,8.25314493797997));
#44028=CARTESIAN_POINT('Ctrl Pts',(1.91207208446215,-1.40341729520979,8.24996037325855));
#44029=CARTESIAN_POINT('Ctrl Pts',(1.90014463649585,-1.41952459649963,8.2486288182691));
#44030=CARTESIAN_POINT('Ctrl Pts',(1.87690799595753,-1.45008661740033,8.24606303112605));
#44031=CARTESIAN_POINT('Ctrl Pts',(1.86563231263638,-1.46456507714444,8.24483015319904));
#44032=CARTESIAN_POINT('Ctrl Pts',(1.83545485539225,-1.50240017601154,8.24156131892143));
#44033=CARTESIAN_POINT('Ctrl Pts',(1.8162758070753,-1.52553035582997,8.23951461028934));
#44034=CARTESIAN_POINT('Ctrl Pts',(1.7385900946876,-1.61567829220736,8.2313395845881));
#44035=CARTESIAN_POINT('Ctrl Pts',(1.67677829675948,-1.67973900204807,8.22508081442414));
#44036=CARTESIAN_POINT('Ctrl Pts',(1.46866786457907,-1.87246396015657,8.20477264528074));
#44037=CARTESIAN_POINT('Ctrl Pts',(1.31007976439556,-1.98665348513427,8.19032081085633));
#44038=CARTESIAN_POINT('Ctrl Pts',(1.10850144091213,-2.09705933987949,8.17406528418838));
#44039=CARTESIAN_POINT('Ctrl Pts',(1.07730251507111,-2.1132564723877,8.17160603655951));
#44040=CARTESIAN_POINT('Ctrl Pts',(1.03241526907004,-2.13530738030571,8.1681589028466));
#44041=CARTESIAN_POINT('Ctrl Pts',(1.01901558864048,-2.1417343800413,8.16714119275506));
#44042=CARTESIAN_POINT('Ctrl Pts',(0.995537648664411,-2.15272506696177,
8.16537880652056));
#44043=CARTESIAN_POINT('Ctrl Pts',(0.985486566507586,-2.15734481914038,
8.16463093807182));
#44044=CARTESIAN_POINT('Ctrl Pts',(0.963305912992754,-2.1673522801188,8.16299522505074));
#44045=CARTESIAN_POINT('Ctrl Pts',(0.951162986656204,-2.1727087198867,8.16210918475372));
#44046=CARTESIAN_POINT('Ctrl Pts',(0.915665308598253,-2.18801267333933,
8.15954458590526));
#44047=CARTESIAN_POINT('Ctrl Pts',(0.892194273293991,-2.19768785731821,
8.15788088410781));
#44048=CARTESIAN_POINT('Ctrl Pts',(0.770420468177783,-2.2456126254546,8.14939070322152));
#44049=CARTESIAN_POINT('Ctrl Pts',(0.669791046594585,-2.27765416237008,
8.14284256141661));
#44050=CARTESIAN_POINT('Ctrl Pts',(0.447954197665646,-2.33230711158163,
8.12876218495918));
#44051=CARTESIAN_POINT('Ctrl Pts',(0.32645304234203,-2.3523916752934,8.12126271370613));
#44052=CARTESIAN_POINT('Ctrl Pts',(0.130006047252304,-2.36934677131047,
8.10889655596297));
#44053=CARTESIAN_POINT('Ctrl Pts',(0.0558148960734866,-2.37225395170327,
8.10417455127448));
#44054=CARTESIAN_POINT('Ctrl Pts',(-0.0462571224614121,-2.37146267247415,
8.09753603246053));
#44055=CARTESIAN_POINT('Ctrl Pts',(-0.0741216301720457,-2.37075532417822,
8.09570945600553));
#44056=CARTESIAN_POINT('Ctrl Pts',(-0.121939470981536,-2.36869763681544,
8.09254700521294));
#44057=CARTESIAN_POINT('Ctrl Pts',(-0.141900460704218,-2.3675856790782,
8.09121852456685));
#44058=CARTESIAN_POINT('Ctrl Pts',(-0.182702282129724,-2.3647949214371,
8.08848477690679));
#44059=CARTESIAN_POINT('Ctrl Pts',(-0.203539688850077,-2.36309261179102,
8.08707890231843));
#44060=CARTESIAN_POINT('Ctrl Pts',(-0.256878037826373,-2.35802444347678,
8.08345396220832));
#44061=CARTESIAN_POINT('Ctrl Pts',(-0.289335961161488,-2.35426211855619,
8.08122297132652));
#44062=CARTESIAN_POINT('Ctrl Pts',(-0.451879636089599,-2.3320090136016,
8.06991866394156));
#44063=CARTESIAN_POINT('Ctrl Pts',(-0.580328744695812,-2.30340403304197,
8.06054109373206));
#44064=CARTESIAN_POINT('Ctrl Pts',(-0.81723435082639,-2.22956647540326,
8.04253914554753));
#44065=CARTESIAN_POINT('Ctrl Pts',(-0.926018120435991,-2.18662519113367,
8.03397489551933));
#44066=CARTESIAN_POINT('Ctrl Pts',(-1.08375095666906,-2.1104709633366,8.02139871354414));
#44067=CARTESIAN_POINT('Ctrl Pts',(-1.13535549606405,-2.08316415344802,
8.01725903610057));
#44068=CARTESIAN_POINT('Ctrl Pts',(-1.20126854733559,-2.04510799275429,
8.01198380868001));
#44069=CARTESIAN_POINT('Ctrl Pts',(-1.21653360218727,-2.03606455351805,
8.01076302271101));
#44070=CARTESIAN_POINT('Ctrl Pts',(-1.24153952980891,-2.0208687062072,8.00876653307164));
#44071=CARTESIAN_POINT('Ctrl Pts',(-1.251339411356,-2.0148152344421,8.00798495725191));
#44072=CARTESIAN_POINT('Ctrl Pts',(-1.27125085489501,-2.00231444003762,
8.00639928493538));
#44073=CARTESIAN_POINT('Ctrl Pts',(-1.28135830893275,-1.99586140614889,
8.0055955629847));
#44074=CARTESIAN_POINT('Ctrl Pts',(-1.3081741193088,-1.97845335791459,8.00346521360673));
#44075=CARTESIAN_POINT('Ctrl Pts',(-1.32479412848804,-1.96736315833756,
8.0021469315357));
#44076=CARTESIAN_POINT('Ctrl Pts',(-1.4123836204893,-1.90730305701429,7.9951992642605));
#44077=CARTESIAN_POINT('Ctrl Pts',(-1.48079066010414,-1.85469530162944,
7.98977149843507));
#44078=CARTESIAN_POINT('Ctrl Pts',(-1.657677160601,-1.70262210404672,7.97528800677892));
#44079=CARTESIAN_POINT('Ctrl Pts',(-1.7600119922211,-1.59661327712456,7.96638697135753));
#44080=CARTESIAN_POINT('Ctrl Pts',(-1.90075606520653,-1.42072024839448,
7.95228721270071));
#44081=CARTESIAN_POINT('Ctrl Pts',(-1.94658175324105,-1.3572535909807,7.94731819457777));
#44082=CARTESIAN_POINT('Ctrl Pts',(-2.0046229189592,-1.26786774288802,7.94039125364936));
#44083=CARTESIAN_POINT('Ctrl Pts',(-2.01963293949227,-1.24381845139883,
7.93853447550187));
#44084=CARTESIAN_POINT('Ctrl Pts',(-2.04452942573839,-1.20228967052306,
7.93533638401601));
#44085=CARTESIAN_POINT('Ctrl Pts',(-2.05463176318525,-1.18494274169053,
7.93400291392176));
#44086=CARTESIAN_POINT('Ctrl Pts',(-2.0747364642462,-1.1493903062716,7.93127367229954));
#44087=CARTESIAN_POINT('Ctrl Pts',(-2.08472226152706,-1.13117749179517,
7.92987746644388));
#44088=CARTESIAN_POINT('Ctrl Pts',(-2.10948045144842,-1.08458014703557,
7.92630893298248));
#44089=CARTESIAN_POINT('Ctrl Pts',(-2.12391959767011,-1.05602426243711,
7.92412540050455));
#44090=CARTESIAN_POINT('Ctrl Pts',(-2.18876632437205,-0.921065493166437,
7.91381623221288));
#44091=CARTESIAN_POINT('Ctrl Pts',(-2.2317767355564,-0.811310732808078,
7.90545059117616));
#44092=CARTESIAN_POINT('Ctrl Pts',(-2.29950494995012,-0.591653742871962,
7.88882900923301));
#44093=CARTESIAN_POINT('Ctrl Pts',(-2.32490698880058,-0.482269670790919,
7.88060883849695));
#44094=CARTESIAN_POINT('Ctrl Pts',(-2.35047194887738,-0.321071218875139,
7.86880966527242));
#44095=CARTESIAN_POINT('Ctrl Pts',(-2.35683956364091,-0.270394110919458,
7.86514610975072));
#44096=CARTESIAN_POINT('Ctrl Pts',(-2.36471438586219,-0.185688753493123,
7.85913521416989));
#44097=CARTESIAN_POINT('Ctrl Pts',(-2.36713384013129,-0.15176331578463,
7.85675775115089));
#44098=CARTESIAN_POINT('Ctrl Pts',(-2.3695518587865,-0.103137917685317,
7.85340336897334));
#44099=CARTESIAN_POINT('Ctrl Pts',(-2.37014470908978,-0.0884733117476614,
7.85239866694298));
#44100=CARTESIAN_POINT('Ctrl Pts',(-2.37094516634511,-0.0627623326196688,
7.85065035756887));
#44101=CARTESIAN_POINT('Ctrl Pts',(-2.37121177635398,-0.0517186674172914,
7.84990372975537));
#44102=CARTESIAN_POINT('Ctrl Pts',(-2.37163109951675,-0.02727032137788,
7.84826053263253));
#44103=CARTESIAN_POINT('Ctrl Pts',(-2.37174735285992,-0.0138657098153779,
7.84736590041356));
#44104=CARTESIAN_POINT('Ctrl Pts',(-2.37175517113766,0.0264064460216114,
7.84469512404593));
#44105=CARTESIAN_POINT('Ctrl Pts',(-2.37130386950719,0.0532728415598212,
7.84293613589667));
#44106=CARTESIAN_POINT('Ctrl Pts',(-2.36935164355241,0.111025454414777,
7.83919283371531));
#44107=CARTESIAN_POINT('Ctrl Pts',(-2.36770310529822,0.141901248863294,
7.83721488955153));
#44108=CARTESIAN_POINT('Ctrl Pts',(-2.36545134965667,0.17273672136364,7.83525515262476));
#44109=CARTESIAN_POINT('Ctrl Pts',(-2.36545135498545,0.17273664839138,7.63805096494753));
#44110=CARTESIAN_POINT('Ctrl Pts',(-2.36969564154637,0.114615494079465,
7.64214124101686));
#44111=CARTESIAN_POINT('Ctrl Pts',(-2.37179705249545,0.056348380075055,
7.64628826398058));
#44112=CARTESIAN_POINT('Ctrl Pts',(-2.37164596878255,-0.127709886715962,
7.65951362959449));
#44113=CARTESIAN_POINT('Ctrl Pts',(-2.36153974571113,-0.253262801395892,
7.66873160391074));
#44114=CARTESIAN_POINT('Ctrl Pts',(-2.32862128519816,-0.457493503369781,
7.68371260501258));
#44115=CARTESIAN_POINT('Ctrl Pts',(-2.31161296451896,-0.536866318069673,
7.68952725375746));
#44116=CARTESIAN_POINT('Ctrl Pts',(-2.2853469329064,-0.63465950711383,7.69656973278061));
#44117=CARTESIAN_POINT('Ctrl Pts',(-2.27987771712292,-0.654034368172074,
7.69795881473493));
#44118=CARTESIAN_POINT('Ctrl Pts',(-2.27068255376979,-0.685090528620246,
7.70017291413598));
#44119=CARTESIAN_POINT('Ctrl Pts',(-2.26711170098149,-0.696816219943959,
7.70100599286095));
#44120=CARTESIAN_POINT('Ctrl Pts',(-2.25986743485643,-0.719959070578163,
7.70264379638817));
#44121=CARTESIAN_POINT('Ctrl Pts',(-2.25619803265587,-0.731377013514615,
7.70344868636484));
#44122=CARTESIAN_POINT('Ctrl Pts',(-2.2465278037122,-0.760702003015854,
7.70550894812826));
#44123=CARTESIAN_POINT('Ctrl Pts',(-2.2403992745425,-0.778566538826394,
7.7067573287942));
#44124=CARTESIAN_POINT('Ctrl Pts',(-2.21128176719794,-0.860251289797022,
7.71244275993688));
#44125=CARTESIAN_POINT('Ctrl Pts',(-2.18577290446614,-0.923145643361853,
7.71675657017447));
#44126=CARTESIAN_POINT('Ctrl Pts',(-2.0833080386943,-1.14762124926618,7.73221111153484));
#44127=CARTESIAN_POINT('Ctrl Pts',(-1.99083931699805,-1.30144906977679,
7.74295817418495));
#44128=CARTESIAN_POINT('Ctrl Pts',(-1.84064497204438,-1.49727434987451,
7.75847953829163));
#44129=CARTESIAN_POINT('Ctrl Pts',(-1.79705069694095,-1.54932628928999,
7.76280725902116));
#44130=CARTESIAN_POINT('Ctrl Pts',(-1.73227507276655,-1.62025182338726,
7.76905481266415));
#44131=CARTESIAN_POINT('Ctrl Pts',(-1.71289370930519,-1.64072786623663,
7.7709026961637));
#44132=CARTESIAN_POINT('Ctrl Pts',(-1.6787799150183,-1.67550509418278,7.77412229560732));
#44133=CARTESIAN_POINT('Ctrl Pts',(-1.66421802662226,-1.6899697155902,7.77548669593648));
#44134=CARTESIAN_POINT('Ctrl Pts',(-1.63383118982182,-1.71937995215943,
7.77831488589928));
#44135=CARTESIAN_POINT('Ctrl Pts',(-1.61798460226904,-1.73430030561914,
7.77977955919315));
#44136=CARTESIAN_POINT('Ctrl Pts',(-1.57631045750859,-1.77247027935652,
7.78360665372633));
#44137=CARTESIAN_POINT('Ctrl Pts',(-1.55017407632125,-1.7953734057534,7.78598289899113));
#44138=CARTESIAN_POINT('Ctrl Pts',(-1.49151540171793,-1.84453964673008,
7.79126698198328));
#44139=CARTESIAN_POINT('Ctrl Pts',(-1.45878340663383,-1.87053343220083,
7.79418401962525));
#44140=CARTESIAN_POINT('Ctrl Pts',(-1.3522332289137,-1.95065109124007,7.80358101733291));
#44141=CARTESIAN_POINT('Ctrl Pts',(-1.27596693791155,-2.00136955097843,
7.81016544377079));
#44142=CARTESIAN_POINT('Ctrl Pts',(-1.06765653125559,-2.12314467568511,
7.82768284562853));
#44143=CARTESIAN_POINT('Ctrl Pts',(-0.931469977135592,-2.18632156072484,
7.83869204615108));
#44144=CARTESIAN_POINT('Ctrl Pts',(-0.76312138283965,-2.24581174228092,
7.8512430068759));
#44145=CARTESIAN_POINT('Ctrl Pts',(-0.735840658237784,-2.25489763171209,
7.85324445091814));
#44146=CARTESIAN_POINT('Ctrl Pts',(-0.695032199689592,-2.26766939983407,
7.85618383034018));
#44147=CARTESIAN_POINT('Ctrl Pts',(-0.681627130546451,-2.2717347434363,
7.8571407255897));
#44148=CARTESIAN_POINT('Ctrl Pts',(-0.658355832589169,-2.27856767124094,
7.85878603650097));
#44149=CARTESIAN_POINT('Ctrl Pts',(-0.648506815866914,-2.28139035537146,
7.85947741973397));
#44150=CARTESIAN_POINT('Ctrl Pts',(-0.62483371581712,-2.28800926160929,
7.86112750599793));
#44151=CARTESIAN_POINT('Ctrl Pts',(-0.610993078232762,-2.29174410382166,
7.86208280696937));
#44152=CARTESIAN_POINT('Ctrl Pts',(-0.567569975762216,-2.30304029914023,
7.86505293303561));
#44153=CARTESIAN_POINT('Ctrl Pts',(-0.537873624393566,-2.31015637273775,
7.86704512408355));
#44154=CARTESIAN_POINT('Ctrl Pts',(-0.465553636509587,-2.32601598385394,
7.87182080459903));
#44155=CARTESIAN_POINT('Ctrl Pts',(-0.422809985104372,-2.33416423601922,
7.87458017118019));
#44156=CARTESIAN_POINT('Ctrl Pts',(-0.228598621890613,-2.36567630713049,
7.88692918202547));
#44157=CARTESIAN_POINT('Ctrl Pts',(-0.0753064098572458,-2.37550301558115,
7.89618393851273));
#44158=CARTESIAN_POINT('Ctrl Pts',(0.169624694623,-2.36745728356231,7.91142775911565));
#44159=CARTESIAN_POINT('Ctrl Pts',(0.261120681090563,-2.35911845059136,
7.91721977463129));
#44160=CARTESIAN_POINT('Ctrl Pts',(0.382374839465579,-2.34092660205461,
7.92516792191327));
#44161=CARTESIAN_POINT('Ctrl Pts',(0.412759534363085,-2.33576054016204,
7.9271823585518));
#44162=CARTESIAN_POINT('Ctrl Pts',(0.461593961683418,-2.32647501784464,
7.93046107111855));
#44163=CARTESIAN_POINT('Ctrl Pts',(0.480110772177981,-2.32272439314004,
7.93171387591075));
#44164=CARTESIAN_POINT('Ctrl Pts',(0.518830169912526,-2.31439891338066,
7.93435472685092));
#44165=CARTESIAN_POINT('Ctrl Pts',(0.539021503823726,-2.30977982672711,
7.93574405480011));
#44166=CARTESIAN_POINT('Ctrl Pts',(0.587632648502854,-2.2979871593182,7.93911960994225));
#44167=CARTESIAN_POINT('Ctrl Pts',(0.615984399798945,-2.29055019645612,
7.94111392619501));
#44168=CARTESIAN_POINT('Ctrl Pts',(0.723396450476649,-2.26023648735781,
7.94877082302968));
#44169=CARTESIAN_POINT('Ctrl Pts',(0.801377070980714,-2.23377786586226,
7.95454327675886));
#44170=CARTESIAN_POINT('Ctrl Pts',(1.03050788939765,-2.14249068864575,7.97214102712916));
#44171=CARTESIAN_POINT('Ctrl Pts',(1.17645690242371,-2.06595140668785,7.98424676714448));
#44172=CARTESIAN_POINT('Ctrl Pts',(1.36724121885025,-1.93908362014461,8.00074901433664));
#44173=CARTESIAN_POINT('Ctrl Pts',(1.41969205063714,-1.901018097494,8.00536054786745));
#44174=CARTESIAN_POINT('Ctrl Pts',(1.48552602775419,-1.848993281622,8.01118725734341));
#44175=CARTESIAN_POINT('Ctrl Pts',(1.50038603632138,-1.83695550678193,8.01250507750834));
#44176=CARTESIAN_POINT('Ctrl Pts',(1.52344906943512,-1.81780603378863,8.01455241612257));
#44177=CARTESIAN_POINT('Ctrl Pts',(1.53175127055003,-1.81081581074017,8.01528984005131));
#44178=CARTESIAN_POINT('Ctrl Pts',(1.54904699417004,-1.79604922335944,8.01682646742827));
#44179=CARTESIAN_POINT('Ctrl Pts',(1.55803055117504,-1.78826178557081,8.01762477042755));
#44180=CARTESIAN_POINT('Ctrl Pts',(1.58074856809176,-1.76826741458194,8.0196450823013));
#44181=CARTESIAN_POINT('Ctrl Pts',(1.59440078030569,-1.75596750746494,8.02086062626168));
#44182=CARTESIAN_POINT('Ctrl Pts',(1.65327649140403,-1.70167082384261,8.02611630101895));
#44183=CARTESIAN_POINT('Ctrl Pts',(1.69699766427537,-1.65807328959127,8.03005495040019));
#44184=CARTESIAN_POINT('Ctrl Pts',(1.83444423949544,-1.50987553642086,8.04275863462969));
#44185=CARTESIAN_POINT('Ctrl Pts',(1.9205914413677,-1.39865721942861,8.05126477026736));
#44186=CARTESIAN_POINT('Ctrl Pts',(2.05297347683027,-1.19225820742046,8.06645018202768));
#44187=CARTESIAN_POINT('Ctrl Pts',(2.10363565199946,-1.1004059149044,8.07302526204957));
#44188=CARTESIAN_POINT('Ctrl Pts',(2.16162641335428,-0.976521331857155,
8.08187980187649));
#44189=CARTESIAN_POINT('Ctrl Pts',(2.17460807708232,-0.947260374851391,
8.08396965671568));
#44190=CARTESIAN_POINT('Ctrl Pts',(2.19520336613113,-0.898181741613311,
8.08747744411587));
#44191=CARTESIAN_POINT('Ctrl Pts',(2.20315045301142,-0.878507992455981,
8.08888422817985));
#44192=CARTESIAN_POINT('Ctrl Pts',(2.21838615907276,-0.839283136580403,
8.09169167190216));
#44193=CARTESIAN_POINT('Ctrl Pts',(2.22568286020632,-0.819737209675419,
8.09309191665765));
#44194=CARTESIAN_POINT('Ctrl Pts',(2.24289023843927,-0.771719012735865,
8.0965362357175));
#44195=CARTESIAN_POINT('Ctrl Pts',(2.25251749986396,-0.74314980117693,8.09858922262866));
#44196=CARTESIAN_POINT('Ctrl Pts',(2.28888139776308,-0.628032488437149,
8.10688030335095));
#44197=CARTESIAN_POINT('Ctrl Pts',(2.31119190450171,-0.540177178709601,
8.113253870805));
#44198=CARTESIAN_POINT('Ctrl Pts',(2.34725336902153,-0.354110555470342,
8.1268268760525));
#44199=CARTESIAN_POINT('Ctrl Pts',(2.35998307784072,-0.255872143085667,
8.13403580336733));
#44200=CARTESIAN_POINT('Ctrl Pts',(2.37365226604275,-0.0500026144207975,
8.1490565709741));
#44201=CARTESIAN_POINT('Ctrl Pts',(2.37348341625518,0.0574954306504039,
8.15685102237765));
#44202=CARTESIAN_POINT('Ctrl Pts',(2.36423809050983,0.19037564767072,8.16618749915465));
#44203=CARTESIAN_POINT('Ctrl Pts',(2.36202556894763,0.216101778496226,8.16798078966887));
#44204=CARTESIAN_POINT('Ctrl Pts',(2.35800700727463,0.255315355196695,8.1706874783744));
#44205=CARTESIAN_POINT('Ctrl Pts',(2.35650437183402,0.268831070883973,8.17161551683453));
#44206=CARTESIAN_POINT('Ctrl Pts',(2.35353748697392,0.293577244666079,8.1733048440311));
#44207=CARTESIAN_POINT('Ctrl Pts',(2.35210898807194,0.304810788808532,8.17406789085659));
#44208=CARTESIAN_POINT('Ctrl Pts',(2.34853564084595,0.331388624277617,8.17586460805309));
#44209=CARTESIAN_POINT('Ctrl Pts',(2.34632082826278,0.34672276961846,8.1768945243763));
#44210=CARTESIAN_POINT('Ctrl Pts',(2.338237176191,0.399059543457767,8.1803901523937));
#44211=CARTESIAN_POINT('Ctrl Pts',(2.33164167447187,0.435946180381342,8.18282035037303));
#44212=CARTESIAN_POINT('Ctrl Pts',(2.31253846050477,0.529880276566465,8.18895841514605));
#44213=CARTESIAN_POINT('Ctrl Pts',(2.29879271471612,0.586651622366909,8.19262009966908));
#44214=CARTESIAN_POINT('Ctrl Pts',(2.23196759388967,0.82396484566138,8.2079340137591));
#44215=CARTESIAN_POINT('Ctrl Pts',(2.15960578153703,0.998348361724775,8.21926382848418));
#44216=CARTESIAN_POINT('Ctrl Pts',(2.04391987270714,1.20411168568955,8.23431180150085));
#44217=CARTESIAN_POINT('Ctrl Pts',(2.01918161697424,1.24514999614181,8.23740135351489));
#44218=CARTESIAN_POINT('Ctrl Pts',(1.97986172581403,1.30612136649654,8.24214586537232));
#44219=CARTESIAN_POINT('Ctrl Pts',(1.96618292678252,1.3266235720469,8.24376867896861));
#44220=CARTESIAN_POINT('Ctrl Pts',(1.94075773319689,1.3634744446508,8.246738088072));
#44221=CARTESIAN_POINT('Ctrl Pts',(1.92911784237151,1.37989399906621,8.24808065421761));
#44222=CARTESIAN_POINT('Ctrl Pts',(1.90332025748293,1.41532034457926,8.25102129431766));
#44223=CARTESIAN_POINT('Ctrl Pts',(1.88908392829844,1.43426689391887,8.25262225017362));
#44224=CARTESIAN_POINT('Ctrl Pts',(1.84733917537291,1.48812340554284,8.2572569771218));
#44225=CARTESIAN_POINT('Ctrl Pts',(1.81913152916892,1.52247605279063,8.26031730590236));
#44226=CARTESIAN_POINT('Ctrl Pts',(1.7316249197129,1.62314018892497,8.26960939772909));
#44227=CARTESIAN_POINT('Ctrl Pts',(1.6695490139937,1.68692385870969,8.2759436405587));
#44228=CARTESIAN_POINT('Ctrl Pts',(1.49951662797459,1.84303671834431,8.29260454631807));
#44229=CARTESIAN_POINT('Ctrl Pts',(1.38658980552346,1.92943062739906,8.30304223665321));
#44230=CARTESIAN_POINT('Ctrl Pts',(1.22122503182619,2.03388551334105,8.31705703773592));
#44231=CARTESIAN_POINT('Ctrl Pts',(1.17486664278883,2.06101192626047,8.32085894779784));
#44232=CARTESIAN_POINT('Ctrl Pts',(1.11171657682316,2.09513991433022,8.325835015011));
#44233=CARTESIAN_POINT('Ctrl Pts',(1.09571090099525,2.10355477186613,8.32707929961259));
#44234=CARTESIAN_POINT('Ctrl Pts',(1.07011744393479,2.11663893401677,8.32904040339933));
#44235=CARTESIAN_POINT('Ctrl Pts',(1.06059207646055,2.12142786331329,8.32976408273877));
#44236=CARTESIAN_POINT('Ctrl Pts',(1.04017066586785,2.13152290924386,8.33130185936936));
#44237=CARTESIAN_POINT('Ctrl Pts',(1.02926552123848,2.13681010613103,8.33211477302627));
#44238=CARTESIAN_POINT('Ctrl Pts',(1.00072291320443,2.15037935197861,8.33422220943636));
#44239=CARTESIAN_POINT('Ctrl Pts',(0.983022682825529,2.15852824186288,8.33550910942496));
#44240=CARTESIAN_POINT('Ctrl Pts',(0.895491942198271,2.19752585908194,8.34178496142611));
#44241=CARTESIAN_POINT('Ctrl Pts',(0.824293947352781,2.2252117998703,8.34661698852776));
#44242=CARTESIAN_POINT('Ctrl Pts',(0.659231984353985,2.28038450036551,8.35747102218209));
#44243=CARTESIAN_POINT('Ctrl Pts',(0.564759026287859,2.30559941016724,8.36343987920138));
#44244=CARTESIAN_POINT('Ctrl Pts',(0.342743285740497,2.35038593267697,8.37739521789696));
#44245=CARTESIAN_POINT('Ctrl Pts',(0.214638188783183,2.36552571928469,8.38540338346822));
#44246=CARTESIAN_POINT('Ctrl Pts',(0.0530895617267232,2.37138367532796,
8.3958574474851));
#44247=CARTESIAN_POINT('Ctrl Pts',(0.0202131137512774,2.37189171318549,
8.39800231243557));
#44248=CARTESIAN_POINT('Ctrl Pts',(-0.0340509465410546,2.37160201001303,
8.40157669179009));
#44249=CARTESIAN_POINT('Ctrl Pts',(-0.0554367298047564,2.37119849032336,
8.40299412389574));
#44250=CARTESIAN_POINT('Ctrl Pts',(-0.0975391702519295,2.36983420820918,
8.40580327672186));
#44251=CARTESIAN_POINT('Ctrl Pts',(-0.118254496977509,2.36889085691657,
8.40719433997542));
#44252=CARTESIAN_POINT('Ctrl Pts',(-0.168348492904814,2.36595093883005,
8.41058098127354));
#44253=CARTESIAN_POINT('Ctrl Pts',(-0.197706879876495,2.36367868314668,
8.41258478020899));
#44254=CARTESIAN_POINT('Ctrl Pts',(-0.310191774486386,2.35286242537215,
8.42033879799712));
#44255=CARTESIAN_POINT('Ctrl Pts',(-0.392879290725077,2.34047508799632,
8.42620261286005));
#44256=CARTESIAN_POINT('Ctrl Pts',(-0.642290695004911,2.28952134777254,
8.44437604281266));
#44257=CARTESIAN_POINT('Ctrl Pts',(-0.805638282673186,2.2372718671673,8.45699196158704));
#44258=CARTESIAN_POINT('Ctrl Pts',(-1.01481840393372,2.14445522883268,8.47342399092133));
#44259=CARTESIAN_POINT('Ctrl Pts',(-1.06682468527166,2.11906366958451,8.47752887289035));
#44260=CARTESIAN_POINT('Ctrl Pts',(-1.13416242524371,2.08307838648856,8.48282524513304));
#44261=CARTESIAN_POINT('Ctrl Pts',(-1.15036873754758,2.07417255572273,8.48409842526894));
#44262=CARTESIAN_POINT('Ctrl Pts',(-1.17581661301567,2.05979819183878,8.4860933211656));
#44263=CARTESIAN_POINT('Ctrl Pts',(-1.18512766426841,2.05445509301553,8.48682230262149));
#44264=CARTESIAN_POINT('Ctrl Pts',(-1.204786015868,2.0429961268592,8.48835891448365));
#44265=CARTESIAN_POINT('Ctrl Pts',(-1.21512375788213,2.03686444915694,8.48916547620686));
#44266=CARTESIAN_POINT('Ctrl Pts',(-1.24169223016957,2.02083149093699,8.49123568267977));
#44267=CARTESIAN_POINT('Ctrl Pts',(-1.25785171772501,2.0108129254032,8.49249220413479));
#44268=CARTESIAN_POINT('Ctrl Pts',(-1.33250806980285,1.96327522922821,8.49829351115728));
#44269=CARTESIAN_POINT('Ctrl Pts',(-1.38946352294843,1.92338772608136,8.50270879454897));
#44270=CARTESIAN_POINT('Ctrl Pts',(-1.59750112761593,1.76362133168454,8.51912281044851));
#44271=CARTESIAN_POINT('Ctrl Pts',(-1.73552178128846,1.62798585545978,8.5306763992787));
#44272=CARTESIAN_POINT('Ctrl Pts',(-1.8915570573266,1.4319714809327,8.54654239017726));
#44273=CARTESIAN_POINT('Ctrl Pts',(-1.92584612712206,1.38551301357996,8.55024574556285));
#44274=CARTESIAN_POINT('Ctrl Pts',(-1.97309190083853,1.31635268208284,8.55571060995324));
#44275=CARTESIAN_POINT('Ctrl Pts',(-1.98742375584441,1.29461297731719,8.55742173148907));
#44276=CARTESIAN_POINT('Ctrl Pts',(-2.01224972916017,1.25557093158282,8.56048559855389));
#44277=CARTESIAN_POINT('Ctrl Pts',(-2.02288594145161,1.23836172515876,8.56183303899265));
#44278=CARTESIAN_POINT('Ctrl Pts',(-2.0449990397418,1.20153791443017,8.56471095382916));
#44279=CARTESIAN_POINT('Ctrl Pts',(-2.05641670523636,1.18189031040987,8.56624336222025));
#44280=CARTESIAN_POINT('Ctrl Pts',(-2.08689607778864,1.12766211278627,8.57046597611491));
#44281=CARTESIAN_POINT('Ctrl Pts',(-2.10537858929404,1.09276610484775,8.57317580482938));
#44282=CARTESIAN_POINT('Ctrl Pts',(-2.14507135880974,1.01307549683747,8.5793509761318));
#44283=CARTESIAN_POINT('Ctrl Pts',(-2.16576548676149,0.968045653083784,
8.58283138115136));
#44284=CARTESIAN_POINT('Ctrl Pts',(-2.24980899744515,0.768959355722094,
8.59817463541804));
#44285=CARTESIAN_POINT('Ctrl Pts',(-2.29823741565605,0.609126018053348,
8.61042233149373));
#44286=CARTESIAN_POINT('Ctrl Pts',(-2.34337050149059,0.37315810509811,8.62778232674803));
#44287=CARTESIAN_POINT('Ctrl Pts',(-2.35383734973825,0.300140048069965,
8.63305077103258));
#44288=CARTESIAN_POINT('Ctrl Pts',(-2.36261357647977,0.208762033060345,
8.639431095488));
#44289=CARTESIAN_POINT('Ctrl Pts',(-2.36413538571208,0.190757491159955,
8.64067795450908));
#44290=CARTESIAN_POINT('Ctrl Pts',(-2.36545134966571,0.172736721239843,
8.64191454572571));
#44291=CARTESIAN_POINT('Origin',(0.,0.,-1.84858989190501));
#44292=CARTESIAN_POINT('',(-2.36545134562115,0.172736776625918,9.83860221205714));
#44293=CARTESIAN_POINT('',(-2.36545135066153,0.172736707603127,9.6385666740965));
#44294=CARTESIAN_POINT('',(-2.36545134966535,0.172736721244682,-1.84858989190501));
#44295=CARTESIAN_POINT('',(-2.37174928960774,0.00183568656896266,8.84980289335711));
#44296=CARTESIAN_POINT('Ctrl Pts',(-2.36545134562115,0.172736776625918,
9.83860221205714));
#44297=CARTESIAN_POINT('Ctrl Pts',(-2.36270050744156,0.210406657936654,
9.83620215240312));
#44298=CARTESIAN_POINT('Ctrl Pts',(-2.35904970563618,0.248012573239168,
9.8337801285158));
#44299=CARTESIAN_POINT('Ctrl Pts',(-2.35079058754754,0.316119639036604,
9.82933468224037));
#44300=CARTESIAN_POINT('Ctrl Pts',(-2.34648425556052,0.346640319302553,
9.82732090913839));
#44301=CARTESIAN_POINT('Ctrl Pts',(-2.33864538914113,0.395319605638881,
9.82407000408802));
#44302=CARTESIAN_POINT('Ctrl Pts',(-2.33549297178358,0.413536447631834,
9.82284465584872));
#44303=CARTESIAN_POINT('Ctrl Pts',(-2.32849878827973,0.451319158251563,
9.82028395987052));
#44304=CARTESIAN_POINT('Ctrl Pts',(-2.32462261746062,0.470877091142648,
9.81894763308492));
#44305=CARTESIAN_POINT('Ctrl Pts',(-2.31480510587413,0.517333685648665,
9.81574654021211));
#44306=CARTESIAN_POINT('Ctrl Pts',(-2.30864092691927,0.544181754669804,
9.81387495945927));
#44307=CARTESIAN_POINT('Ctrl Pts',(-2.28477943873297,0.640394606301797,
9.80708697444798));
#44308=CARTESIAN_POINT('Ctrl Pts',(-2.26441311991512,0.709051318997952,
9.80208899537439));
#44309=CARTESIAN_POINT('Ctrl Pts',(-2.20072850434366,0.892803063625451,
9.78828985711847));
#44310=CARTESIAN_POINT('Ctrl Pts',(-2.15151896239858,1.00561647988228,9.77934296383663));
#44311=CARTESIAN_POINT('Ctrl Pts',(-2.03857427984995,1.21788058930933,9.7618318409391));
#44312=CARTESIAN_POINT('Ctrl Pts',(-1.9757069980223,1.31742382282463,9.75329419851088));
#44313=CARTESIAN_POINT('Ctrl Pts',(-1.89339139947278,1.42852906700827,9.74366631357741));
#44314=CARTESIAN_POINT('Ctrl Pts',(-1.88085491333681,1.44499520874845,9.74223695077601));
#44315=CARTESIAN_POINT('Ctrl Pts',(-1.86062117095188,1.47086179543048,9.73999027065234));
#44316=CARTESIAN_POINT('Ctrl Pts',(-1.85306476463591,1.48037041220486,9.73916410196991));
#44317=CARTESIAN_POINT('Ctrl Pts',(-1.83826240761646,1.49870603613134,9.73757111125329));
#44318=CARTESIAN_POINT('Ctrl Pts',(-1.83102523376705,1.50753940638888,9.73680379237504));
#44319=CARTESIAN_POINT('Ctrl Pts',(-1.81270633540309,1.52957210109908,9.73488927583652));
#44320=CARTESIAN_POINT('Ctrl Pts',(-1.80154373987051,1.54270388166164,9.73374760731058));
#44321=CARTESIAN_POINT('Ctrl Pts',(-1.75528770810446,1.59593305605895,9.72911187892828));
#44322=CARTESIAN_POINT('Ctrl Pts',(-1.71898843840322,1.63496695209525,9.72569339917936));
#44323=CARTESIAN_POINT('Ctrl Pts',(-1.60743111652266,1.74710144017612,9.71569727336568));
#44324=CARTESIAN_POINT('Ctrl Pts',(-1.52860509433746,1.81647112432048,9.70927274410999));
#44325=CARTESIAN_POINT('Ctrl Pts',(-1.33537542780856,1.96500467536336,9.69428831203965));
#44326=CARTESIAN_POINT('Ctrl Pts',(-1.21810517814577,2.03977577559265,9.68572804350183));
#44327=CARTESIAN_POINT('Ctrl Pts',(-1.06143646155453,2.1213157141372,9.67437244120528));
#44328=CARTESIAN_POINT('Ctrl Pts',(-1.02748532640278,2.13796664503385,9.67191754482246));
#44329=CARTESIAN_POINT('Ctrl Pts',(-0.973029592836558,2.16307708760159,
9.66798071826503));
#44330=CARTESIAN_POINT('Ctrl Pts',(-0.952778597555091,2.17207319512371,
9.66651686859763));
#44331=CARTESIAN_POINT('Ctrl Pts',(-0.914394760430712,2.18848439615754,
9.66374102914066));
#44332=CARTESIAN_POINT('Ctrl Pts',(-0.896290215716101,2.19596118830619,
9.66243123263873));
#44333=CARTESIAN_POINT('Ctrl Pts',(-0.854891246715128,2.21246084451294,
9.65943396945349));
#44334=CARTESIAN_POINT('Ctrl Pts',(-0.831543039991164,2.22134151439018,
9.65774199565556));
#44335=CARTESIAN_POINT('Ctrl Pts',(-0.757227346005807,2.24827223840126,
9.65234948064842));
#44336=CARTESIAN_POINT('Ctrl Pts',(-0.705783781283619,2.26494807233927,
9.64860574404602));
#44337=CARTESIAN_POINT('Ctrl Pts',(-0.579238666376462,2.3012388555889,9.63936603286962));
#44338=CARTESIAN_POINT('Ctrl Pts',(-0.503660228994815,2.31895283300851,
9.63382086267452));
#44339=CARTESIAN_POINT('Ctrl Pts',(-0.275644278827654,2.36072169090191,
9.61706958517277));
#44340=CARTESIAN_POINT('Ctrl Pts',(-0.121586092798391,2.37364783199222,
9.60570019123308));
#44341=CARTESIAN_POINT('Ctrl Pts',(0.0745043209719084,2.37094926265457,
9.59174929891972));
#44342=CARTESIAN_POINT('Ctrl Pts',(0.116352444014803,2.36926442102748,9.58880424929518));
#44343=CARTESIAN_POINT('Ctrl Pts',(0.174386803344021,2.36538634230217,9.58478344614116));
#44344=CARTESIAN_POINT('Ctrl Pts',(0.190625796520028,2.36413306474882,9.58366528033896));
#44345=CARTESIAN_POINT('Ctrl Pts',(0.218057287231003,2.36173148816722,9.58178955411183));
#44346=CARTESIAN_POINT('Ctrl Pts',(0.229256670591841,2.36067066810648,9.5810274834417));
#44347=CARTESIAN_POINT('Ctrl Pts',(0.252878045339787,2.35826352434265,9.57942846014892));
#44348=CARTESIAN_POINT('Ctrl Pts',(0.26529755923328,2.3568986780344,9.57859248976774));
#44349=CARTESIAN_POINT('Ctrl Pts',(0.299897820725673,2.35281930454158,9.576275332844));
#44350=CARTESIAN_POINT('Ctrl Pts',(0.322052476829829,2.34988928929035,9.57480522194572));
#44351=CARTESIAN_POINT('Ctrl Pts',(0.372575813571147,2.34247944643263,9.57147695196925));
#44352=CARTESIAN_POINT('Ctrl Pts',(0.400911531880738,2.33779656633737,9.56962789498759));
#44353=CARTESIAN_POINT('Ctrl Pts',(0.497248445979401,2.32007230685416,9.56338035238693));
#44354=CARTESIAN_POINT('Ctrl Pts',(0.564763735187445,2.30456821714492,9.5590679320742));
#44355=CARTESIAN_POINT('Ctrl Pts',(0.803746270857736,2.23855305867927,9.54374650529064));
#44356=CARTESIAN_POINT('Ctrl Pts',(0.970043926634828,2.17166733256299,9.53293075161675));
#44357=CARTESIAN_POINT('Ctrl Pts',(1.16253735612875,2.06768309354584,9.51894100399682));
#44358=CARTESIAN_POINT('Ctrl Pts',(1.1973322815509,2.04773084155132,9.51635086817113));
#44359=CARTESIAN_POINT('Ctrl Pts',(1.25269665527534,2.01408995877829,9.51211782517234));
#44360=CARTESIAN_POINT('Ctrl Pts',(1.27358810668015,2.00094490990692,9.51049394907116));
#44361=CARTESIAN_POINT('Ctrl Pts',(1.31066127777069,1.97680239039825,9.50756198936938));
#44362=CARTESIAN_POINT('Ctrl Pts',(1.32691946359158,1.96592608571232,9.50625840288692));
#44363=CARTESIAN_POINT('Ctrl Pts',(1.36146103620129,1.9421949867402,9.5034493650615));
#44364=CARTESIAN_POINT('Ctrl Pts',(1.37970085826088,1.92928043662882,9.50194177480713));
#44365=CARTESIAN_POINT('Ctrl Pts',(1.42988779852772,1.89267031093537,9.49772401081248));
#44366=CARTESIAN_POINT('Ctrl Pts',(1.46142418337214,1.86842689305581,9.49499338920738));
#44367=CARTESIAN_POINT('Ctrl Pts',(1.53151363736918,1.81168569083562,9.48873578259558));
#44368=CARTESIAN_POINT('Ctrl Pts',(1.56966907965354,1.7787291664496,9.48519260472642));
#44369=CARTESIAN_POINT('Ctrl Pts',(1.69723382146595,1.6612433823564,9.47286948261818));
#44370=CARTESIAN_POINT('Ctrl Pts',(1.78109613134552,1.57099462126244,9.46390578762221));
#44371=CARTESIAN_POINT('Ctrl Pts',(1.9231243329933,1.39208685928815,9.44727246873413));
#44372=CARTESIAN_POINT('Ctrl Pts',(1.98310221828972,1.30522889538571,9.43962257802322));
#44373=CARTESIAN_POINT('Ctrl Pts',(2.05010164696505,1.19286433184417,9.43045558052956));
#44374=CARTESIAN_POINT('Ctrl Pts',(2.06274834906272,1.17085927889165,9.42869331467381));
#44375=CARTESIAN_POINT('Ctrl Pts',(2.08146663801651,1.13704475877193,9.4260397119296));
#44376=CARTESIAN_POINT('Ctrl Pts',(2.0877959088263,1.12538100766158,9.4251340797626));
#44377=CARTESIAN_POINT('Ctrl Pts',(2.09922141537343,1.10389758724809,9.42348450798587));
#44378=CARTESIAN_POINT('Ctrl Pts',(2.10434713881205,1.09409485922022,9.42273889499029));
#44379=CARTESIAN_POINT('Ctrl Pts',(2.11619884701865,1.07103753188662,9.42100124563398));
#44380=CARTESIAN_POINT('Ctrl Pts',(2.12286909686738,1.05775506637138,9.42001253282783));
#44381=CARTESIAN_POINT('Ctrl Pts',(2.14489632760124,1.0128444631606,9.4167077014125));
#44382=CARTESIAN_POINT('Ctrl Pts',(2.15967555931199,0.980936259162319,9.41442287419263));
#44383=CARTESIAN_POINT('Ctrl Pts',(2.25162658892635,0.770252448630054,9.39967037301248));
#44384=CARTESIAN_POINT('Ctrl Pts',(2.30724774696957,0.582867953444738,9.38804546966571));
#44385=CARTESIAN_POINT('Ctrl Pts',(2.35398489395921,0.303081012668453,9.37038258339995));
#44386=CARTESIAN_POINT('Ctrl Pts',(2.36368990795524,0.214640460521849,9.36476610209));
#44387=CARTESIAN_POINT('Ctrl Pts',(2.37000197749197,0.0958706998814639,
9.35705220257052));
#44388=CARTESIAN_POINT('Ctrl Pts',(2.37102612379592,0.0658449271813441,
9.35508789110941));
#44389=CARTESIAN_POINT('Ctrl Pts',(2.37175671902164,0.0174604707631053,
9.351895736216));
#44390=CARTESIAN_POINT('Ctrl Pts',(2.37182081505484,-0.000890064131993465,
9.35067886859219));
#44391=CARTESIAN_POINT('Ctrl Pts',(2.37150938071795,-0.0392817225884852,
9.34811913561296));
#44392=CARTESIAN_POINT('Ctrl Pts',(2.37109273929517,-0.0593209616367282,
9.34677511187267));
#44393=CARTESIAN_POINT('Ctrl Pts',(2.36947963077305,-0.107508127718996,
9.3435230524556));
#44394=CARTESIAN_POINT('Ctrl Pts',(2.36803552972143,-0.13564413609758,9.34160761734316));
#44395=CARTESIAN_POINT('Ctrl Pts',(2.36079395430166,-0.240282697912474,
9.33441911486086));
#44396=CARTESIAN_POINT('Ctrl Pts',(2.35178739339884,-0.31650869089915,9.32905097784582));
#44397=CARTESIAN_POINT('Ctrl Pts',(2.31579802713164,-0.531174582923423,
9.31356420449228));
#44398=CARTESIAN_POINT('Ctrl Pts',(2.28014605224576,-0.667828467604391,
9.30324597625646));
#44399=CARTESIAN_POINT('Ctrl Pts',(2.20095577962291,-0.888690206711893,
9.2862031748829));
#44400=CARTESIAN_POINT('Ctrl Pts',(2.16413116120363,-0.974944346914091,
9.27945422654761));
#44401=CARTESIAN_POINT('Ctrl Pts',(2.11324919574331,-1.07693386461123,9.27152307729709));
#44402=CARTESIAN_POINT('Ctrl Pts',(2.10397028471449,-1.0949510584915,9.27012406548367));
#44403=CARTESIAN_POINT('Ctrl Pts',(2.08880602639335,-1.1234913044795,9.26791382446343));
#44404=CARTESIAN_POINT('Ctrl Pts',(2.08306963689263,-1.13409180883961,9.26709420235118));
#44405=CARTESIAN_POINT('Ctrl Pts',(2.07171387091418,-1.15469970331739,9.26550405715009));
#44406=CARTESIAN_POINT('Ctrl Pts',(2.0661022637037,-1.16471078439809,9.26473314711422));
#44407=CARTESIAN_POINT('Ctrl Pts',(2.05173624496531,-1.18990912131953,9.26279572665168));
#44408=CARTESIAN_POINT('Ctrl Pts',(2.04288549987597,-1.20504116719562,9.26163503396239));
#44409=CARTESIAN_POINT('Ctrl Pts',(2.00497463911275,-1.26823868811787,9.25679317361903));
#44410=CARTESIAN_POINT('Ctrl Pts',(1.97437751565054,-1.31536579168252,9.25319631211771));
#44411=CARTESIAN_POINT('Ctrl Pts',(1.875525925207,-1.45638812724973,9.24233437402656));
#44412=CARTESIAN_POINT('Ctrl Pts',(1.80203098960492,-1.54639944790171,9.23525463550883));
#44413=CARTESIAN_POINT('Ctrl Pts',(1.6293174172416,-1.72881122447544,9.21979336805014));
#44414=CARTESIAN_POINT('Ctrl Pts',(1.52818960089582,-1.81881663940329,9.21141018122371));
#44415=CARTESIAN_POINT('Ctrl Pts',(1.39393444562791,-1.91916654685332,9.20056995388185));
#44416=CARTESIAN_POINT('Ctrl Pts',(1.3675172362166,-1.93807892489162,9.19845058952825));
#44417=CARTESIAN_POINT('Ctrl Pts',(1.32350627133017,-1.96823899044793,9.19493652423275));
#44418=CARTESIAN_POINT('Ctrl Pts',(1.30613715882049,-1.97980788213726,9.19355385942387));
#44419=CARTESIAN_POINT('Ctrl Pts',(1.27181650266675,-2.00201932400792,9.19082857177794));
#44420=CARTESIAN_POINT('Ctrl Pts',(1.25487840794817,-2.01267949010304,9.18948674154045));
#44421=CARTESIAN_POINT('Ctrl Pts',(1.2139248055203,-2.0377361338441,9.18624884619042));
#44422=CARTESIAN_POINT('Ctrl Pts',(1.1897857828507,-2.05192389264015,9.18434554383304));
#44423=CARTESIAN_POINT('Ctrl Pts',(1.09985562970788,-2.10266009807007,9.17727062619719));
#44424=CARTESIAN_POINT('Ctrl Pts',(1.0325928457344,-2.1364952259127,9.17200788030211));
#44425=CARTESIAN_POINT('Ctrl Pts',(0.840061338669288,-2.22212677658948,
9.15702668573074));
#44426=CARTESIAN_POINT('Ctrl Pts',(0.71180009157355,-2.2664698008437,9.14712598959486));
#44427=CARTESIAN_POINT('Ctrl Pts',(0.482730480164854,-2.32429149206015,
9.12994584922038));
#44428=CARTESIAN_POINT('Ctrl Pts',(0.383507563603569,-2.3427090560478,9.12266645747431));
#44429=CARTESIAN_POINT('Ctrl Pts',(0.263154416729208,-2.357194059464,9.11422958443261));
#44430=CARTESIAN_POINT('Ctrl Pts',(0.242872578004368,-2.35937005586239,
9.11282123186898));
#44431=CARTESIAN_POINT('Ctrl Pts',(0.210536987005296,-2.36241786795112,
9.11059979628028));
#44432=CARTESIAN_POINT('Ctrl Pts',(0.198500781770552,-2.36345963818564,
9.10977817956339));
#44433=CARTESIAN_POINT('Ctrl Pts',(0.175034580057199,-2.36531017778293,
9.10818724699811));
#44434=CARTESIAN_POINT('Ctrl Pts',(0.163605842878579,-2.36612816152204,
9.10741750993013));
#44435=CARTESIAN_POINT('Ctrl Pts',(0.134772797036977,-2.36798190863626,
9.10548745284677));
#44436=CARTESIAN_POINT('Ctrl Pts',(0.117361725280073,-2.36890867184927,
9.10433285788303));
#44437=CARTESIAN_POINT('Ctrl Pts',(0.0447678396191601,-2.37197037068075,
9.09955833901055));
#44438=CARTESIAN_POINT('Ctrl Pts',(-0.0104748885017752,-2.37236989014969,
9.09601981523516));
#44439=CARTESIAN_POINT('Ctrl Pts',(-0.177896848822243,-2.36773136469762,
9.08544953002196));
#44440=CARTESIAN_POINT('Ctrl Pts',(-0.289752313701264,-2.35665984568789,
9.07859192665172));
#44441=CARTESIAN_POINT('Ctrl Pts',(-0.527318272950489,-2.31596894895503,
9.06376438725667));
#44442=CARTESIAN_POINT('Ctrl Pts',(-0.652234487547055,-2.28393565129467,
9.05579795693928));
#44443=CARTESIAN_POINT('Ctrl Pts',(-0.809837273814174,-2.22953019097822,
9.04507998303646));
#44444=CARTESIAN_POINT('Ctrl Pts',(-0.84544283577815,-2.21627332269943,
9.04261380548274));
#44445=CARTESIAN_POINT('Ctrl Pts',(-0.901322996518006,-2.19392516319354,
9.03866306388553));
#44446=CARTESIAN_POINT('Ctrl Pts',(-0.921815492790863,-2.18539399381889,
9.03719680538935));
#44447=CARTESIAN_POINT('Ctrl Pts',(-0.958357186485925,-2.16957602425655,
9.03454924420304));
#44448=CARTESIAN_POINT('Ctrl Pts',(-0.974450789235,-2.16239548950957,9.03337156109689));
#44449=CARTESIAN_POINT('Ctrl Pts',(-1.0121996299569,-2.14504598613897,9.03058081650466));
#44450=CARTESIAN_POINT('Ctrl Pts',(-1.03378363103694,-2.13472754850017,
9.02896280660588));
#44451=CARTESIAN_POINT('Ctrl Pts',(-1.09819935279767,-2.10272697265849,
9.0240645511428));
#44452=CARTESIAN_POINT('Ctrl Pts',(-1.14053032554868,-2.08007032434139,
9.02075168815866));
#44453=CARTESIAN_POINT('Ctrl Pts',(-1.37258617161447,-1.94665421909629,
9.00204869593388));
#44454=CARTESIAN_POINT('Ctrl Pts',(-1.54688001653122,-1.81123930582838,
8.98579199854102));
#44455=CARTESIAN_POINT('Ctrl Pts',(-1.74126217921008,-1.61142898912077,
8.96576133403349));
#44456=CARTESIAN_POINT('Ctrl Pts',(-1.78091403174461,-1.56749602011773,
8.96156117454602));
#44457=CARTESIAN_POINT('Ctrl Pts',(-1.83061712209207,-1.50810252738383,
8.95618849039318));
#44458=CARTESIAN_POINT('Ctrl Pts',(-1.8421877198278,-1.49394669793652,8.95492958640676));
#44459=CARTESIAN_POINT('Ctrl Pts',(-1.86013185161236,-1.47146776427559,
8.95296602716394));
#44460=CARTESIAN_POINT('Ctrl Pts',(-1.866615601405,-1.46323412131904,8.95225416216658));
#44461=CARTESIAN_POINT('Ctrl Pts',(-1.88012729557723,-1.4458397946568,8.95076612831986));
#44462=CARTESIAN_POINT('Ctrl Pts',(-1.88714331607727,-1.43667027293165,
8.94999084636571));
#44463=CARTESIAN_POINT('Ctrl Pts',(-1.90485056480025,-1.41317441048455,
8.94802642209817));
#44464=CARTESIAN_POINT('Ctrl Pts',(-1.91544756830534,-1.39877741208341,
8.94684343973901));
#44465=CARTESIAN_POINT('Ctrl Pts',(-1.96078173005553,-1.33570536164168,
8.94174353341617));
#44466=CARTESIAN_POINT('Ctrl Pts',(-1.99383663185622,-1.28584234999697,
8.93792256592909));
#44467=CARTESIAN_POINT('Ctrl Pts',(-2.07225254057941,-1.15724429647089,
8.92844524260235));
#44468=CARTESIAN_POINT('Ctrl Pts',(-2.11504147136868,-1.07705438838185,
8.92287064418814));
#44469=CARTESIAN_POINT('Ctrl Pts',(-2.21585241640659,-0.858818090973323,
8.90809257166433));
#44470=CARTESIAN_POINT('Ctrl Pts',(-2.26558509578718,-0.717417723420512,
8.89888880217024));
#44471=CARTESIAN_POINT('Ctrl Pts',(-2.31030672126261,-0.53755170271021,
8.88694363773667));
#44472=CARTESIAN_POINT('Ctrl Pts',(-2.31815487282011,-0.502629834645124,
8.88461527215623));
#44473=CARTESIAN_POINT('Ctrl Pts',(-2.32945614205047,-0.446426025598749,
8.88084620698829));
#44474=CARTESIAN_POINT('Ctrl Pts',(-2.33341466301461,-0.425250601657645,
8.87942129469152));
#44475=CARTESIAN_POINT('Ctrl Pts',(-2.34030328579034,-0.385403313807903,
8.87672939529146));
#44476=CARTESIAN_POINT('Ctrl Pts',(-2.34329972388754,-0.366744533584877,
8.87546458485171));
#44477=CARTESIAN_POINT('Ctrl Pts',(-2.34888497990102,-0.329096702985042,
8.87290310592351));
#44478=CARTESIAN_POINT('Ctrl Pts',(-2.35146724466143,-0.310108125147207,
8.8716063360082));
#44479=CARTESIAN_POINT('Ctrl Pts',(-2.35689798317458,-0.266194076338138,
8.86859550506835));
#44480=CARTESIAN_POINT('Ctrl Pts',(-2.35958159577236,-0.241250908077913,
8.86687656214506));
#44481=CARTESIAN_POINT('Ctrl Pts',(-2.36850940866389,-0.143751205703641,
8.86012153730056));
#44482=CARTESIAN_POINT('Ctrl Pts',(-2.37180564160149,-0.0709723861126348,
8.85500019683922));
#44483=CARTESIAN_POINT('Ctrl Pts',(-2.37174928960774,0.00183568656896266,
8.84980289335711));
#44484=CARTESIAN_POINT('Ctrl Pts',(-2.37174929161342,0.00183309335181954,
8.8498030784703));
#44485=CARTESIAN_POINT('Ctrl Pts',(-2.37170518086058,0.0589058260080911,
8.84572902179415));
#44486=CARTESIAN_POINT('Ctrl Pts',(-2.3696010754449,0.11591062296176,8.84161489479427));
#44487=CARTESIAN_POINT('Ctrl Pts',(-2.36545132340079,0.172737080910408,
8.8374806621729));
#44488=CARTESIAN_POINT('',(-2.37175040066033,0.000883970845875868,8.65336333906485));
#44489=CARTESIAN_POINT('Ctrl Pts',(-2.36545134966571,0.172736721239843,
8.64191454572571));
#44490=CARTESIAN_POINT('Ctrl Pts',(-2.36557018947359,0.171109332564596,
8.64202621767707));
#44491=CARTESIAN_POINT('Ctrl Pts',(-2.36568735056825,0.169481811544686,
8.6421378058687));
#44492=CARTESIAN_POINT('Ctrl Pts',(-2.36666375034735,0.15572004744893,8.64308056562317));
#44493=CARTESIAN_POINT('Ctrl Pts',(-2.3674313260975,0.1435791522688,8.64390708121543));
#44494=CARTESIAN_POINT('Ctrl Pts',(-2.3686911561697,0.120879978181028,8.64544199252111));
#44495=CARTESIAN_POINT('Ctrl Pts',(-2.36920630706136,0.110323373530993,
8.64615162813759));
#44496=CARTESIAN_POINT('Ctrl Pts',(-2.37029459880395,0.0844735103778954,
8.64787979921009));
#44497=CARTESIAN_POINT('Ctrl Pts',(-2.37079033270636,0.0691772150860396,
8.64889428094819));
#44498=CARTESIAN_POINT('Ctrl Pts',(-2.3715392963827,0.0362149919024032,
8.65106492675962));
#44499=CARTESIAN_POINT('Ctrl Pts',(-2.37174326919453,0.0185488449211695,
8.65221871811156));
#44500=CARTESIAN_POINT('Ctrl Pts',(-2.37174983615641,0.000881584965583026,
8.65336447339507));
#44501=CARTESIAN_POINT('Ctrl Pts',(-2.37174983524487,0.000884033889070948,
8.65336431457769));
#44502=CARTESIAN_POINT('Ctrl Pts',(-2.37179372306343,-0.116861368983434,
8.66100033204862));
#44503=CARTESIAN_POINT('Ctrl Pts',(-2.36306931368071,-0.234464575574185,
8.66827214436893));
#44504=CARTESIAN_POINT('Ctrl Pts',(-2.32974670086994,-0.457183799256998,
8.68213251040277));
#44505=CARTESIAN_POINT('Ctrl Pts',(-2.30665348437395,-0.562214556911442,
8.68870951212139));
#44506=CARTESIAN_POINT('Ctrl Pts',(-2.25533256558931,-0.737820610276738,
8.70017655204398));
#44507=CARTESIAN_POINT('Ctrl Pts',(-2.23069258861883,-0.809267053886955,
8.70497970519907));
#44508=CARTESIAN_POINT('Ctrl Pts',(-2.19210784323786,-0.905911386254933,
8.7117450238051));
#44509=CARTESIAN_POINT('Ctrl Pts',(-2.1810509698559,-0.932217137115946,
8.71361453659954));
#44510=CARTESIAN_POINT('Ctrl Pts',(-2.16120708480675,-0.977141515638886,
8.71685941333449));
#44511=CARTESIAN_POINT('Ctrl Pts',(-2.15264713529207,-0.995857355066325,
8.71822713532883));
#44512=CARTESIAN_POINT('Ctrl Pts',(-2.13569477445129,-1.03168259252301,
8.72087710551277));
#44513=CARTESIAN_POINT('Ctrl Pts',(-2.12733755885752,-1.04880694894374,
8.72215807955269));
#44514=CARTESIAN_POINT('Ctrl Pts',(-2.10450477690648,-1.09419655689606,
8.72559273890156));
#44515=CARTESIAN_POINT('Ctrl Pts',(-2.08966676137337,-1.12227408491665,
8.7277586362397));
#44516=CARTESIAN_POINT('Ctrl Pts',(-2.02534606750555,-1.23828571285982,
8.73688629157932));
#44517=CARTESIAN_POINT('Ctrl Pts',(-1.97084741425494,-1.32330420913838,
8.7440179199265));
#44518=CARTESIAN_POINT('Ctrl Pts',(-1.82580459678857,-1.52065241319603,
8.76163722084073));
#44519=CARTESIAN_POINT('Ctrl Pts',(-1.73010907691664,-1.62870087703635,
8.77223096655667));
#44520=CARTESIAN_POINT('Ctrl Pts',(-1.57975788007769,-1.77015732066095,
8.78707924861977));
#44521=CARTESIAN_POINT('Ctrl Pts',(-1.53263614208144,-1.8111100818324,8.79151436243348));
#44522=CARTESIAN_POINT('Ctrl Pts',(-1.46956886898191,-1.86169419190209,
8.79712217679343));
#44523=CARTESIAN_POINT('Ctrl Pts',(-1.45505322777612,-1.87306115247112,
8.79839144269398));
#44524=CARTESIAN_POINT('Ctrl Pts',(-1.43095142528555,-1.89148558168181,
8.80046201231934));
#44525=CARTESIAN_POINT('Ctrl Pts',(-1.42144226626367,-1.89864203898062,
8.8012696682457));
#44526=CARTESIAN_POINT('Ctrl Pts',(-1.40193643119075,-1.91309315699462,
8.80290693580885));
#44527=CARTESIAN_POINT('Ctrl Pts',(-1.39193581805137,-1.92038170161609,
8.80373616127631));
#44528=CARTESIAN_POINT('Ctrl Pts',(-1.36507154225771,-1.93964053019555,
8.80593793641216));
#44529=CARTESIAN_POINT('Ctrl Pts',(-1.34810719074599,-1.95146938849341,
8.80730156187858));
#44530=CARTESIAN_POINT('Ctrl Pts',(-1.25178032569586,-2.01678020694889,
8.81490849064949));
#44531=CARTESIAN_POINT('Ctrl Pts',(-1.16938383968617,-2.06564806790555,
8.82090428927282));
#44532=CARTESIAN_POINT('Ctrl Pts',(-0.961455990256574,-2.17252454134085,
8.83537702358837));
#44533=CARTESIAN_POINT('Ctrl Pts',(-0.833387212095843,-2.22479794335441,
8.84376176089531));
#44534=CARTESIAN_POINT('Ctrl Pts',(-0.628678541069258,-2.28818105717448,
8.85718879052238));
#44535=CARTESIAN_POINT('Ctrl Pts',(-0.554819532077321,-2.307202388462,8.8620343896621));
#44536=CARTESIAN_POINT('Ctrl Pts',(-0.452153228605651,-2.32842746618177,
8.86884935434976));
#44537=CARTESIAN_POINT('Ctrl Pts',(-0.424027102977316,-2.33371333074984,
8.87072416419694));
#44538=CARTESIAN_POINT('Ctrl Pts',(-0.375507928059135,-2.34192569762119,
8.8739752535841));
#44539=CARTESIAN_POINT('Ctrl Pts',(-0.355159340236062,-2.34509786062143,
8.8753438108793));
#44540=CARTESIAN_POINT('Ctrl Pts',(-0.315927280468617,-2.3506914683562,
8.87799329472398));
#44541=CARTESIAN_POINT('Ctrl Pts',(-0.297050832954015,-2.35315133232896,
8.87927292233956));
#44542=CARTESIAN_POINT('Ctrl Pts',(-0.24671780393453,-2.35909516017397,
8.88269880868327));
#44543=CARTESIAN_POINT('Ctrl Pts',(-0.215218554301381,-2.36217705923991,
8.8848571642157));
#44544=CARTESIAN_POINT('Ctrl Pts',(-0.0838762823906145,-2.37237884054155,
8.89392096761391));
#44545=CARTESIAN_POINT('Ctrl Pts',(0.0162936412259015,-2.37380424034094,
8.90099343632069));
#44546=CARTESIAN_POINT('Ctrl Pts',(0.260961529613066,-2.36179824181781,
8.91861049124884));
#44547=CARTESIAN_POINT('Ctrl Pts',(0.404717249582548,-2.34145113839692,
8.92926756455896));
#44548=CARTESIAN_POINT('Ctrl Pts',(0.606593221353358,-2.29372103237233,
8.94418929212688));
#44549=CARTESIAN_POINT('Ctrl Pts',(0.6668846373904,-2.2769228736431,8.94863589387079));
#44550=CARTESIAN_POINT('Ctrl Pts',(0.744008509792408,-2.25210785072657,
8.9542556831629));
#44551=CARTESIAN_POINT('Ctrl Pts',(0.761505107755759,-2.24625209106925,
8.95552592393854));
#44552=CARTESIAN_POINT('Ctrl Pts',(0.790175382134453,-2.23628321527518,
8.95759765456637));
#44553=CARTESIAN_POINT('Ctrl Pts',(0.80138933509745,-2.23228916322732,8.95840551013263));
#44554=CARTESIAN_POINT('Ctrl Pts',(0.82419491735044,-2.22397253302153,8.960042726459));
#44555=CARTESIAN_POINT('Ctrl Pts',(0.835783647940387,-2.21964339484492,
8.96087170620349));
#44556=CARTESIAN_POINT('Ctrl Pts',(0.866636296614415,-2.20784204438973,
8.9630720696475));
#44557=CARTESIAN_POINT('Ctrl Pts',(0.885837808127657,-2.20020826541884,
8.96443454910261));
#44558=CARTESIAN_POINT('Ctrl Pts',(0.992939094369361,-2.15599947078173,
8.97200812964924));
#44559=CARTESIAN_POINT('Ctrl Pts',(1.0786836597914,-2.11440473670555,8.97797432928183));
#44560=CARTESIAN_POINT('Ctrl Pts',(1.2824185670099,-1.99994307935794,8.9924429385108));
#44561=CARTESIAN_POINT('Ctrl Pts',(1.39696015664093,-1.92168459733474,9.00085057921141));
#44562=CARTESIAN_POINT('Ctrl Pts',(1.56304481093426,-1.78547365322691,9.01430822075435));
#44563=CARTESIAN_POINT('Ctrl Pts',(1.61969281526299,-1.73424875426698,9.01916024509753));
#44564=CARTESIAN_POINT('Ctrl Pts',(1.69405320708211,-1.66018115116672,9.02598271818351));
#44565=CARTESIAN_POINT('Ctrl Pts',(1.71396913253943,-1.63961197313436,9.02785832085443));
#44566=CARTESIAN_POINT('Ctrl Pts',(1.74756373403812,-1.60363438986966,9.03111033678072));
#44567=CARTESIAN_POINT('Ctrl Pts',(1.76142321988089,-1.58839870844333,9.03247901567897));
#44568=CARTESIAN_POINT('Ctrl Pts',(1.78770516075917,-1.5587400599745,9.03512841865597));
#44569=CARTESIAN_POINT('Ctrl Pts',(1.80015590011304,-1.54434420254431,9.03640784007747));
#44570=CARTESIAN_POINT('Ctrl Pts',(1.83283443706518,-1.50562829084868,9.03983239979772));
#44571=CARTESIAN_POINT('Ctrl Pts',(1.85275064788113,-1.48105148347431,9.04198961763356));
#44572=CARTESIAN_POINT('Ctrl Pts',(1.93332650582873,-1.37745064778358,9.05101943219595));
#44573=CARTESIAN_POINT('Ctrl Pts',(1.98946184425113,-1.29505164227659,9.05805728880425));
#44574=CARTESIAN_POINT('Ctrl Pts',(2.11434220414787,-1.0843757392714,9.07566759371563));
#44575=CARTESIAN_POINT('Ctrl Pts',(2.17679015512256,-0.952835703272854,
9.08635593936601));
#44576=CARTESIAN_POINT('Ctrl Pts',(2.24836738241969,-0.757604949658079,
9.10131389948319));
#44577=CARTESIAN_POINT('Ctrl Pts',(2.26759166227018,-0.697961736111654,
9.10576613665012));
#44578=CARTESIAN_POINT('Ctrl Pts',(2.28939501658166,-0.619846061076553,
9.11139179506727));
#44579=CARTESIAN_POINT('Ctrl Pts',(2.29414923065706,-0.602011661625137,
9.11266250966497));
#44580=CARTESIAN_POINT('Ctrl Pts',(2.30162688783925,-0.572584888065648,
9.11473480246667));
#44581=CARTESIAN_POINT('Ctrl Pts',(2.30447201778613,-0.561024531815689,
9.11554275299629));
#44582=CARTESIAN_POINT('Ctrl Pts',(2.31009538771382,-0.537410775497299,
9.11717993898898));
#44583=CARTESIAN_POINT('Ctrl Pts',(2.31286660472596,-0.525356191280125,
9.11800879596065));
#44584=CARTESIAN_POINT('Ctrl Pts',(2.32001301190973,-0.4931168447722,9.12020845899542));
#44585=CARTESIAN_POINT('Ctrl Pts',(2.32421918116902,-0.472895195337293,
9.12157037066672));
#44586=CARTESIAN_POINT('Ctrl Pts',(2.34626273956681,-0.359508893452298,
9.12912068675838));
#44587=CARTESIAN_POINT('Ctrl Pts',(2.35876464196294,-0.26538439971447,9.13506603029884));
#44588=CARTESIAN_POINT('Ctrl Pts',(2.37558356834476,-0.0323788539098895,
9.14953148894067));
#44589=CARTESIAN_POINT('Ctrl Pts',(2.37341128534998,0.106603224990083,9.15795502267828));
#44590=CARTESIAN_POINT('Ctrl Pts',(2.35122358668863,0.320599429235769,9.17143390718812));
#44591=CARTESIAN_POINT('Ctrl Pts',(2.33967620201412,0.396169060316314,9.17629038752998));
#44592=CARTESIAN_POINT('Ctrl Pts',(2.31881537652723,0.499112683783822,9.18311807043744));
#44593=CARTESIAN_POINT('Ctrl Pts',(2.31261990620061,0.527074261853204,9.1849942253064));
#44594=CARTESIAN_POINT('Ctrl Pts',(2.30110068735885,0.574941690245038,9.18824688892575));
#44595=CARTESIAN_POINT('Ctrl Pts',(2.29602096949749,0.594903339868322,9.18961565491708));
#44596=CARTESIAN_POINT('Ctrl Pts',(2.28574889139593,0.633176316492555,9.19226500806614));
#44597=CARTESIAN_POINT('Ctrl Pts',(2.28059481982479,0.651496334873831,9.1935442899917));
#44598=CARTESIAN_POINT('Ctrl Pts',(2.26629173182967,0.700085499829344,9.19696794194264));
#44599=CARTESIAN_POINT('Ctrl Pts',(2.25675715943362,0.730236181229485,9.19912437961339));
#44600=CARTESIAN_POINT('Ctrl Pts',(2.21479559465308,0.854247690298336,9.20813151502607));
#44601=CARTESIAN_POINT('Ctrl Pts',(2.17709641091932,0.946205802471104,9.21514630375487));
#44602=CARTESIAN_POINT('Ctrl Pts',(2.07018457269287,1.16650370500511,9.23275207975238));
#44603=CARTESIAN_POINT('Ctrl Pts',(1.99469629829437,1.29134783978998,9.24346124788048));
#44604=CARTESIAN_POINT('Ctrl Pts',(1.88293945247744,1.44275855791601,9.25699879074772));
#44605=CARTESIAN_POINT('Ctrl Pts',(1.85671778152915,1.47635114754548,9.26003905496627));
#44606=CARTESIAN_POINT('Ctrl Pts',(1.81046376490667,1.53242414630268,9.26515549960008));
#44607=CARTESIAN_POINT('Ctrl Pts',(1.79088277782216,1.55526264173026,9.26725180693668));
#44608=CARTESIAN_POINT('Ctrl Pts',(1.76139038974623,1.5883655434728,9.27030135519299));
#44609=CARTESIAN_POINT('Ctrl Pts',(1.75181318207251,1.59892207601551,9.27127557035272));
#44610=CARTESIAN_POINT('Ctrl Pts',(1.73519140684872,1.61691488234794,9.27293805111133));
#44611=CARTESIAN_POINT('Ctrl Pts',(1.72819313902993,1.62439263724029,9.27362951982974));
#44612=CARTESIAN_POINT('Ctrl Pts',(1.71145629477165,1.64204560329323,9.27526326004018));
#44613=CARTESIAN_POINT('Ctrl Pts',(1.70167522968684,1.65217972663099,9.27620236640042));
#44614=CARTESIAN_POINT('Ctrl Pts',(1.67136831838386,1.68302592076169,9.27906686687213));
#44615=CARTESIAN_POINT('Ctrl Pts',(1.65054953055276,1.70344789586658,9.28097186207313));
#44616=CARTESIAN_POINT('Ctrl Pts',(1.52082225668994,1.82609045261793,9.29250554138645));
#44617=CARTESIAN_POINT('Ctrl Pts',(1.40282373501614,1.91822897164638,9.30159404090192));
#44618=CARTESIAN_POINT('Ctrl Pts',(1.19992450246832,2.04785973213286,9.31641544467116));
#44619=CARTESIAN_POINT('Ctrl Pts',(1.12014419618952,2.09256391138063,9.32206467321359));
#44620=CARTESIAN_POINT('Ctrl Pts',(0.983638335424083,2.15900611353173,9.33166200283295));
#44621=CARTESIAN_POINT('Ctrl Pts',(0.928300954092049,2.18337083378392,9.33553417123717));
#44622=CARTESIAN_POINT('Ctrl Pts',(0.847485857200007,2.21532529709751,9.34120057415677));
#44623=CARTESIAN_POINT('Ctrl Pts',(0.822714730877479,2.22464352900618,9.34293879377814));
#44624=CARTESIAN_POINT('Ctrl Pts',(0.778696262658941,2.24036636150025,9.34603282140109));
#44625=CARTESIAN_POINT('Ctrl Pts',(0.75951269160746,2.24694230721723,9.34738293179338));
#44626=CARTESIAN_POINT('Ctrl Pts',(0.718878956443703,2.26029135522454,9.35024743744187));
#44627=CARTESIAN_POINT('Ctrl Pts',(0.69741214219613,2.26700688339401,9.35176352790779));
#44628=CARTESIAN_POINT('Ctrl Pts',(0.639108837106248,2.28433961300818,9.35589018287369));
#44629=CARTESIAN_POINT('Ctrl Pts',(0.60210649530224,2.29437029529611,9.35851888894639));
#44630=CARTESIAN_POINT('Ctrl Pts',(0.412817780964479,2.34078890277546,9.37202261613574));
#44631=CARTESIAN_POINT('Ctrl Pts',(0.257460687460128,2.36292417204575,9.38332623428927));
#44632=CARTESIAN_POINT('Ctrl Pts',(-0.0282386144223951,2.37511159089061,
9.40414739207685));
#44633=CARTESIAN_POINT('Ctrl Pts',(-0.157805640889021,2.37003283343738,
9.41359046922257));
#44634=CARTESIAN_POINT('Ctrl Pts',(-0.309053741926881,2.35163949504515,
9.42422816095906));
#44635=CARTESIAN_POINT('Ctrl Pts',(-0.331747316249773,2.34854558030169,
9.4258135312875));
#44636=CARTESIAN_POINT('Ctrl Pts',(-0.367094058144187,2.34320400362349,
9.42826252557851));
#44637=CARTESIAN_POINT('Ctrl Pts',(-0.379779172827328,2.341181507056,9.42913730598617));
#44638=CARTESIAN_POINT('Ctrl Pts',(-0.403794872948664,2.33715214493119,
9.43078488082172));
#44639=CARTESIAN_POINT('Ctrl Pts',(-0.415128152612725,2.33516574788753,
9.43155866692182));
#44640=CARTESIAN_POINT('Ctrl Pts',(-0.443095402285866,2.33005385449331,
9.43345976999947));
#44641=CARTESIAN_POINT('Ctrl Pts',(-0.459711590970065,2.32683256675571,
9.4345819738873));
#44642=CARTESIAN_POINT('Ctrl Pts',(-0.5198423245129,2.31450606222062,9.4386211606779));
#44643=CARTESIAN_POINT('Ctrl Pts',(-0.563135752546555,2.30435523368947,
9.44148772379871));
#44644=CARTESIAN_POINT('Ctrl Pts',(-0.752024240275808,2.25442514980073,
9.4539118565018));
#44645=CARTESIAN_POINT('Ctrl Pts',(-0.893923667037494,2.20201742940164,
9.46304575106073));
#44646=CARTESIAN_POINT('Ctrl Pts',(-1.11259142243794,2.09660857354435,9.47804454533811));
#44647=CARTESIAN_POINT('Ctrl Pts',(-1.19290316324345,2.05197638749887,9.48377096393206));
#44648=CARTESIAN_POINT('Ctrl Pts',(-1.30789038000232,1.97903754157429,9.4924803630756));
#44649=CARTESIAN_POINT('Ctrl Pts',(-1.34468264219999,1.95422491990727,9.49534967173548));
#44650=CARTESIAN_POINT('Ctrl Pts',(-1.40001262852944,1.91460796245393,9.49980780081128));
#44651=CARTESIAN_POINT('Ctrl Pts',(-1.4190614144967,1.90053246377956,9.50136969980118));
#44652=CARTESIAN_POINT('Ctrl Pts',(-1.45390187939598,1.87397237895215,9.50427900686337));
#44653=CARTESIAN_POINT('Ctrl Pts',(-1.46975168775729,1.86156737360077,9.50562328073469));
#44654=CARTESIAN_POINT('Ctrl Pts',(-1.50466691632841,1.83351676496829,9.50863232706772));
#44655=CARTESIAN_POINT('Ctrl Pts',(-1.52364981087767,1.81777265694587,9.51030087207649));
#44656=CARTESIAN_POINT('Ctrl Pts',(-1.57171738282024,1.77662422136479,9.51461222496199));
#44657=CARTESIAN_POINT('Ctrl Pts',(-1.60043242356906,1.75080122218608,9.5172714780035));
#44658=CARTESIAN_POINT('Ctrl Pts',(-1.75980516826424,1.6002818864886,9.53252235407453));
#44659=CARTESIAN_POINT('Ctrl Pts',(-1.87649555236717,1.46169794568453,9.54569198610676));
#44660=CARTESIAN_POINT('Ctrl Pts',(-2.0145653845745,1.25359926660599,9.5638493504636));
#44661=CARTESIAN_POINT('Ctrl Pts',(-2.05027710838781,1.19429880409366,9.56885668814467));
#44662=CARTESIAN_POINT('Ctrl Pts',(-2.1033595398428,1.09673615524912,9.57675286767496));
#44663=CARTESIAN_POINT('Ctrl Pts',(-2.12239628268073,1.05942723080523,9.57969602322076));
#44664=CARTESIAN_POINT('Ctrl Pts',(-2.1473884429696,1.00706574991752,9.58370371718454));
#44665=CARTESIAN_POINT('Ctrl Pts',(-2.1541919649714,0.992429122613123,9.58481097094586));
#44666=CARTESIAN_POINT('Ctrl Pts',(-2.16558682494587,0.967245591501632,
9.58669251750971));
#44667=CARTESIAN_POINT('Ctrl Pts',(-2.17025171679305,0.95673289831598,9.58747095952193));
#44668=CARTESIAN_POINT('Ctrl Pts',(-2.18012977117355,0.934027860484056,
9.58913685060091));
#44669=CARTESIAN_POINT('Ctrl Pts',(-2.18531742133855,0.921825174228508,
9.59002285352634));
#44670=CARTESIAN_POINT('Ctrl Pts',(-2.19968876111952,0.887216843486742,
9.59251117304434));
#44671=CARTESIAN_POINT('Ctrl Pts',(-2.20863233727088,0.864712484018269,
9.5941004253458));
#44672=CARTESIAN_POINT('Ctrl Pts',(-2.26708116695001,0.710813311491544,
9.6047997574685));
#44673=CARTESIAN_POINT('Ctrl Pts',(-2.30518410320021,0.575368198759008,
9.61339651281581));
#44674=CARTESIAN_POINT('Ctrl Pts',(-2.34749610666244,0.349836134732319,
9.62750854484987));
#44675=CARTESIAN_POINT('Ctrl Pts',(-2.35896962915478,0.261497209672887,
9.6329851523993));
#44676=CARTESIAN_POINT('Ctrl Pts',(-2.36545135066152,0.172736707603127,
9.6385666740965));
#44677=CARTESIAN_POINT('Origin',(0.,0.,-1.84858989190501));
#44678=CARTESIAN_POINT('',(-2.36545134966486,0.172736721251459,10.8348238720555));
#44679=CARTESIAN_POINT('',(-2.36545136240482,0.172736546790724,10.6389210243916));
#44680=CARTESIAN_POINT('',(-2.36545134966535,0.172736721244682,-1.84858989190501));
#44681=CARTESIAN_POINT('Ctrl Pts',(-2.36545134966486,0.172736721251459,
10.8348238720555));
#44682=CARTESIAN_POINT('Ctrl Pts',(-2.3648141310891,0.18146277283564,10.8342459745555));
#44683=CARTESIAN_POINT('Ctrl Pts',(-2.3641286153735,0.190185463792282,10.8336704060082));
#44684=CARTESIAN_POINT('Ctrl Pts',(-2.35774171655097,0.266075007693205,
10.8286796145128));
#44685=CARTESIAN_POINT('Ctrl Pts',(-2.34922700958003,0.332980587207781,
10.8243938670154));
#44686=CARTESIAN_POINT('Ctrl Pts',(-2.30931187874156,0.566599868191367,
10.8095534952512));
#44687=CARTESIAN_POINT('Ctrl Pts',(-2.26290578278085,0.730217755192301,
10.799351455385));
#44688=CARTESIAN_POINT('Ctrl Pts',(-2.17056280845768,0.959068574332726,
10.7838965278587));
#44689=CARTESIAN_POINT('Ctrl Pts',(-2.13820686814942,1.02918660912107,10.7789918880586));
#44690=CARTESIAN_POINT('Ctrl Pts',(-2.08940851850851,1.12266178918704,10.7721370901271));
#44691=CARTESIAN_POINT('Ctrl Pts',(-2.07587748434274,1.14748856672506,10.7702848726713));
#44692=CARTESIAN_POINT('Ctrl Pts',(-2.05197197303922,1.18954327629968,10.7670893754009));
#44693=CARTESIAN_POINT('Ctrl Pts',(-2.04181609014105,1.20689237179421,10.7657538211073));
#44694=CARTESIAN_POINT('Ctrl Pts',(-2.02066802775424,1.24198811468645,10.763015454579));
#44695=CARTESIAN_POINT('Ctrl Pts',(-2.0096596602795,1.25972288941445,10.7616121501886));
#44696=CARTESIAN_POINT('Ctrl Pts',(-1.98101498902868,1.30453900453872,10.7580145626201));
#44697=CARTESIAN_POINT('Ctrl Pts',(-1.96305710380138,1.33140866517373,10.7558088039106));
#44698=CARTESIAN_POINT('Ctrl Pts',(-1.8710470939999,1.4631697756384,10.7447411160274));
#44699=CARTESIAN_POINT('Ctrl Pts',(-1.78912234796644,1.56227885267622,10.735590339397));
#44700=CARTESIAN_POINT('Ctrl Pts',(-1.61550699902938,1.74065198449498,10.7175537602029));
#44701=CARTESIAN_POINT('Ctrl Pts',(-1.52495534534345,1.82050650707048,10.708714496717));
#44702=CARTESIAN_POINT('Ctrl Pts',(-1.38304871472863,1.92760183507202,10.6959616385389));
#44703=CARTESIAN_POINT('Ctrl Pts',(-1.33613639479233,1.96041149267173,10.6919059437773));
#44704=CARTESIAN_POINT('Ctrl Pts',(-1.27323768544861,2.00109377160363,10.6867157281602));
#44705=CARTESIAN_POINT('Ctrl Pts',(-1.25828863512325,2.01052735442731,10.6854998211298));
#44706=CARTESIAN_POINT('Ctrl Pts',(-1.23340926665106,2.02584124900257,10.6835069184944));
#44707=CARTESIAN_POINT('Ctrl Pts',(-1.22353921032068,2.03181766040372,10.6827241646119));
#44708=CARTESIAN_POINT('Ctrl Pts',(-1.20326641684351,2.04389172163566,10.6811330192878));
#44709=CARTESIAN_POINT('Ctrl Pts',(-1.19286008859937,2.04998250345789,10.6803250443467));
#44710=CARTESIAN_POINT('Ctrl Pts',(-1.16486247531842,2.06608400485279,10.6781734100825));
#44711=CARTESIAN_POINT('Ctrl Pts',(-1.14718831923316,2.07594959663167,10.6768383609062));
#44712=CARTESIAN_POINT('Ctrl Pts',(-1.04808750146148,2.12961475008131,10.6694687091436));
#44713=CARTESIAN_POINT('Ctrl Pts',(-0.96427132847863,2.16885476744213,10.6636662253407));
#44714=CARTESIAN_POINT('Ctrl Pts',(-0.74667557557877,2.25560939722666,10.6491513370789));
#44715=CARTESIAN_POINT('Ctrl Pts',(-0.610542022154624,2.29620045458269,
10.6405527020144));
#44716=CARTESIAN_POINT('Ctrl Pts',(-0.396224604427038,2.33968356900343,
10.6268550999262));
#44717=CARTESIAN_POINT('Ctrl Pts',(-0.320158015855828,2.35129969454769,
10.6219673329604));
#44718=CARTESIAN_POINT('Ctrl Pts',(-0.215617203381814,2.36209704448768,
10.615134888227));
#44719=CARTESIAN_POINT('Ctrl Pts',(-0.187519346495358,2.3644935212483,10.6132874998247));
#44720=CARTESIAN_POINT('Ctrl Pts',(-0.139378520658169,2.3677360116027,10.610100124849));
#44721=CARTESIAN_POINT('Ctrl Pts',(-0.119354913118796,2.36882978627102,
10.6087678321376));
#44722=CARTESIAN_POINT('Ctrl Pts',(-0.0809829145337113,2.37043807808947,
10.6062011137326));
#44723=CARTESIAN_POINT('Ctrl Pts',(-0.0626376342545772,2.37099375983227,
10.6049680485464));
#44724=CARTESIAN_POINT('Ctrl Pts',(-0.0142604907776587,2.37189727382489,
10.6016998656697));
#44725=CARTESIAN_POINT('Ctrl Pts',(0.0157739053772274,2.37188766220675,
10.5996540141048));
#44726=CARTESIAN_POINT('Ctrl Pts',(0.134472654783052,2.36959514221939,10.5914982985479));
#44727=CARTESIAN_POINT('Ctrl Pts',(0.222970232197642,2.36291029130619,10.5852588485014));
#44728=CARTESIAN_POINT('Ctrl Pts',(0.504326148275779,2.32571062461546,10.5649401243395));
#44729=CARTESIAN_POINT('Ctrl Pts',(0.693864280823634,2.2763614459825,10.5504535969875));
#44730=CARTESIAN_POINT('Ctrl Pts',(0.908068546570374,2.19131452540714,10.5341491846981));
#44731=CARTESIAN_POINT('Ctrl Pts',(0.940631960859903,2.17753522624725,10.5316750467083));
#44732=CARTESIAN_POINT('Ctrl Pts',(0.986457265934111,2.15692416528568,10.5282112610055));
#44733=CARTESIAN_POINT('Ctrl Pts',(0.999980082003424,2.15068818205457,10.527191388972));
#44734=CARTESIAN_POINT('Ctrl Pts',(1.02344169457039,2.1395998336077,10.5254270371241));
#44735=CARTESIAN_POINT('Ctrl Pts',(1.03340662243669,2.13480470318847,10.5246793290169));
#44736=CARTESIAN_POINT('Ctrl Pts',(1.05522078656389,2.12411916504763,10.5230463799002));
#44737=CARTESIAN_POINT('Ctrl Pts',(1.06705472855796,2.11819908468151,10.5221629115309));
#44738=CARTESIAN_POINT('Ctrl Pts',(1.10130511691628,2.10070500383746,10.519611108604));
#44739=CARTESIAN_POINT('Ctrl Pts',(1.1235879509367,2.08887163599751,10.5179574375262));
#44740=CARTESIAN_POINT('Ctrl Pts',(1.23582887752474,2.02694983129745,10.5096393431796));
#44741=CARTESIAN_POINT('Ctrl Pts',(1.32265484723054,1.9713922231618,10.5032403605874));
#44742=CARTESIAN_POINT('Ctrl Pts',(1.47744407124267,1.85750166541294,10.4913920741543));
#44743=CARTESIAN_POINT('Ctrl Pts',(1.54624610457917,1.80063218823078,10.4859398222646));
#44744=CARTESIAN_POINT('Ctrl Pts',(1.66291419243344,1.69256938183855,10.4760884550932));
#44745=CARTESIAN_POINT('Ctrl Pts',(1.71202307151968,1.64287879355183,10.4717232198946));
#44746=CARTESIAN_POINT('Ctrl Pts',(1.792611234361,1.5537931981403,10.4640772630206));
#44747=CARTESIAN_POINT('Ctrl Pts',(1.82515909854651,1.51542800838617,10.4608369381118));
#44748=CARTESIAN_POINT('Ctrl Pts',(1.8715967231593,1.45702273188902,10.4559587524949));
#44749=CARTESIAN_POINT('Ctrl Pts',(1.88643824095814,1.4377552737608,10.454357953188));
#44750=CARTESIAN_POINT('Ctrl Pts',(1.91265093136617,1.4026208936315,10.4514518467481));
#44751=CARTESIAN_POINT('Ctrl Pts',(1.92412762198314,1.386835178612,10.4501507309009));
#44752=CARTESIAN_POINT('Ctrl Pts',(1.94844993226337,1.35249770111347,10.4473292647408));
#44753=CARTESIAN_POINT('Ctrl Pts',(1.96122814167697,1.33390077832656,10.4458065543122));
#44754=CARTESIAN_POINT('Ctrl Pts',(1.99580075672399,1.28201421743131,10.441571270367));
#44755=CARTESIAN_POINT('Ctrl Pts',(2.01702491864424,1.24835542519301,10.4388384109042));
#44756=CARTESIAN_POINT('Ctrl Pts',(2.1315680743255,1.05615231855416,10.4233051830074));
#44757=CARTESIAN_POINT('Ctrl Pts',(2.20702545692803,0.887725761489421,10.4098941541254));
#44758=CARTESIAN_POINT('Ctrl Pts',(2.28344453173726,0.645023878770619,10.39138324805));
#44759=CARTESIAN_POINT('Ctrl Pts',(2.301620107805,0.576819475705937,10.386273753754));
#44760=CARTESIAN_POINT('Ctrl Pts',(2.32294711951267,0.479539264592612,10.3791909449151));
#44761=CARTESIAN_POINT('Ctrl Pts',(2.32864424771602,0.451062466477919,10.3771421003303));
#44762=CARTESIAN_POINT('Ctrl Pts',(2.33783063240883,0.400316894994948,10.3735422212544));
#44763=CARTESIAN_POINT('Ctrl Pts',(2.34152811505399,0.37808975031402,10.3719827202543));
#44764=CARTESIAN_POINT('Ctrl Pts',(2.34678744748623,0.34342919410319,10.3695810749327));
#44765=CARTESIAN_POINT('Ctrl Pts',(2.34856837556704,0.331031022692462,10.3687279874603));
#44766=CARTESIAN_POINT('Ctrl Pts',(2.3517599125972,0.307489069047457,10.3671201949803));
#44767=CARTESIAN_POINT('Ctrl Pts',(2.3531896923688,0.296348596491448,10.3663645563449));
#44768=CARTESIAN_POINT('Ctrl Pts',(2.35648660710815,0.269129912239733,10.3645302932968));
#44769=CARTESIAN_POINT('Ctrl Pts',(2.35826843566734,0.253041617117834,10.3634562009092));
#44770=CARTESIAN_POINT('Ctrl Pts',(2.36400432916913,0.195911999072798,10.3596738600485));
#44771=CARTESIAN_POINT('Ctrl Pts',(2.36705303451665,0.154784930732243,10.3570089964869));
#44772=CARTESIAN_POINT('Ctrl Pts',(2.37644775935924,-0.0411396795073466,
10.34450146443));
#44773=CARTESIAN_POINT('Ctrl Pts',(2.36869021113247,-0.196243010957284,
10.3351351007388));
#44774=CARTESIAN_POINT('Ctrl Pts',(2.33440778276043,-0.426353287744361,
10.3207677746636));
#44775=CARTESIAN_POINT('Ctrl Pts',(2.31918688695937,-0.502601015078118,
10.31593114651));
#44776=CARTESIAN_POINT('Ctrl Pts',(2.28706120515446,-0.630459586801942,
10.3075626595756));
#44777=CARTESIAN_POINT('Ctrl Pts',(2.27207766100117,-0.682488585136529,
10.3040831143584));
#44778=CARTESIAN_POINT('Ctrl Pts',(2.24759278377427,-0.757726592283991,
10.298915719759));
#44779=CARTESIAN_POINT('Ctrl Pts',(2.23948222970795,-0.781371983244245,
10.297271813723));
#44780=CARTESIAN_POINT('Ctrl Pts',(2.22434916611074,-0.823318223939019,
10.2943175244825));
#44781=CARTESIAN_POINT('Ctrl Pts',(2.21747057464733,-0.841668772533344,
10.2930119105771));
#44782=CARTESIAN_POINT('Ctrl Pts',(2.20232873042736,-0.880589325818423,
10.2902135091187));
#44783=CARTESIAN_POINT('Ctrl Pts',(2.19400295642084,-0.901132824899221,
10.288718767672));
#44784=CARTESIAN_POINT('Ctrl Pts',(2.17069707417738,-0.956400715814385,
10.2846479963427));
#44785=CARTESIAN_POINT('Ctrl Pts',(2.15517294739815,-0.990887180850716,
10.2820542495652));
#44786=CARTESIAN_POINT('Ctrl Pts',(2.07974775404617,-1.14827642455878,10.269960546378));
#44787=CARTESIAN_POINT('Ctrl Pts',(2.01012276805081,-1.26620921364307,10.2601431563836));
#44788=CARTESIAN_POINT('Ctrl Pts',(1.86898575226593,-1.46403442175285,10.242471663215));
#44789=CARTESIAN_POINT('Ctrl Pts',(1.80147730257742,-1.54634579389781,10.2346912839414));
#44790=CARTESIAN_POINT('Ctrl Pts',(1.69192278767077,-1.66297212317622,10.2232306794748));
#44791=CARTESIAN_POINT('Ctrl Pts',(1.65385333285412,-1.70083776383401,10.2194325867183));
#44792=CARTESIAN_POINT('Ctrl Pts',(1.60186958416066,-1.74914566083241,10.2145180945304));
#44793=CARTESIAN_POINT('Ctrl Pts',(1.58908179283713,-1.76077136684891,10.2133298044658));
#44794=CARTESIAN_POINT('Ctrl Pts',(1.56762475138897,-1.77985432161889,10.2113715603265));
#44795=CARTESIAN_POINT('Ctrl Pts',(1.55902675260742,-1.78739038062069,10.2105961761196));
#44796=CARTESIAN_POINT('Ctrl Pts',(1.54119063240015,-1.80279692760646,10.2090072859227));
#44797=CARTESIAN_POINT('Ctrl Pts',(1.5319460424184,-1.81065918018273,10.208194331883));
#44798=CARTESIAN_POINT('Ctrl Pts',(1.50681161680059,-1.83170496440405,10.2060111584463));
#44799=CARTESIAN_POINT('Ctrl Pts',(1.49080892291326,-1.84475286973174,10.2046500205725));
#44800=CARTESIAN_POINT('Ctrl Pts',(1.38334282867479,-1.9300641855689,10.1956834633304));
#44801=CARTESIAN_POINT('Ctrl Pts',(1.28681788630652,-1.99571832487647,10.1884518772964));
#44802=CARTESIAN_POINT('Ctrl Pts',(1.08083871268706,-2.11463642461871,10.1737993064892));
#44803=CARTESIAN_POINT('Ctrl Pts',(0.971342583306341,-2.16711601016415,
10.1664001503345));
#44804=CARTESIAN_POINT('Ctrl Pts',(0.789641824565459,-2.23765296125633,
10.1541725078488));
#44805=CARTESIAN_POINT('Ctrl Pts',(0.719768256692264,-2.26109643578134,
10.1494840027605));
#44806=CARTESIAN_POINT('Ctrl Pts',(0.622177418744681,-2.28885701956249,
10.1428847059099));
#44807=CARTESIAN_POINT('Ctrl Pts',(0.595302356795183,-2.2959935095681,10.1410623794665));
#44808=CARTESIAN_POINT('Ctrl Pts',(0.548910660374062,-2.30744325243948,
10.137904921298));
#44809=CARTESIAN_POINT('Ctrl Pts',(0.529453185160148,-2.31198541525999,
10.1365771201438));
#44810=CARTESIAN_POINT('Ctrl Pts',(0.489503681551775,-2.32078050281092,
10.1338426264221));
#44811=CARTESIAN_POINT('Ctrl Pts',(0.469008155770108,-2.3250090964655,10.132435301074));
#44812=CARTESIAN_POINT('Ctrl Pts',(0.416277359050632,-2.33516280838918,
10.1288019527366));
#44813=CARTESIAN_POINT('Ctrl Pts',(0.38397127387502,-2.3406917907855,10.1265638956521));
#44814=CARTESIAN_POINT('Ctrl Pts',(0.21775659539949,-2.36560485353525,10.1149818512508));
#44815=CARTESIAN_POINT('Ctrl Pts',(0.0825010830535566,-2.37417088071727,
10.1053134787959));
#44816=CARTESIAN_POINT('Ctrl Pts',(-0.168241020979051,-2.36859516527716,
10.0871049815437));
#44817=CARTESIAN_POINT('Ctrl Pts',(-0.28341381764386,-2.35758894018879,
10.0786350637776));
#44818=CARTESIAN_POINT('Ctrl Pts',(-0.452579406046273,-2.32884325429845,
10.0663288918297));
#44819=CARTESIAN_POINT('Ctrl Pts',(-0.50748633557062,-2.31749815459589,
10.0623580114539));
#44820=CARTESIAN_POINT('Ctrl Pts',(-0.578961329777634,-2.30006709812867,
10.0572608026467));
#44821=CARTESIAN_POINT('Ctrl Pts',(-0.595932840175838,-2.29572841863876,
10.0560559108339));
#44822=CARTESIAN_POINT('Ctrl Pts',(-0.62393818688567,-2.2882374918552,10.0540783804432));
#44823=CARTESIAN_POINT('Ctrl Pts',(-0.634999784714441,-2.28519254633209,
10.0533000817387));
#44824=CARTESIAN_POINT('Ctrl Pts',(-0.65763716674221,-2.27878404195903,
10.0517136101878));
#44825=CARTESIAN_POINT('Ctrl Pts',(-0.669210150471104,-2.27541230181822,
10.0509058946002));
#44826=CARTESIAN_POINT('Ctrl Pts',(-0.700178890948696,-2.26613297256069,
10.048752217557));
#44827=CARTESIAN_POINT('Ctrl Pts',(-0.7195259122602,-2.26006452489786,10.0474149282273));
#44828=CARTESIAN_POINT('Ctrl Pts',(-0.828193461994642,-2.22444259066834,
10.0399374670984));
#44829=CARTESIAN_POINT('Ctrl Pts',(-0.915781017700501,-2.18983980194483,
10.0340383114291));
#44830=CARTESIAN_POINT('Ctrl Pts',(-1.1285963660017,-2.09075362488835,10.0195017973996));
#44831=CARTESIAN_POINT('Ctrl Pts',(-1.25056690711633,-2.02016402201288,
10.0109697039868));
#44832=CARTESIAN_POINT('Ctrl Pts',(-1.42822612332949,-1.89505721795778,
9.99735904815005));
#44833=CARTESIAN_POINT('Ctrl Pts',(-1.48870715734687,-1.84792342922087,
9.99248817102497));
#44834=CARTESIAN_POINT('Ctrl Pts',(-1.56814445432427,-1.77958254919911,
9.98567580007995));
#44835=CARTESIAN_POINT('Ctrl Pts',(-1.58916251857746,-1.76083885131525,
9.98383092800014));
#44836=CARTESIAN_POINT('Ctrl Pts',(-1.62455728823117,-1.72812420052886,
9.98064704182713));
#44837=CARTESIAN_POINT('Ctrl Pts',(-1.63910003194645,-1.71433680456435,
9.97931569550324));
#44838=CARTESIAN_POINT('Ctrl Pts',(-1.66662109221823,-1.68757485677465,
9.97675023058455));
#44839=CARTESIAN_POINT('Ctrl Pts',(-1.67962700254257,-1.67463066449613,
9.97551746507842));
#44840=CARTESIAN_POINT('Ctrl Pts',(-1.71352971008069,-1.64009656373993,
9.97224875510829));
#44841=CARTESIAN_POINT('Ctrl Pts',(-1.73416812655504,-1.61825880915578,
9.97020205607362));
#44842=CARTESIAN_POINT('Ctrl Pts',(-1.81426320576979,-1.53021714923285,
9.96202562341005));
#44843=CARTESIAN_POINT('Ctrl Pts',(-1.87038274324857,-1.46108884227429,
9.95576535214964));
#44844=CARTESIAN_POINT('Ctrl Pts',(-2.03649625447272,-1.23117160498902,
9.93545655850457));
#44845=CARTESIAN_POINT('Ctrl Pts',(-2.13063912030509,-1.0599395923189,9.92100575524482));
#44846=CARTESIAN_POINT('Ctrl Pts',(-2.21582609706409,-0.846491663826748,
9.9047511244005));
#44847=CARTESIAN_POINT('Ctrl Pts',(-2.22812789102517,-0.813559978279359,
9.90229175700462));
#44848=CARTESIAN_POINT('Ctrl Pts',(-2.24458304096902,-0.766332724797668,
9.89884456317377));
#44849=CARTESIAN_POINT('Ctrl Pts',(-2.24934042632534,-0.752254310552646,
9.89782690529501));
#44850=CARTESIAN_POINT('Ctrl Pts',(-2.25740774013701,-0.727619890423506,
9.89606461250593));
#44851=CARTESIAN_POINT('Ctrl Pts',(-2.26077660489127,-0.717084074930183,
9.8953167855619));
#44852=CARTESIAN_POINT('Ctrl Pts',(-2.26802511500451,-0.693856076639133,
9.89368113967146));
#44853=CARTESIAN_POINT('Ctrl Pts',(-2.27187210272346,-0.681154422108647,
9.89279512512651));
#44854=CARTESIAN_POINT('Ctrl Pts',(-2.28276537955258,-0.644068687399322,
9.89023076260137));
#44855=CARTESIAN_POINT('Ctrl Pts',(-2.28952735818247,-0.619602172120532,
9.88856726612624));
#44856=CARTESIAN_POINT('Ctrl Pts',(-2.32234578774264,-0.492973930230632,
9.88008048405161));
#44857=CARTESIAN_POINT('Ctrl Pts',(-2.34196457564742,-0.389255626507347,
9.87353526268328));
#44858=CARTESIAN_POINT('Ctrl Pts',(-2.36595613954081,-0.190739644980454,
9.86121175177847));
#44859=CARTESIAN_POINT('Ctrl Pts',(-2.37167706481602,-0.0963206531594225,
9.85543516074478));
#44860=CARTESIAN_POINT('Ctrl Pts',(-2.37179383901357,0.0564438951617469,
9.84594930673836));
#44861=CARTESIAN_POINT('Ctrl Pts',(-2.36969193076758,0.114666352731385,
9.84230205067175));
#44862=CARTESIAN_POINT('Ctrl Pts',(-2.36545134562115,0.172736776625918,
9.83860221205714));
#44863=CARTESIAN_POINT('Ctrl Pts',(-2.36545135066152,0.172736707603127,
9.6385666740965));
#44864=CARTESIAN_POINT('Ctrl Pts',(-2.36639360499426,0.159833504717226,
9.63937806548334));
#44865=CARTESIAN_POINT('Ctrl Pts',(-2.3672303695368,0.146921388370306,9.64019160353449));
#44866=CARTESIAN_POINT('Ctrl Pts',(-2.37047125625906,0.089651233376424,
9.64380842025643));
#44867=CARTESIAN_POINT('Ctrl Pts',(-2.37173443215917,0.0452411583139775,
9.64663578726132));
#44868=CARTESIAN_POINT('Ctrl Pts',(-2.37176249280153,-0.0355626031238575,
9.65184189280179));
#44869=CARTESIAN_POINT('Ctrl Pts',(-2.37093779965913,-0.0719426650288141,
9.65420854366404));
#44870=CARTESIAN_POINT('Ctrl Pts',(-2.36826774342647,-0.130361960128773,
9.65805303530838));
#44871=CARTESIAN_POINT('Ctrl Pts',(-2.36695043613609,-0.152420221659169,
9.65951476531774));
#44872=CARTESIAN_POINT('Ctrl Pts',(-2.36382526246912,-0.194792171052408,
9.66234362817504));
#44873=CARTESIAN_POINT('Ctrl Pts',(-2.36206321913186,-0.21510733712454,
9.66370923523363));
#44874=CARTESIAN_POINT('Ctrl Pts',(-2.35732846829581,-0.262576979943863,
9.6669231681066));
#44875=CARTESIAN_POINT('Ctrl Pts',(-2.35414819498047,-0.289707348872911,
9.66877769041165));
#44876=CARTESIAN_POINT('Ctrl Pts',(-2.34165493301826,-0.382408287116409,
9.67517770567363));
#44877=CARTESIAN_POINT('Ctrl Pts',(-2.33006541988164,-0.447635610921445,
9.67979103325344));
#44878=CARTESIAN_POINT('Ctrl Pts',(-2.29282793492771,-0.61596525676266,
9.69198644334059));
#44879=CARTESIAN_POINT('Ctrl Pts',(-2.26295795769526,-0.71797683906012,
9.69967098386616));
#44880=CARTESIAN_POINT('Ctrl Pts',(-2.18059222158132,-0.942252356629987,
9.71706106564632));
#44881=CARTESIAN_POINT('Ctrl Pts',(-2.12444095959257,-1.06281603295799,
9.72676515016147));
#44882=CARTESIAN_POINT('Ctrl Pts',(-2.04609033152589,-1.19972319162559,
9.7378106293349));
#44883=CARTESIAN_POINT('Ctrl Pts',(-2.03334749892793,-1.221195909545,9.73954332027444));
#44884=CARTESIAN_POINT('Ctrl Pts',(-2.01323739071232,-1.25389527339919,
9.74217789292613));
#44885=CARTESIAN_POINT('Ctrl Pts',(-2.00611030562084,-1.26526661660371,
9.74309331055332));
#44886=CARTESIAN_POINT('Ctrl Pts',(-1.993336312459,-1.28526835842575,9.74470130233207));
#44887=CARTESIAN_POINT('Ctrl Pts',(-1.98772930226305,-1.29392296304453,
9.74539625733571));
#44888=CARTESIAN_POINT('Ctrl Pts',(-1.97377705560849,-1.31515397589286,
9.74709944800765));
#44889=CARTESIAN_POINT('Ctrl Pts',(-1.96536794705419,-1.32768772967732,
9.74810358619174));
#44890=CARTESIAN_POINT('Ctrl Pts',(-1.93709729653372,-1.36896781556788,
9.75140928311966));
#44891=CARTESIAN_POINT('Ctrl Pts',(-1.91671929569221,-1.39735688167427,
9.75368033294478));
#44892=CARTESIAN_POINT('Ctrl Pts',(-1.76482359039027,-1.59938760735871,
9.76990653054075));
#44893=CARTESIAN_POINT('Ctrl Pts',(-1.61055830996404,-1.75464117308747,
9.78281547696509));
#44894=CARTESIAN_POINT('Ctrl Pts',(-1.38173225494166,-1.92895962212783,
9.80088738321199));
#44895=CARTESIAN_POINT('Ctrl Pts',(-1.32437757469801,-1.96877930735889,
9.8053334114941));
#44896=CARTESIAN_POINT('Ctrl Pts',(-1.24124523755315,-2.02121766462845,
9.81172370164513));
#44897=CARTESIAN_POINT('Ctrl Pts',(-1.21686472698057,-2.03598887812035,
9.81359138805103));
#44898=CARTESIAN_POINT('Ctrl Pts',(-1.17443686846665,-2.06065996654257,
9.81683420300584));
#44899=CARTESIAN_POINT('Ctrl Pts',(-1.15651563028311,-2.0707711144347,9.81820171888499));
#44900=CARTESIAN_POINT('Ctrl Pts',(-1.1194605353785,-2.09104650870954,9.82102598159974));
#44901=CARTESIAN_POINT('Ctrl Pts',(-1.10031447758006,-2.10118428262918,
9.82248348654896));
#44902=CARTESIAN_POINT('Ctrl Pts',(-1.05055258037578,-2.12666640527462,
9.82626848847833));
#44903=CARTESIAN_POINT('Ctrl Pts',(-1.01973937174752,-2.14161203995885,
9.82860923540437));
#44904=CARTESIAN_POINT('Ctrl Pts',(-0.850880303116009,-2.21904501163313,
9.84142734029265));
#44905=CARTESIAN_POINT('Ctrl Pts',(-0.707432316130912,-2.26885071822584,
9.85231569664025));
#44906=CARTESIAN_POINT('Ctrl Pts',(-0.424767738568074,-2.33756445858952,
9.87347981575511));
#44907=CARTESIAN_POINT('Ctrl Pts',(-0.286646392333594,-2.35848994046285,
9.88368695588045));
#44908=CARTESIAN_POINT('Ctrl Pts',(-0.123245512745035,-2.36867011652855,
9.89514135227839));
#44909=CARTESIAN_POINT('Ctrl Pts',(-0.0989896574277021,-2.36980774237117,
9.89682524168229));
#44910=CARTESIAN_POINT('Ctrl Pts',(-0.0614524736573346,-2.37099089937664,
9.89940156381164));
#44911=CARTESIAN_POINT('Ctrl Pts',(-0.048181773143534,-2.37129770145853,
9.90030666883464));
#44912=CARTESIAN_POINT('Ctrl Pts',(-0.0234128799076648,-2.37166230408445,
9.90198447805365));
#44913=CARTESIAN_POINT('Ctrl Pts',(-0.0119163092021866,-2.37174793246545,
9.90275851053423));
#44914=CARTESIAN_POINT('Ctrl Pts',(0.0156932799462805,-2.37175280855637,
9.90460667181672));
#44915=CARTESIAN_POINT('Ctrl Pts',(0.0318055874955957,-2.37159147064463,
9.90567653172282));
#44916=CARTESIAN_POINT('Ctrl Pts',(0.0895918935778713,-2.37042379813828,
9.9094863911435));
#44917=CARTESIAN_POINT('Ctrl Pts',(0.13124172156159,-2.36848301235794,9.91218172025578));
#44918=CARTESIAN_POINT('Ctrl Pts',(0.241336667800836,-2.36043937877468,
9.91922261929333));
#44919=CARTESIAN_POINT('Ctrl Pts',(0.309606469528001,-2.35245881317323,
9.92350311508977));
#44920=CARTESIAN_POINT('Ctrl Pts',(0.55373968521195,-2.31310626125181,9.9387906450863));
#44921=CARTESIAN_POINT('Ctrl Pts',(0.726255724265185,-2.26487024704045,
9.94960382151006));
#44922=CARTESIAN_POINT('Ctrl Pts',(0.928881109966353,-2.18265573504321,
9.96358857293454));
#44923=CARTESIAN_POINT('Ctrl Pts',(0.96564996926563,-2.1666393387325,9.96617880212663));
#44924=CARTESIAN_POINT('Ctrl Pts',(1.02472157724201,-2.13910554670781,9.97043770533736));
#44925=CARTESIAN_POINT('Ctrl Pts',(1.04727939818361,-2.12815239946008,9.97208776570118));
#44926=CARTESIAN_POINT('Ctrl Pts',(1.08763922339423,-2.10775824852671,9.97508541547286));
#44927=CARTESIAN_POINT('Ctrl Pts',(1.10550283439582,-2.09844403208524,9.97642857870606));
#44928=CARTESIAN_POINT('Ctrl Pts',(1.1438100635774,-2.07784547024858,9.97934562592108));
#44929=CARTESIAN_POINT('Ctrl Pts',(1.16420988063791,-2.06648458678929,9.98092206282418));
#44930=CARTESIAN_POINT('Ctrl Pts',(1.22138876535772,-2.03352564593499,9.98540796363083));
#44931=CARTESIAN_POINT('Ctrl Pts',(1.25775609430766,-2.01123501352887,9.98834137837533));
#44932=CARTESIAN_POINT('Ctrl Pts',(1.42934802394508,-1.89958670169278,10.0025813366958));
#44933=CARTESIAN_POINT('Ctrl Pts',(1.55575843956376,-1.79751661791073,10.0143353943163));
#44934=CARTESIAN_POINT('Ctrl Pts',(1.74975203220688,-1.60497749846737,10.034236821544));
#44935=CARTESIAN_POINT('Ctrl Pts',(1.8231363199652,-1.52110587796986,10.0423250622157));
#44936=CARTESIAN_POINT('Ctrl Pts',(1.90580893265975,-1.41200015440256,10.0519174248317));
#44937=CARTESIAN_POINT('Ctrl Pts',(1.92092441448219,-1.39136682636255,10.053693400758));
#44938=CARTESIAN_POINT('Ctrl Pts',(1.94353156266508,-1.35943614521977,10.0563794347307));
#44939=CARTESIAN_POINT('Ctrl Pts',(1.95126459898187,-1.34831304033031,10.0573038162807));
#44940=CARTESIAN_POINT('Ctrl Pts',(1.96529013481159,-1.32776546740986,10.0589898947209));
#44941=CARTESIAN_POINT('Ctrl Pts',(1.97161076734034,-1.31836164985411,10.0597532975408));
#44942=CARTESIAN_POINT('Ctrl Pts',(1.98645513001782,-1.29593071006068,10.0615552410154));
#44943=CARTESIAN_POINT('Ctrl Pts',(1.99491836446462,-1.28286442771054,10.0625899553305));
#44944=CARTESIAN_POINT('Ctrl Pts',(2.02357220881625,-1.23765674464989,10.0661223500924));
#44945=CARTESIAN_POINT('Ctrl Pts',(2.04312064333208,-1.20511290368074,10.0685834956661));
#44946=CARTESIAN_POINT('Ctrl Pts',(2.09130284835018,-1.12035481403923,10.0748235211222));
#44947=CARTESIAN_POINT('Ctrl Pts',(2.11876764923243,-1.06750504966171,10.0785542480441));
#44948=CARTESIAN_POINT('Ctrl Pts',(2.22831860070386,-0.835773023645834,
10.0944656166325));
#44949=CARTESIAN_POINT('Ctrl Pts',(2.28995066449202,-0.648108395524297,
10.1063090792218));
#44950=CARTESIAN_POINT('Ctrl Pts',(2.33569536007661,-0.414080435520385,
10.1215894055156));
#44951=CARTESIAN_POINT('Ctrl Pts',(2.34261124873455,-0.372971355377189,
10.1242884867938));
#44952=CARTESIAN_POINT('Ctrl Pts',(2.35171252700854,-0.308534823812108,
10.1285541584056));
#44953=CARTESIAN_POINT('Ctrl Pts',(2.35464180164886,-0.285319942218089,
10.130097968569));
#44954=CARTESIAN_POINT('Ctrl Pts',(2.35945291851521,-0.242045015064398,
10.132990659529));
#44955=CARTESIAN_POINT('Ctrl Pts',(2.36142355876905,-0.221996842522349,
10.134336679354));
#44956=CARTESIAN_POINT('Ctrl Pts',(2.36526851300837,-0.176999483583623,
10.137372132063));
#44957=CARTESIAN_POINT('Ctrl Pts',(2.36700387791533,-0.152041166589389,
10.1390656618073));
#44958=CARTESIAN_POINT('Ctrl Pts',(2.37111039744496,-0.0754979156906682,
10.1442917880726));
#44959=CARTESIAN_POINT('Ctrl Pts',(2.37219188992352,-0.0238620303363823,
10.1478626068129));
#44960=CARTESIAN_POINT('Ctrl Pts',(2.37074469235968,0.0997532523843913,
10.1565236720387));
#44961=CARTESIAN_POINT('Ctrl Pts',(2.36662467502378,0.171660252464469,10.1616541110278));
#44962=CARTESIAN_POINT('Ctrl Pts',(2.35044142080663,0.328610265406669,10.1730251913194));
#44963=CARTESIAN_POINT('Ctrl Pts',(2.33701675852122,0.413414253722766,10.179282683062));
#44964=CARTESIAN_POINT('Ctrl Pts',(2.29780771385445,0.596254905614223,10.1928903195935));
#44965=CARTESIAN_POINT('Ctrl Pts',(2.2702739150326,0.693757956272299,10.2002224021083));
#44966=CARTESIAN_POINT('Ctrl Pts',(2.22812497186673,0.813206406142454,10.2090969099169));
#44967=CARTESIAN_POINT('Ctrl Pts',(2.21927174254811,0.837065474140007,10.2108636905687));
#44968=CARTESIAN_POINT('Ctrl Pts',(2.20512839486497,0.873378303476749,10.213538940998));
#44969=CARTESIAN_POINT('Ctrl Pts',(2.20011316108581,0.885936227436829,10.2144615609834));
#44970=CARTESIAN_POINT('Ctrl Pts',(2.19108861313925,0.907983951431249,10.2160760331935));
#44971=CARTESIAN_POINT('Ctrl Pts',(2.18712463254486,0.917491152261432,10.2167703653121));
#44972=CARTESIAN_POINT('Ctrl Pts',(2.17725282851906,0.94074007816281,10.2184640872232));
#44973=CARTESIAN_POINT('Ctrl Pts',(2.17127676513124,0.954452205043743,10.2194595080588));
#44974=CARTESIAN_POINT('Ctrl Pts',(2.15125714420827,0.999226070389373,10.2227011282124));
#44975=CARTESIAN_POINT('Ctrl Pts',(2.13667299484858,1.03004312083716,10.2249184481402));
#44976=CARTESIAN_POINT('Ctrl Pts',(2.09869231990535,1.10601718521974,10.2303761210652));
#44977=CARTESIAN_POINT('Ctrl Pts',(2.07449790283775,1.15075737007607,10.2335823071362));
#44978=CARTESIAN_POINT('Ctrl Pts',(1.98783787901939,1.29937882642102,10.2443194272543));
#44979=CARTESIAN_POINT('Ctrl Pts',(1.91885772736134,1.39923960234297,10.2516900207509));
#44980=CARTESIAN_POINT('Ctrl Pts',(1.77447471032154,1.57737912387246,10.2658789603067));
#44981=CARTESIAN_POINT('Ctrl Pts',(1.70074824901947,1.65660403889973,10.272653631145));
#44982=CARTESIAN_POINT('Ctrl Pts',(1.59839434067211,1.75253239646334,10.2817327830896));
#44983=CARTESIAN_POINT('Ctrl Pts',(1.57446240837882,1.77406376303652,10.2838341393073));
#44984=CARTESIAN_POINT('Ctrl Pts',(1.53400958624207,1.80899547784127,10.2873562767059));
#44985=CARTESIAN_POINT('Ctrl Pts',(1.51773294158545,1.82267295999115,10.2887657285559));
#44986=CARTESIAN_POINT('Ctrl Pts',(1.4851357454157,1.84932541527664,10.2915747026501));
#44987=CARTESIAN_POINT('Ctrl Pts',(1.46882360354959,1.86230766757743,10.2929737627064));
#44988=CARTESIAN_POINT('Ctrl Pts',(1.4286082108599,1.89345661131758,10.2964082767619));
#44989=CARTESIAN_POINT('Ctrl Pts',(1.40452760876528,1.91138730114274,10.2984525098614));
#44990=CARTESIAN_POINT('Ctrl Pts',(1.30758576481174,1.98075009579461,10.3066376482886));
#44991=CARTESIAN_POINT('Ctrl Pts',(1.23219671829373,2.02850669567647,10.3129094529943));
#44992=CARTESIAN_POINT('Ctrl Pts',(0.989780091523776,2.1635627868354,10.3327703199869));
#44993=CARTESIAN_POINT('Ctrl Pts',(0.814935718426447,2.23529477751987,10.3467249850365));
#44994=CARTESIAN_POINT('Ctrl Pts',(0.595947395346577,2.29598773703518,10.3628536728971));
#44995=CARTESIAN_POINT('Ctrl Pts',(0.558186515639164,2.30545899981303,10.3655859323603));
#44996=CARTESIAN_POINT('Ctrl Pts',(0.506019520548593,2.31718660707905,10.3692791209043));
#44997=CARTESIAN_POINT('Ctrl Pts',(0.491802319326017,2.32024568351708,10.3702773975033));
#44998=CARTESIAN_POINT('Ctrl Pts',(0.46621508008337,2.32550546058195,10.3720582054168));
#44999=CARTESIAN_POINT('Ctrl Pts',(0.454855371541248,2.32775401656357,10.3728432238834));
#45000=CARTESIAN_POINT('Ctrl Pts',(0.431040604373656,2.33228694238738,10.37447671837));
#45001=CARTESIAN_POINT('Ctrl Pts',(0.418582987263027,2.33455492228331,10.37532431861));
#45002=CARTESIAN_POINT('Ctrl Pts',(0.384364718018118,2.34050183754267,10.3776351009658));
#45003=CARTESIAN_POINT('Ctrl Pts',(0.362569358446222,2.34397709723222,10.3790877328344));
#45004=CARTESIAN_POINT('Ctrl Pts',(0.312968571991182,2.35117748061079,10.3823564854415));
#45005=CARTESIAN_POINT('Ctrl Pts',(0.285138860795388,2.35471459873277,10.3841641893994));
#45006=CARTESIAN_POINT('Ctrl Pts',(0.191778442823405,2.36490102928783,10.3901600171776));
#45007=CARTESIAN_POINT('Ctrl Pts',(0.126031722727445,2.36931486718475,10.3942703640904));
#45008=CARTESIAN_POINT('Ctrl Pts',(-0.133674627215506,2.37590700097228,
10.4103473933092));
#45009=CARTESIAN_POINT('Ctrl Pts',(-0.327387855482908,2.35703543831419,
10.4220572208828));
#45010=CARTESIAN_POINT('Ctrl Pts',(-0.553949739640424,2.30646895790663,
10.4369855217963));
#45011=CARTESIAN_POINT('Ctrl Pts',(-0.591050259319969,2.29724154170777,
10.439468189087));
#45012=CARTESIAN_POINT('Ctrl Pts',(-0.649565601167914,2.2811766488887,10.4434535441794));
#45013=CARTESIAN_POINT('Ctrl Pts',(-0.67113500886909,2.27492420023726,10.4449378061231));
#45014=CARTESIAN_POINT('Ctrl Pts',(-0.711990826386118,2.26244948777299,
10.4477799348037));
#45015=CARTESIAN_POINT('Ctrl Pts',(-0.73129271505082,2.25628445538158,10.4491358638286));
#45016=CARTESIAN_POINT('Ctrl Pts',(-0.775616143406512,2.24149904405615,
10.452281213657));
#45017=CARTESIAN_POINT('Ctrl Pts',(-0.800576718113202,2.23270579978593,
10.4540760650354));
#45018=CARTESIAN_POINT('Ctrl Pts',(-0.882132910821974,2.20243133413291,
10.4600209516387));
#45019=CARTESIAN_POINT('Ctrl Pts',(-0.938049772733661,2.17920255559462,
10.464226381512));
#45020=CARTESIAN_POINT('Ctrl Pts',(-1.07620637779581,2.11550706600887,10.4749506164428));
#45021=CARTESIAN_POINT('Ctrl Pts',(-1.15710042642071,2.07236730063999,10.4815418509632));
#45022=CARTESIAN_POINT('Ctrl Pts',(-1.36350671292189,1.9464342658207,10.4990968383773));
#45023=CARTESIAN_POINT('Ctrl Pts',(-1.48400733116188,1.85620142546291,10.5101374063558));
#45024=CARTESIAN_POINT('Ctrl Pts',(-1.6162020083751,1.73605787626332,10.5226905445083));
#45025=CARTESIAN_POINT('Ctrl Pts',(-1.63689117564138,1.71656439799656,10.5246686937491));
#45026=CARTESIAN_POINT('Ctrl Pts',(-1.66719699994388,1.68696369126029,10.5275804108877));
#45027=CARTESIAN_POINT('Ctrl Pts',(-1.67708228052583,1.67713666120871,10.5285324762579));
#45028=CARTESIAN_POINT('Ctrl Pts',(-1.69480662440035,1.65920333311865,10.5302427976604));
#45029=CARTESIAN_POINT('Ctrl Pts',(-1.70267509328861,1.65112771498011,10.5310031669544));
#45030=CARTESIAN_POINT('Ctrl Pts',(-1.72087248490399,1.63218281696118,10.5327645593599));
#45031=CARTESIAN_POINT('Ctrl Pts',(-1.73115634698567,1.62127128770843,10.5337622977637));
#45032=CARTESIAN_POINT('Ctrl Pts',(-1.76466334700609,1.58503685182561,10.5370238241358));
#45033=CARTESIAN_POINT('Ctrl Pts',(-1.78744084120629,1.5593056380903,10.5392581842554));
#45034=CARTESIAN_POINT('Ctrl Pts',(-1.84289675431923,1.49384560388232,10.5447689368369));
#45035=CARTESIAN_POINT('Ctrl Pts',(-1.87485784171472,1.45353081576012,10.5480102347343));
#45036=CARTESIAN_POINT('Ctrl Pts',(-2.01735215698087,1.26126380576498,10.5629381770528));
#45037=CARTESIAN_POINT('Ctrl Pts',(-2.11088653623396,1.09756826182258,10.574220843688));
#45038=CARTESIAN_POINT('Ctrl Pts',(-2.20612426412014,0.872581375981715,
10.5897062650098));
#45039=CARTESIAN_POINT('Ctrl Pts',(-2.22625891694627,0.819849377514655,
10.5933291373229));
#45040=CARTESIAN_POINT('Ctrl Pts',(-2.25284165486595,0.742004023144325,
10.5986980916821));
#45041=CARTESIAN_POINT('Ctrl Pts',(-2.26079006270558,0.717421563725073,
10.6003963670633));
#45042=CARTESIAN_POINT('Ctrl Pts',(-2.27423951853357,0.673380542939109,
10.6034465341006));
#45043=CARTESIAN_POINT('Ctrl Pts',(-2.27989634816886,0.653971973923773,
10.6047933124285));
#45044=CARTESIAN_POINT('Ctrl Pts',(-2.29141892940331,0.612470232885562,
10.607679811952));
#45045=CARTESIAN_POINT('Ctrl Pts',(-2.29721474009163,0.590359951306312,
10.6092215939715));
#45046=CARTESIAN_POINT('Ctrl Pts',(-2.30842545787716,0.54492494591839,10.6123991557904));
#45047=CARTESIAN_POINT('Ctrl Pts',(-2.31380849312682,0.521595127925753,
10.6140357351284));
#45048=CARTESIAN_POINT('Ctrl Pts',(-2.32902548512657,0.45076706446286,10.6190205451965));
#45049=CARTESIAN_POINT('Ctrl Pts',(-2.33775597571351,0.403047266101511,
10.6224012594135));
#45050=CARTESIAN_POINT('Ctrl Pts',(-2.35418213593451,0.294570640936105,
10.6301365372826));
#45051=CARTESIAN_POINT('Ctrl Pts',(-2.3609967220633,0.2337383165994,10.6345099255067));
#45052=CARTESIAN_POINT('Ctrl Pts',(-2.36545136240482,0.172736546790724,
10.6389210243916));
#45053=CARTESIAN_POINT('Origin',(0.,0.,0.));
#45054=CARTESIAN_POINT('',(-2.94199911155216,0.00228640028720795,0.322176117089596));
#45055=CARTESIAN_POINT('',(1.29074626225713,2.64842276394507,7.39067040906624E-5));
#45056=CARTESIAN_POINT('Ctrl Pts',(-2.94437861999191,0.00228824954296311,
0.322176117089596));
#45057=CARTESIAN_POINT('Ctrl Pts',(-2.94551635113874,0.142778583613822,
0.314557432409286));
#45058=CARTESIAN_POINT('Ctrl Pts',(-2.87303612132235,1.24792270671419,0.254559243224474));
#45059=CARTESIAN_POINT('Ctrl Pts',(-1.53809074754619,3.05021726920943,0.147191839762635));
#45060=CARTESIAN_POINT('Ctrl Pts',(0.503747753874156,3.02562475113786,0.0474431209811117));
#45061=CARTESIAN_POINT('Ctrl Pts',(1.29074626225713,2.64842276394507,7.39067040906624E-5));
#45062=CARTESIAN_POINT('',(-1.28892185405326,2.64462557919716,0.));
#45063=CARTESIAN_POINT('Origin',(0.,0.,0.));
#45064=CARTESIAN_POINT('',(-2.94208929002299,0.0031237281129026,0.177823882910396));
#45065=CARTESIAN_POINT('Ctrl Pts',(-1.28892185405326,2.64462557919716,1.87350135405495E-15));
#45066=CARTESIAN_POINT('Ctrl Pts',(-2.16038499609478,2.21989706654312,0.0524451052237091));
#45067=CARTESIAN_POINT('Ctrl Pts',(-2.88156023630951,1.21946533172,0.111719732860507));
#45068=CARTESIAN_POINT('Ctrl Pts',(-2.94535953294187,0.128940758021734,
0.170994360497305));
#45069=CARTESIAN_POINT('Ctrl Pts',(-2.94436911647834,0.00312614869137163,
0.177823882910396));
#45070=CARTESIAN_POINT('',(-2.94199999091258,0.000231236646814539,1.17782388286648));
#45071=CARTESIAN_POINT('Ctrl Pts',(-2.94199834176125,0.00312363154967357,
0.177823882910396));
#45072=CARTESIAN_POINT('Ctrl Pts',(-2.94209484212644,-0.087765421741547,
0.182761583941182));
#45073=CARTESIAN_POINT('Ctrl Pts',(-2.93797538754606,-0.178839988680605,
0.187699284971969));
#45074=CARTESIAN_POINT('Ctrl Pts',(-2.92961510475039,-0.269665233240012,
0.192636986002755));
#45075=CARTESIAN_POINT('Ctrl Pts',(-2.92100587058736,-0.363195059615083,
0.197721721225234));
#45076=CARTESIAN_POINT('Ctrl Pts',(-2.90789915985505,-0.456459991579172,
0.202806456447713));
#45077=CARTESIAN_POINT('Ctrl Pts',(-2.89032562029103,-0.54898252129668,
0.207891191670192));
#45078=CARTESIAN_POINT('Ctrl Pts',(-2.87329698184751,-0.638636213468393,
0.212818264976582));
#45079=CARTESIAN_POINT('Ctrl Pts',(-2.85207453592643,-0.727592368507746,
0.217745338282971));
#45080=CARTESIAN_POINT('Ctrl Pts',(-2.82673878856991,-0.815421253827921,
0.222672411589361));
#45081=CARTESIAN_POINT('Ctrl Pts',(-2.80141446685841,-0.903210531014497,
0.227597262936801));
#45082=CARTESIAN_POINT('Ctrl Pts',(-2.77198065287895,-0.989873101288184,
0.232522114284241));
#45083=CARTESIAN_POINT('Ctrl Pts',(-2.73856850990087,-1.07499140302578,
0.237446965631682));
#45084=CARTESIAN_POINT('Ctrl Pts',(-2.70516121687009,-1.1600973493967,0.242371102111192));
#45085=CARTESIAN_POINT('Ctrl Pts',(-2.6677769119081,-1.24365903992741,0.247295238590702));
#45086=CARTESIAN_POINT('Ctrl Pts',(-2.62659549866888,-1.32527736205383,
0.252219375070212));
#45087=CARTESIAN_POINT('Ctrl Pts',(-2.58540746886886,-1.40690879768337,
0.257144302703932));
#45088=CARTESIAN_POINT('Ctrl Pts',(-2.54042133172357,-1.4865958314944,0.262069230337652));
#45089=CARTESIAN_POINT('Ctrl Pts',(-2.49186301833919,-1.5639637776603,0.266994157971371));
#45090=CARTESIAN_POINT('Ctrl Pts',(-2.4432540951925,-1.64141236034535,0.271924218596738));
#45091=CARTESIAN_POINT('Ctrl Pts',(-2.39106581805803,-1.71653664093556,
0.276854279222104));
#45092=CARTESIAN_POINT('Ctrl Pts',(-2.33556715859271,-1.7889913492533,0.281784339847471));
#45093=CARTESIAN_POINT('Ctrl Pts',(-2.2800335455957,-1.86149169016772,0.2867175054673));
#45094=CARTESIAN_POINT('Ctrl Pts',(-2.22118570578933,-1.93131876318205,
0.291650671087129));
#45095=CARTESIAN_POINT('Ctrl Pts',(-2.15933097659477,-1.9981625893601,0.296583836706958));
#45096=CARTESIAN_POINT('Ctrl Pts',(-2.09738264979832,-2.06510756256303,
0.301524467115298));
#45097=CARTESIAN_POINT('Ctrl Pts',(-2.03241869343511,-2.1290599663488,0.306465097523638));
#45098=CARTESIAN_POINT('Ctrl Pts',(-1.96478059555267,-2.18974912063909,
0.311405727931977));
#45099=CARTESIAN_POINT('Ctrl Pts',(-1.94988156188092,-2.20311747045361,
0.312494029068734));
#45100=CARTESIAN_POINT('Ctrl Pts',(-1.93485288848935,-2.21632764836611,
0.31358233020549));
#45101=CARTESIAN_POINT('Ctrl Pts',(-1.91969840995316,-2.22937704635697,
0.314670631342247));
#45102=CARTESIAN_POINT('Ctrl Pts',(-1.84914814332196,-2.29012730611899,
0.319737116156612));
#45103=CARTESIAN_POINT('Ctrl Pts',(-1.77559096880863,-2.3476290234709,0.324803600970976));
#45104=CARTESIAN_POINT('Ctrl Pts',(-1.69935779057415,-2.40157179772227,
0.329870085785341));
#45105=CARTESIAN_POINT('Ctrl Pts',(-1.62322724574283,-2.45544194833881,
0.334929749546319));
#45106=CARTESIAN_POINT('Ctrl Pts',(-1.54442821490432,-2.50576242592437,
0.339989413307297));
#45107=CARTESIAN_POINT('Ctrl Pts',(-1.46332566611215,-2.552262132873,0.345049077068274));
#45108=CARTESIAN_POINT('Ctrl Pts',(-1.3785330937065,-2.60087749486843,0.35033894664932));
#45109=CARTESIAN_POINT('Ctrl Pts',(-1.29122277624355,-2.64531582486387,
0.355628816230366));
#45110=CARTESIAN_POINT('Ctrl Pts',(-1.20184727105266,-2.6853169528127,0.360918685811411));
#45111=CARTESIAN_POINT('Ctrl Pts',(-1.11651204589616,-2.72350980277463,
0.365969423267753));
#45112=CARTESIAN_POINT('Ctrl Pts',(-1.0292947386691,-2.75765769436651,0.371020160724095));
#45113=CARTESIAN_POINT('Ctrl Pts',(-0.94061438002265,-2.78758113569715,
0.376070898180437));
#45114=CARTESIAN_POINT('Ctrl Pts',(-0.851963908520084,-2.81749449219942,
0.381119933432149));
#45115=CARTESIAN_POINT('Ctrl Pts',(-0.761851783158,-2.84318608660473,0.38616896868386));
#45116=CARTESIAN_POINT('Ctrl Pts',(-0.670715073634204,-2.86452531669732,
0.391218003935572));
#45117=CARTESIAN_POINT('Ctrl Pts',(-0.579584009289163,-2.88586322499796,
0.396266726440568));
#45118=CARTESIAN_POINT('Ctrl Pts',(-0.48742891675585,-2.90284920499647,
0.401315448945565));
#45119=CARTESIAN_POINT('Ctrl Pts',(-0.394698937554703,-2.91540335951875,
0.406364171450561));
#45120=CARTESIAN_POINT('Ctrl Pts',(-0.301949194876519,-2.92796018969939,
0.411413969986332));
#45121=CARTESIAN_POINT('Ctrl Pts',(-0.208624759428889,-2.93608325943364,
0.416463768522102));
#45122=CARTESIAN_POINT('Ctrl Pts',(-0.115180699757438,-2.93974444576453,
0.421513567057873));
#45123=CARTESIAN_POINT('Ctrl Pts',(-0.0216371349240405,-2.94340953075885,
0.426568742939435));
#45124=CARTESIAN_POINT('Ctrl Pts',(0.0720258668843346,-2.94260323236971,
0.431623918820998));
#45125=CARTESIAN_POINT('Ctrl Pts',(0.165352752788341,-2.93734956502377,
0.436679094702561));
#45126=CARTESIAN_POINT('Ctrl Pts',(0.258737808413396,-2.93209262311915,
0.441737421425042));
#45127=CARTESIAN_POINT('Ctrl Pts',(0.351785892563366,-2.92238283867174,
0.446795748147523));
#45128=CARTESIAN_POINT('Ctrl Pts',(0.444048176176827,-2.90829593013401,
0.451854074870004));
#45129=CARTESIAN_POINT('Ctrl Pts',(0.536449344569062,-2.89418781621202,
0.456920016021267));
#45130=CARTESIAN_POINT('Ctrl Pts',(0.62806191986878,-2.87568951449999,0.46198595717253));
#45131=CARTESIAN_POINT('Ctrl Pts',(0.718449120449233,-2.85292741956849,
0.467051898323793));
#45132=CARTESIAN_POINT('Ctrl Pts',(0.747912720546424,-2.84550763824847,
0.468703247886986));
#45133=CARTESIAN_POINT('Ctrl Pts',(0.777246254132491,-2.83763518819118,
0.470354597450178));
#45134=CARTESIAN_POINT('Ctrl Pts',(0.806435029787981,-2.82931556082577,
0.47200594701337));
#45135=CARTESIAN_POINT('Ctrl Pts',(0.895996558094848,-2.80378798986549,
0.477072873848329));
#45136=CARTESIAN_POINT('Ctrl Pts',(0.984494601690804,-2.77396099009945,
0.482139800683287));
#45137=CARTESIAN_POINT('Ctrl Pts',(1.07148797004047,-2.73994115448828,0.487206727518246));
#45138=CARTESIAN_POINT('Ctrl Pts',(1.15836681946443,-2.7059661029233,0.492266984200884));
#45139=CARTESIAN_POINT('Ctrl Pts',(1.24374452278692,-2.6678093451109,0.497327240883522));
#45140=CARTESIAN_POINT('Ctrl Pts',(1.32719410318614,-2.62562750832404,0.50238749756616));
#45141=CARTESIAN_POINT('Ctrl Pts',(1.41442813673475,-2.58153271781937,0.507677237779424));
#45142=CARTESIAN_POINT('Ctrl Pts',(1.4995545525342,-2.53303925475134,0.512966977992688));
#45143=CARTESIAN_POINT('Ctrl Pts',(1.58210772607098,-2.48038286220223,0.518256718205952));
#45144=CARTESIAN_POINT('Ctrl Pts',(1.66094607775778,-2.43009596205664,0.523308424656453));
#45145=CARTESIAN_POINT('Ctrl Pts',(1.73743734516003,-2.37601294348077,0.528360131106955));
#45146=CARTESIAN_POINT('Ctrl Pts',(1.81120153325415,-2.31838586217605,0.533411837557456));
#45147=CARTESIAN_POINT('Ctrl Pts',(1.8849428630771,-2.26077663852673,0.538461978569783));
#45148=CARTESIAN_POINT('Ctrl Pts',(1.95595844546941,-2.1996258058906,0.54351211958211));
#45149=CARTESIAN_POINT('Ctrl Pts',(2.02389929647884,-2.13522730352355,0.548562260594437));
#45150=CARTESIAN_POINT('Ctrl Pts',(2.09183776955575,-2.07083105510668,0.553612224851625));
#45151=CARTESIAN_POINT('Ctrl Pts',(2.15670140547223,-2.00318766693933,0.558662189108813));
#45152=CARTESIAN_POINT('Ctrl Pts',(2.21817701801937,-1.93262896509669,0.563712153366002));
#45153=CARTESIAN_POINT('Ctrl Pts',(2.27966737706337,-1.86205333794606,0.568763328986185));
#45154=CARTESIAN_POINT('Ctrl Pts',(2.33776780880627,-1.78856134071885,0.573814504606368));
#45155=CARTESIAN_POINT('Ctrl Pts',(2.392205184704,-1.71251813253912,0.578865680226551));
#45156=CARTESIAN_POINT('Ctrl Pts',(2.44670262226623,-1.63639102461989,0.583922428893017));
#45157=CARTESIAN_POINT('Ctrl Pts',(2.49752868096425,-1.55770744722914,0.588979177559483));
#45158=CARTESIAN_POINT('Ctrl Pts',(2.5444535663963,-1.47686155358353,0.59403592622595));
#45159=CARTESIAN_POINT('Ctrl Pts',(2.59140876108098,-1.39596344076695,0.599095941096936));
#45160=CARTESIAN_POINT('Ctrl Pts',(2.63445756290023,-1.31290062220285,0.604155955967922));
#45161=CARTESIAN_POINT('Ctrl Pts',(2.67341711042726,-1.22808996155605,0.609215970838908));
#45162=CARTESIAN_POINT('Ctrl Pts',(2.71243650719976,-1.14314901566804,0.6142837588513));
#45163=CARTESIAN_POINT('Ctrl Pts',(2.74735394768481,-1.05645527715427,0.619351546863693));
#45164=CARTESIAN_POINT('Ctrl Pts',(2.77803555508529,-0.968443315161994,
0.624419334876086));
#45165=CARTESIAN_POINT('Ctrl Pts',(2.78796839996764,-0.939950376221435,
0.626059977478889));
#45166=CARTESIAN_POINT('Ctrl Pts',(2.79745769571003,-0.911319374307146,
0.627700620081692));
#45167=CARTESIAN_POINT('Ctrl Pts',(2.80650004517479,-0.882565293014582,
0.629341262684495));
#45168=CARTESIAN_POINT('Ctrl Pts',(2.83434355154955,-0.794024759507225,
0.634393184527139));
#45169=CARTESIAN_POINT('Ctrl Pts',(2.8580426961888,-0.704007223986515,0.639445106369783));
#45170=CARTESIAN_POINT('Ctrl Pts',(2.87744208044141,-0.612936435289163,
0.644497028212428));
#45171=CARTESIAN_POINT('Ctrl Pts',(2.89681485382117,-0.521990571854782,
0.649542020141828));
#45172=CARTESIAN_POINT('Ctrl Pts',(2.9118994955391,-0.429994757065229,0.654587012071229));
#45173=CARTESIAN_POINT('Ctrl Pts',(2.92259009067868,-0.337388739982193,
0.65963200400063));
#45174=CARTESIAN_POINT('Ctrl Pts',(2.93380733780313,-0.240220662315065,
0.664925527932088));
#45175=CARTESIAN_POINT('Ctrl Pts',(2.94018634157949,-0.14238118685994,0.670219051863546));
#45176=CARTESIAN_POINT('Ctrl Pts',(2.94166506875022,-0.0443917029946411,
0.675512575795003));
#45177=CARTESIAN_POINT('Ctrl Pts',(2.94307183060904,0.0488289202518063,
0.680548479451143));
#45178=CARTESIAN_POINT('Ctrl Pts',(2.94004407342124,0.142184790760255,0.685584383107282));
#45179=CARTESIAN_POINT('Ctrl Pts',(2.93258153638806,0.235222304290782,0.690620286763422));
#45180=CARTESIAN_POINT('Ctrl Pts',(2.92512156149596,0.328227874899626,0.695654461423697));
#45181=CARTESIAN_POINT('Ctrl Pts',(2.91322986727545,0.420914863234052,0.700688636083973));
#45182=CARTESIAN_POINT('Ctrl Pts',(2.89695823735506,0.512832303019893,0.705722810744248));
#45183=CARTESIAN_POINT('Ctrl Pts',(2.88068764156459,0.604743901069218,0.710756665461736));
#45184=CARTESIAN_POINT('Ctrl Pts',(2.86003774144722,0.695885610416984,0.715790520179223));
#45185=CARTESIAN_POINT('Ctrl Pts',(2.83511168149093,0.785815343114191,0.720824374896711));
#45186=CARTESIAN_POINT('Ctrl Pts',(2.81018023198376,0.875764520556002,0.725859318041979));
#45187=CARTESIAN_POINT('Ctrl Pts',(2.78097090544223,0.964500772946039,0.730894261187247));
#45188=CARTESIAN_POINT('Ctrl Pts',(2.74763675774148,1.05159699862061,0.735929204332515));
#45189=CARTESIAN_POINT('Ctrl Pts',(2.7142663279024,1.13878802309839,0.740969627699006));
#45190=CARTESIAN_POINT('Ctrl Pts',(2.67676227588859,1.2243350429165,0.746010051065497));
#45191=CARTESIAN_POINT('Ctrl Pts',(2.63532574672929,1.30783110860146,0.751050474431987));
#45192=CARTESIAN_POINT('Ctrl Pts',(2.59386296360743,1.39138007694564,0.756094091383679));
#45193=CARTESIAN_POINT('Ctrl Pts',(2.54846295945311,1.47287511674493,0.76113770833537));
#45194=CARTESIAN_POINT('Ctrl Pts',(2.49937169266774,1.5519359335653,0.766181325287062));
#45195=CARTESIAN_POINT('Ctrl Pts',(2.45020449602868,1.63111903438132,0.7712327432413));
#45196=CARTESIAN_POINT('Ctrl Pts',(2.39733489394231,1.70786003317449,0.776284161195538));
#45197=CARTESIAN_POINT('Ctrl Pts',(2.34105060003791,1.7818097788659,0.781335579149776));
#45198=CARTESIAN_POINT('Ctrl Pts',(2.32121363730996,1.80787279302601,0.78311591221839));
#45199=CARTESIAN_POINT('Ctrl Pts',(2.30095286381563,1.83358941222552,0.784896245287003));
#45200=CARTESIAN_POINT('Ctrl Pts',(2.28028196720395,1.85894544030869,0.786676578355616));
#45201=CARTESIAN_POINT('Ctrl Pts',(2.22152962691378,1.93101420531368,0.791736771739677));
#45202=CARTESIAN_POINT('Ctrl Pts',(2.15925557718462,2.00041973759941,0.796796965123737));
#45203=CARTESIAN_POINT('Ctrl Pts',(2.09373019662748,2.0667989412931,0.801857158507798));
#45204=CARTESIAN_POINT('Ctrl Pts',(2.02829324392291,2.13308856488227,0.806910523056516));
#45205=CARTESIAN_POINT('Ctrl Pts',(1.95961398874799,2.19635966400071,0.811963887605234));
#45206=CARTESIAN_POINT('Ctrl Pts',(1.88800327535986,2.25628181578242,0.817017252153952));
#45207=CARTESIAN_POINT('Ctrl Pts',(1.81301877070208,2.31902707632783,0.822308695565318));
#45208=CARTESIAN_POINT('Ctrl Pts',(1.73482010442831,2.37809969142808,0.827600138976684));
#45209=CARTESIAN_POINT('Ctrl Pts',(1.65380805324627,2.43316315174667,0.83289158238805));
#45210=CARTESIAN_POINT('Ctrl Pts',(1.57657718863523,2.48565655966353,0.837936051003985));
#45211=CARTESIAN_POINT('Ctrl Pts',(1.49679007148308,2.53450636709367,0.842980519619919));
#45212=CARTESIAN_POINT('Ctrl Pts',(1.41482693862869,2.57946287698245,0.848024988235853));
#45213=CARTESIAN_POINT('Ctrl Pts',(1.33289104795545,2.6244044446241,0.853067780215926));
#45214=CARTESIAN_POINT('Ctrl Pts',(1.24878096634701,2.66545507322319,0.858110572195999));
#45215=CARTESIAN_POINT('Ctrl Pts',(1.16290326250868,2.70241003588402,0.863153364176072));
#45216=CARTESIAN_POINT('Ctrl Pts',(1.0770303008776,2.73936295787441,0.868195877690797));
#45217=CARTESIAN_POINT('Ctrl Pts',(0.989390317856509,2.77222048917931,0.873238391205521));
#45218=CARTESIAN_POINT('Ctrl Pts',(0.900410641304936,2.80082571343253,0.878280904720246));
#45219=CARTESIAN_POINT('Ctrl Pts',(0.811411218019824,2.82943728587404,0.883324537290182));
#45220=CARTESIAN_POINT('Ctrl Pts',(0.721071932073303,2.85379454182169,0.888368169860118));
#45221=CARTESIAN_POINT('Ctrl Pts',(0.629834990614495,2.87379050812644,0.893411802430054));
#45222=CARTESIAN_POINT('Ctrl Pts',(0.53849896313161,2.89380819064358,0.898460912534531));
#45223=CARTESIAN_POINT('Ctrl Pts',(0.446263767364402,2.9094550357618,0.903510022639008));
#45224=CARTESIAN_POINT('Ctrl Pts',(0.35358118898701,2.92067532307077,0.908559132743485));
#45225=CARTESIAN_POINT('Ctrl Pts',(0.260839829542242,2.93190272650097,0.913611445090352));
#45226=CARTESIAN_POINT('Ctrl Pts',(0.167650963502087,2.93869795083421,0.918663757437218));
#45227=CARTESIAN_POINT('Ctrl Pts',(0.0744687496395253,2.94105736178795,
0.923716069784084));
#45228=CARTESIAN_POINT('Ctrl Pts',(-0.018856247074606,2.94342038806065,
0.928776123775349));
#45229=CARTESIAN_POINT('Ctrl Pts',(-0.112174129778242,2.9413340453754,0.933836177766613));
#45230=CARTESIAN_POINT('Ctrl Pts',(-0.205033788460614,2.93484669882253,
0.938896231757877));
#45231=CARTESIAN_POINT('Ctrl Pts',(-0.236327173408762,2.93266048539194,
0.940601452514165));
#45232=CARTESIAN_POINT('Ctrl Pts',(-0.267568591902607,2.92997489653949,
0.942306673270454));
#45233=CARTESIAN_POINT('Ctrl Pts',(-0.298741044927317,2.92679308938567,
0.944011894026742));
#45234=CARTESIAN_POINT('Ctrl Pts',(-0.39123235943881,2.9173523974406,0.949071428775464));
#45235=CARTESIAN_POINT('Ctrl Pts',(-0.483435904631205,2.90350675974296,
0.954130963524185));
#45236=CARTESIAN_POINT('Ctrl Pts',(-0.574899822984667,2.88528234208235,
0.959190498272906));
#45237=CARTESIAN_POINT('Ctrl Pts',(-0.666240499171527,2.86708248073594,
0.964243215600773));
#45238=CARTESIAN_POINT('Ctrl Pts',(-0.756843098468711,2.84451565082106,
0.969295932928639));
#45239=CARTESIAN_POINT('Ctrl Pts',(-0.846260802748927,2.81765978317659,
0.974348650256506));
#45240=CARTESIAN_POINT('Ctrl Pts',(-0.939906120169776,2.78953418690432,
0.979640256899896));
#45241=CARTESIAN_POINT('Ctrl Pts',(-1.03225124784787,2.75670402781351,0.984931863543286));
#45242=CARTESIAN_POINT('Ctrl Pts',(-1.12279461453534,2.71931907902887,0.990223470186676));
#45243=CARTESIAN_POINT('Ctrl Pts',(-1.20909876630351,2.68368448301378,0.99526732529784));
#45244=CARTESIAN_POINT('Ctrl Pts',(-1.29376560658863,2.64391217426158,1.000311180409));
#45245=CARTESIAN_POINT('Ctrl Pts',(-1.37637759321857,2.60018243992337,1.00535503552017));
#45246=CARTESIAN_POINT('Ctrl Pts',(-1.4589623444017,2.55646712236537,1.01039722777763));
#45247=CARTESIAN_POINT('Ctrl Pts',(-1.53949319701646,2.5087971784811,1.0154394200351));
#45248=CARTESIAN_POINT('Ctrl Pts',(-1.61757569704293,2.45739961429477,1.02048161229256));
#45249=CARTESIAN_POINT('Ctrl Pts',(-1.69565411141169,2.40600473948,1.02552354071791));
#45250=CARTESIAN_POINT('Ctrl Pts',(-1.77128405842607,2.350882876062,1.03056546914325));
#45251=CARTESIAN_POINT('Ctrl Pts',(-1.84409960994581,2.29230465440301,1.03560739756859));
#45252=CARTESIAN_POINT('Ctrl Pts',(-1.91693154667289,2.23371325126991,1.04065046054611));
#45253=CARTESIAN_POINT('Ctrl Pts',(-1.98694748536537,2.17166422283282,1.04569352352363));
#45254=CARTESIAN_POINT('Ctrl Pts',(-2.05381503892687,2.10646808328012,1.05073658650115));
#45255=CARTESIAN_POINT('Ctrl Pts',(-2.12075557248106,2.04120078793458,1.05578515353378));
#45256=CARTESIAN_POINT('Ctrl Pts',(-2.18454054577324,1.97277983592785,1.0608337205664));
#45257=CARTESIAN_POINT('Ctrl Pts',(-2.244875119947,1.90155191773534,1.06588228759902));
#45258=CARTESIAN_POINT('Ctrl Pts',(-2.30524813984925,1.83027861247842,1.07093407162356));
#45259=CARTESIAN_POINT('Ctrl Pts',(-2.36216611417598,1.75619513085989,1.0759858556481));
#45260=CARTESIAN_POINT('Ctrl Pts',(-2.41537641249584,1.67967877463482,1.08103763967264));
#45261=CARTESIAN_POINT('Ctrl Pts',(-2.46866853256563,1.60304475881447,1.0860971918515));
#45262=CARTESIAN_POINT('Ctrl Pts',(-2.51824136337206,1.52397077629439,1.09115674403037));
#45263=CARTESIAN_POINT('Ctrl Pts',(-2.56388738984611,1.44286016376782,1.09621629620923));
#45264=CARTESIAN_POINT('Ctrl Pts',(-2.57931733335747,1.41544195749376,1.09792660070545));
#45265=CARTESIAN_POINT('Ctrl Pts',(-2.59429897366065,1.38779120837025,1.09963690520166));
#45266=CARTESIAN_POINT('Ctrl Pts',(-2.60882554488161,1.35992399654289,1.10134720969787));
#45267=CARTESIAN_POINT('Ctrl Pts',(-2.65422890282685,1.27282395247274,1.10669283228531));
#45268=CARTESIAN_POINT('Ctrl Pts',(-2.69532627336188,1.18333337786699,1.11203845487275));
#45269=CARTESIAN_POINT('Ctrl Pts',(-2.73187469153183,1.09189041106143,1.11738407746019));
#45270=CARTESIAN_POINT('Ctrl Pts',(-2.76831966707044,1.00070625439259,1.12271457038418));
#45271=CARTESIAN_POINT('Ctrl Pts',(-2.80024121316959,0.907581057944109,
1.12804506330817));
#45272=CARTESIAN_POINT('Ctrl Pts',(-2.8274432620727,0.812975153224073,1.13337555623216));
#45273=CARTESIAN_POINT('Ctrl Pts',(-2.85459889591541,0.718530675269989,
1.13869695369602));
#45274=CARTESIAN_POINT('Ctrl Pts',(-2.87705096140675,0.622610869338626,
1.14401835115989));
#45275=CARTESIAN_POINT('Ctrl Pts',(-2.89465180269297,0.525694722406793,
1.14933974862376));
#45276=CARTESIAN_POINT('Ctrl Pts',(-2.91221171667489,0.429003934966152,
1.15464877222153));
#45277=CARTESIAN_POINT('Ctrl Pts',(-2.92494282082446,0.33132178351378,1.1599577958193));
#45278=CARTESIAN_POINT('Ctrl Pts',(-2.93274783360769,0.233139753086851,
1.16526681941707));
#45279=CARTESIAN_POINT('Ctrl Pts',(-2.93890138450316,0.155732048829,1.16945250723354));
#45280=CARTESIAN_POINT('Ctrl Pts',(-2.94199387730798,0.0780139969306237,
1.17363819505001));
#45281=CARTESIAN_POINT('Ctrl Pts',(-2.94199999091258,0.0002312366468149,
1.17782388286648));
#45282=CARTESIAN_POINT('',(-2.94199916389813,-0.00221802224694258,2.1778238829104));
#45283=CARTESIAN_POINT('Ctrl Pts',(-2.94199999091264,0.000231235830579614,
1.1778238829104));
#45284=CARTESIAN_POINT('Ctrl Pts',(-2.94200765316831,-0.0972551962378792,
1.18306987533197));
#45285=CARTESIAN_POINT('Ctrl Pts',(-2.93716551547198,-0.194662940964098,
1.18831586775354));
#45286=CARTESIAN_POINT('Ctrl Pts',(-2.92752287042165,-0.291502732677018,
1.19356186017511));
#45287=CARTESIAN_POINT('Ctrl Pts',(-2.91754802661955,-0.391678751925135,
1.1989885822746));
#45288=CARTESIAN_POINT('Ctrl Pts',(-2.90243600485248,-0.491246522856216,
1.20441530437409));
#45289=CARTESIAN_POINT('Ctrl Pts',(-2.88229873438933,-0.589676187188932,
1.20984202647358));
#45290=CARTESIAN_POINT('Ctrl Pts',(-2.86276374898589,-0.685161921440928,
1.2151064408934));
#45291=CARTESIAN_POINT('Ctrl Pts',(-2.83850002950619,-0.779576312685586,
1.22037085531322));
#45292=CARTESIAN_POINT('Ctrl Pts',(-2.80966034937286,-0.872452131157923,
1.22563526973304));
#45293=CARTESIAN_POINT('Ctrl Pts',(-2.77948693070997,-0.969623144895513,
1.23114314567237));
#45294=CARTESIAN_POINT('Ctrl Pts',(-2.74430432737846,-1.06510939896652,
1.23665102161169));
#45295=CARTESIAN_POINT('Ctrl Pts',(-2.70434292712315,-1.15840119670129,
1.24215889755102));
#45296=CARTESIAN_POINT('Ctrl Pts',(-2.66438152686785,-1.25169299443606,
1.24766677349034));
#45297=CARTESIAN_POINT('Ctrl Pts',(-2.61964160962512,-1.34278994127986,
1.25317464942966));
#45298=CARTESIAN_POINT('Ctrl Pts',(-2.57040644515614,-1.43121441674537,
1.25868252536899));
#45299=CARTESIAN_POINT('Ctrl Pts',(-2.52518458599781,-1.5124311491109,1.26374143788967));
#45300=CARTESIAN_POINT('Ctrl Pts',(-2.47603107530938,-1.59164364202472,
1.26880035041034));
#45301=CARTESIAN_POINT('Ctrl Pts',(-2.42314835223583,-1.66844720115945,
1.27385926293102));
#45302=CARTESIAN_POINT('Ctrl Pts',(-2.37033708093894,-1.74514698820312,
1.2789113401704));
#45303=CARTESIAN_POINT('Ctrl Pts',(-2.31380685980803,-1.819443948046,1.28396341740979));
#45304=CARTESIAN_POINT('Ctrl Pts',(-2.25380569606738,-1.89095845654373,
1.28901549464918));
#45305=CARTESIAN_POINT('Ctrl Pts',(-2.19095787938252,-1.96586584900366,
1.29430725908213));
#45306=CARTESIAN_POINT('Ctrl Pts',(-2.12430185730173,-2.03771980690957,
1.29959902351509));
#45307=CARTESIAN_POINT('Ctrl Pts',(-2.05417342114962,-2.10611859966206,
1.30489078794804));
#45308=CARTESIAN_POINT('Ctrl Pts',(-1.9873393864957,-2.17130424383058,1.30993396282685));
#45309=CARTESIAN_POINT('Ctrl Pts',(-1.91735215473173,-2.23335165073221,
1.31497713770566));
#45310=CARTESIAN_POINT('Ctrl Pts',(-1.84454221207067,-2.2919485220854,1.32002031258447));
#45311=CARTESIAN_POINT('Ctrl Pts',(-1.77175646859857,-2.35052591812093,
1.32506181130838));
#45312=CARTESIAN_POINT('Ctrl Pts',(-1.69615022297717,-2.40565477984259,
1.3301033100323));
#45313=CARTESIAN_POINT('Ctrl Pts',(-1.61808776203471,-2.45706247261918,
1.33514480875621));
#45314=CARTESIAN_POINT('Ctrl Pts',(-1.54002957896282,-2.5084673482228,1.34018603120291));
#45315=CARTESIAN_POINT('Ctrl Pts',(-1.4595158183549,-2.55615121723485,1.34522725364962));
#45316=CARTESIAN_POINT('Ctrl Pts',(-1.37693957557334,-2.59988488307077,
1.35026847609632));
#45317=CARTESIAN_POINT('Ctrl Pts',(-1.29434493859787,-2.64362829075862,
1.35531082149582));
#45318=CARTESIAN_POINT('Ctrl Pts',(-1.20968729840001,-2.68341954067785,
1.36035316689533));
#45319=CARTESIAN_POINT('Ctrl Pts',(-1.12338314000202,-2.71907600496183,
1.36539551229483));
#45320=CARTESIAN_POINT('Ctrl Pts',(-1.0369850038881,-2.75477129603162,1.37044334836955));
#45321=CARTESIAN_POINT('Ctrl Pts',(-0.948937181157173,-2.7863226464533,
1.37549118444428));
#45322=CARTESIAN_POINT('Ctrl Pts',(-0.859674555171333,-2.81359621466744,
1.380539020519));
#45323=CARTESIAN_POINT('Ctrl Pts',(-0.770355194027269,-2.84088711791057,
1.38559006498889));
#45324=CARTESIAN_POINT('Ctrl Pts',(-0.679819921165122,-2.86389471709149,
1.39064110945879));
#45325=CARTESIAN_POINT('Ctrl Pts',(-0.588515064254157,-2.88253603952248,
1.39569215392868));
#45326=CARTESIAN_POINT('Ctrl Pts',(-0.497069908538492,-2.90120600616083,
1.40075095982032));
#45327=CARTESIAN_POINT('Ctrl Pts',(-0.40485324530817,-2.9154962382094,1.40580976571195));
#45328=CARTESIAN_POINT('Ctrl Pts',(-0.312317492516556,-2.92537549450804,
1.41086857160359));
#45329=CARTESIAN_POINT('Ctrl Pts',(-0.280920654748795,-2.92872746818219,
1.4125849947491));
#45330=CARTESIAN_POINT('Ctrl Pts',(-0.249487087405726,-2.93157209130842,
1.4143014178946));
#45331=CARTESIAN_POINT('Ctrl Pts',(-0.218034427519059,-2.93390950583286,
1.41601784104011));
#45332=CARTESIAN_POINT('Ctrl Pts',(-0.12533607140344,-2.9407984139493,1.42107654210261));
#45333=CARTESIAN_POINT('Ctrl Pts',(-0.032149715563284,-2.94330172661396,
1.42613524316511));
#45334=CARTESIAN_POINT('Ctrl Pts',(0.061075339909064,-2.9413659756744,1.43119394422761));
#45335=CARTESIAN_POINT('Ctrl Pts',(0.154174426977337,-2.93943284037775,
1.43624580982623));
#45336=CARTESIAN_POINT('Ctrl Pts',(0.24731167059882,-2.93307257090482,1.44129767542485));
#45337=CARTESIAN_POINT('Ctrl Pts',(0.340033650333316,-2.92228354487394,
1.44634954102347));
#45338=CARTESIAN_POINT('Ctrl Pts',(0.437159705798388,-2.91098206550853,
1.4516413583438));
#45339=CARTESIAN_POINT('Ctrl Pts',(0.533829582463102,-2.89482065294382,
1.45693317566412));
#45340=CARTESIAN_POINT('Ctrl Pts',(0.629523046017409,-2.87385885779608,
1.46222499298444));
#45341=CARTESIAN_POINT('Ctrl Pts',(0.720716429955741,-2.85388281176384,
1.46726795736989));
#45342=CARTESIAN_POINT('Ctrl Pts',(0.811022666097952,-2.82954774423491,
1.47231092175533));
#45343=CARTESIAN_POINT('Ctrl Pts',(0.899999209849383,-2.80095794725135,
1.47735388614077));
#45344=CARTESIAN_POINT('Ctrl Pts',(0.988946195632898,-2.77237764778552,
1.4823951752557));
#45345=CARTESIAN_POINT('Ctrl Pts',(1.0765639453971,-2.73954556257775,1.48743646437063));
#45346=CARTESIAN_POINT('Ctrl Pts',(1.16242445608337,-2.70261602598284,1.49247775348557));
#45347=CARTESIAN_POINT('Ctrl Pts',(1.24828028117491,-2.66568850471303,1.49751876748639));
#45348=CARTESIAN_POINT('Ctrl Pts',(1.33237865122145,-2.62466415215104,1.50255978148722));
#45349=CARTESIAN_POINT('Ctrl Pts',(1.41431200286067,-2.57974525071067,1.50760079548805));
#45350=CARTESIAN_POINT('Ctrl Pts',(1.49626362969372,-2.53481633013139,1.51264293388457));
#45351=CARTESIAN_POINT('Ctrl Pts',(1.57604889086872,-2.48599134852284,1.51768507228109));
#45352=CARTESIAN_POINT('Ctrl Pts',(1.65328625784548,-2.43351773151939,1.52272721067762));
#45353=CARTESIAN_POINT('Ctrl Pts',(1.73060778418476,-2.38098693822513,1.52777484308785));
#45354=CARTESIAN_POINT('Ctrl Pts',(1.80537550886616,-2.32479982438058,1.53282247549809));
#45355=CARTESIAN_POINT('Ctrl Pts',(1.8772385351632,-2.26524600917832,1.53787010790832));
#45356=CARTESIAN_POINT('Ctrl Pts',(1.94914726350187,-2.20565432010571,1.54292095041307));
#45357=CARTESIAN_POINT('Ctrl Pts',(2.01814728913691,-2.14269196536669,1.54797179291781));
#45358=CARTESIAN_POINT('Ctrl Pts',(2.08392391124165,-2.0766860937935,1.55302263542256));
#45359=CARTESIAN_POINT('Ctrl Pts',(2.14980166466098,-2.0105787384355,1.55808124357909));
#45360=CARTESIAN_POINT('Ctrl Pts',(2.21244582682778,-1.941418854671,1.56313985173561));
#45361=CARTESIAN_POINT('Ctrl Pts',(2.27158155730201,-1.86956712330031,1.56819845989214));
#45362=CARTESIAN_POINT('Ctrl Pts',(2.29166789675473,-1.84516160306739,1.56991669216517));
#45363=CARTESIAN_POINT('Ctrl Pts',(2.31134982887331,-1.82044576576877,1.5716349244382));
#45364=CARTESIAN_POINT('Ctrl Pts',(2.33061774403031,-1.79543446864849,1.57335315671124));
#45365=CARTESIAN_POINT('Ctrl Pts',(2.38734249612612,-1.72180119710962,1.57841163340354));
#45366=CARTESIAN_POINT('Ctrl Pts',(2.44067303442736,-1.64534888832417,1.58347011009584));
#45367=CARTESIAN_POINT('Ctrl Pts',(2.49031762523661,-1.56642335447218,1.58852858678814));
#45368=CARTESIAN_POINT('Ctrl Pts',(2.53989508790734,-1.48760454169661,1.59358022353839));
#45369=CARTESIAN_POINT('Ctrl Pts',(2.58579627403676,-1.40631952173164,1.59863186028864));
#45370=CARTESIAN_POINT('Ctrl Pts',(2.62777048391585,-1.3229460623399,1.6036834970389));
#45371=CARTESIAN_POINT('Ctrl Pts',(2.67174083249057,-1.23560766855251,1.60897537101154));
#45372=CARTESIAN_POINT('Ctrl Pts',(2.71140113034999,-1.14597765671579,1.61426724498419));
#45373=CARTESIAN_POINT('Ctrl Pts',(2.74651498733101,-1.05452331617947,1.61955911895683));
#45374=CARTESIAN_POINT('Ctrl Pts',(2.77997564038546,-0.967374759395649,
1.62460184494111));
#45375=CARTESIAN_POINT('Ctrl Pts',(2.80930806479646,-0.878570225485862,
1.62964457092539));
#45376=CARTESIAN_POINT('Ctrl Pts',(2.83435600314663,-0.788536649387113,
1.63468729690967));
#45377=CARTESIAN_POINT('Ctrl Pts',(2.85939560529548,-0.698533037351899,
1.63972834462493));
#45378=CARTESIAN_POINT('Ctrl Pts',(2.88015343593823,-0.607301622209397,
1.64476939234019));
#45379=CARTESIAN_POINT('Ctrl Pts',(2.89652302991949,-0.515284714644266,
1.64981044005545));
#45380=CARTESIAN_POINT('Ctrl Pts',(2.9128917217824,-0.423272878074804,1.65485120996164));
#45381=CARTESIAN_POINT('Ctrl Pts',(2.92487258077865,-0.330476071339442,
1.65989197986783));
#45382=CARTESIAN_POINT('Ctrl Pts',(2.93241042874529,-0.237345902399574,
1.66493274977402));
#45383=CARTESIAN_POINT('Ctrl Pts',(2.93994995452725,-0.144195004038615,
1.66997464168228));
#45384=CARTESIAN_POINT('Ctrl Pts',(2.94304446969761,-0.0507110375434266,
1.67501653359054));
#45385=CARTESIAN_POINT('Ctrl Pts',(2.94169081752702,0.0426513080366752,
1.6800584254988));
#45386=CARTESIAN_POINT('Ctrl Pts',(2.94033569091073,0.136115347176504,1.68510580921355));
#45387=CARTESIAN_POINT('Ctrl Pts',(2.93452273378389,0.229457057583668,1.69015319292831));
#45388=CARTESIAN_POINT('Ctrl Pts',(2.92430087528032,0.322224131366271,1.69520057664306));
#45389=CARTESIAN_POINT('Ctrl Pts',(2.91407251893188,0.415050175448054,1.70025116888554));
#45390=CARTESIAN_POINT('Ctrl Pts',(2.89942975104263,0.507300418757901,1.70530176112801));
#45391=CARTESIAN_POINT('Ctrl Pts',(2.88047275094337,0.598532147067083,1.71035235337049));
#45392=CARTESIAN_POINT('Ctrl Pts',(2.8614866040822,0.689904145959685,1.71541071099824));
#45393=CARTESIAN_POINT('Ctrl Pts',(2.83817309694171,0.780254076555261,1.720469068626));
#45394=CARTESIAN_POINT('Ctrl Pts',(2.81068233516932,0.869154077691133,1.72552742625376));
#45395=CARTESIAN_POINT('Ctrl Pts',(2.8013327201323,0.89938899057909,1.72724777496329));
#45396=CARTESIAN_POINT('Ctrl Pts',(2.7915003401192,0.929456364812504,1.72896812367282));
#45397=CARTESIAN_POINT('Ctrl Pts',(2.78119234739785,0.959339943281655,1.73068847238236));
#45398=CARTESIAN_POINT('Ctrl Pts',(2.75088182548335,1.04721222691228,1.7357471359525));
#45399=CARTESIAN_POINT('Ctrl Pts',(2.71634999530264,1.1337994539328,1.74080579952265));
#45400=CARTESIAN_POINT('Ctrl Pts',(2.67772531176649,1.21866777865219,1.74586446309279));
#45401=CARTESIAN_POINT('Ctrl Pts',(2.63915283356409,1.30342139487921,1.75091628934556));
#45402=CARTESIAN_POINT('Ctrl Pts',(2.59649867763927,1.38646032609095,1.75596811559833));
#45403=CARTESIAN_POINT('Ctrl Pts',(2.54994055222832,1.46736743186617,1.76101994185109));
#45404=CARTESIAN_POINT('Ctrl Pts',(2.50117055712073,1.55211824857107,1.76631176877619));
#45405=CARTESIAN_POINT('Ctrl Pts',(2.44811661779715,1.63452919777494,1.77160359570129));
#45406=CARTESIAN_POINT('Ctrl Pts',(2.39103904914586,1.71414592886943,1.77689542262639));
#45407=CARTESIAN_POINT('Ctrl Pts',(2.33664617980532,1.79001780908566,1.78193834329227));
#45408=CARTESIAN_POINT('Ctrl Pts',(2.27859990313235,1.86335196543142,1.78698126395815));
#45409=CARTESIAN_POINT('Ctrl Pts',(2.21717092098241,1.93378310757696,1.79202418462403));
#45410=CARTESIAN_POINT('Ctrl Pts',(2.15576236415779,2.00419083115133,1.79706542850329));
#45411=CARTESIAN_POINT('Ctrl Pts',(2.090973627524,2.0716971249235,1.80210667238255));
#45412=CARTESIAN_POINT('Ctrl Pts',(2.02311563396547,2.13596983396407,1.80714791626181));
#45413=CARTESIAN_POINT('Ctrl Pts',(1.95526136329416,2.20023901681657,1.81218888356375));
#45414=CARTESIAN_POINT('Ctrl Pts',(1.8843384924389,2.26127466350019,1.81722985086568));
#45415=CARTESIAN_POINT('Ctrl Pts',(1.81069391041864,2.31878234484672,1.82227081816762));
#45416=CARTESIAN_POINT('Ctrl Pts',(1.73703292248094,2.37630283726837,1.82731290845363));
#45417=CARTESIAN_POINT('Ctrl Pts',(1.66064936836453,2.43029353110668,1.83235499873965));
#45418=CARTESIAN_POINT('Ctrl Pts',(1.58192131534117,2.48050175409518,1.83739708902567));
#45419=CARTESIAN_POINT('Ctrl Pts',(1.50310750675042,2.53076466705103,1.84244467147486));
#45420=CARTESIAN_POINT('Ctrl Pts',(1.42194447643817,2.57723664802215,1.84749225392405));
#45421=CARTESIAN_POINT('Ctrl Pts',(1.33883694336503,2.61970983871897,1.85253983637324));
#45422=CARTESIAN_POINT('Ctrl Pts',(1.25567657527345,2.66221003144234,1.85759062778679));
#45423=CARTESIAN_POINT('Ctrl Pts',(1.17056964643962,2.70070619055931,1.86264141920034));
#45424=CARTESIAN_POINT('Ctrl Pts',(1.0839410443022,2.73503853948661,1.86769221061389));
#45425=CARTESIAN_POINT('Ctrl Pts',(0.997179271437195,2.76942366617753,1.87275076640953));
#45426=CARTESIAN_POINT('Ctrl Pts',(0.908891574806107,2.79963206485873,1.87780932220518));
#45427=CARTESIAN_POINT('Ctrl Pts',(0.819517889678413,2.82555382686245,1.88286787800082));
#45428=CARTESIAN_POINT('Ctrl Pts',(0.789153315268341,2.83436070631559,1.88458651468504));
#45429=CARTESIAN_POINT('Ctrl Pts',(0.758663468110167,2.84267322009762,1.88630515136926));
#45430=CARTESIAN_POINT('Ctrl Pts',(0.728065806503105,2.85048841102731,1.88802378805348));
#45431=CARTESIAN_POINT('Ctrl Pts',(0.638004965636491,2.87349156321913,1.89308240550317));
#45432=CARTESIAN_POINT('Ctrl Pts',(0.546696209144975,2.89226236604903,1.89814102295285));
#45433=CARTESIAN_POINT('Ctrl Pts',(0.454572528752249,2.9066695402305,1.90319964040254));
#45434=CARTESIAN_POINT('Ctrl Pts',(0.362573369558742,2.92105724060677,1.90825142024968));
#45435=CARTESIAN_POINT('Ctrl Pts',(0.269761909506563,2.93109296605129,1.91330320009683));
#45436=CARTESIAN_POINT('Ctrl Pts',(0.176584271950763,2.9366957613787,1.91835497994397));
#45437=CARTESIAN_POINT('Ctrl Pts',(0.0789788687414522,2.94256479939443,
1.92364681843483));
#45438=CARTESIAN_POINT('Ctrl Pts',(-0.0190279012904845,2.9435690350207,
1.92893865692569));
#45439=CARTESIAN_POINT('Ctrl Pts',(-0.116913393579505,2.9396760465061,1.93423049541655));
#45440=CARTESIAN_POINT('Ctrl Pts',(-0.21019367688271,2.93596621103358,1.93927336931011));
#45441=CARTESIAN_POINT('Ctrl Pts',(-0.303363336766012,2.9278095227097,1.94431624320366));
#45442=CARTESIAN_POINT('Ctrl Pts',(-0.395968419911317,2.91523121045878,
1.94935911709722));
#45443=CARTESIAN_POINT('Ctrl Pts',(-0.48854271069598,2.90265708065566,1.95440031417147));
#45444=CARTESIAN_POINT('Ctrl Pts',(-0.580552359244172,2.88566430773528,
1.95944151124571));
#45445=CARTESIAN_POINT('Ctrl Pts',(-0.671548970857717,2.86432993555909,
1.96448270831996));
#45446=CARTESIAN_POINT('Ctrl Pts',(-0.76254059060031,2.84299673373893,1.96952362884539));
#45447=CARTESIAN_POINT('Ctrl Pts',(-0.852518852812673,2.81732250785056,
1.97456454937082));
#45448=CARTESIAN_POINT('Ctrl Pts',(-0.941047095307283,2.7874350870314,1.97960546989625));
#45449=CARTESIAN_POINT('Ctrl Pts',(-1.02959506113424,2.75754100755148,1.98464751349549));
#45450=CARTESIAN_POINT('Ctrl Pts',(-1.11669194615718,2.72343201078684,1.98968955709474));
#45451=CARTESIAN_POINT('Ctrl Pts',(-1.20191882058613,2.68528492877774,1.99473160069398));
#45452=CARTESIAN_POINT('Ctrl Pts',(-1.28723853710523,2.64709629115779,1.99977913685492));
#45453=CARTESIAN_POINT('Ctrl Pts',(-1.3706837727355,2.60486097036844,2.00482667301587));
#45454=CARTESIAN_POINT('Ctrl Pts',(-1.45185837263565,2.55880270161804,2.00987420917681));
#45455=CARTESIAN_POINT('Ctrl Pts',(-1.53308458203182,2.51271514976626,2.0149249544795));
#45456=CARTESIAN_POINT('Ctrl Pts',(-1.61203690779445,2.46280004757637,2.0199756997822));
#45457=CARTESIAN_POINT('Ctrl Pts',(-1.68834826456665,2.40932441517011,2.02502644508489));
#45458=CARTESIAN_POINT('Ctrl Pts',(-1.7647769426638,2.35576656915486,2.03008495541963));
#45459=CARTESIAN_POINT('Ctrl Pts',(-1.8385561989998,2.29863753859219,2.03514346575437));
#45460=CARTESIAN_POINT('Ctrl Pts',(-1.90935232539742,2.23824433373559,2.0402019760891));
#45461=CARTESIAN_POINT('Ctrl Pts',(-1.93341109868383,2.21772080374012,2.04192101863427));
#45462=CARTESIAN_POINT('Ctrl Pts',(-1.95712568315988,2.19682061711989,2.04364006117944));
#45463=CARTESIAN_POINT('Ctrl Pts',(-1.9804840002322,2.17555673904963,2.0453591037246));
#45464=CARTESIAN_POINT('Ctrl Pts',(-2.04821780767799,2.11389632840008,2.05034393616715));
#45465=CARTESIAN_POINT('Ctrl Pts',(-2.11320397033815,2.04894673415118,2.0553287686097));
#45466=CARTESIAN_POINT('Ctrl Pts',(-2.17509965886792,1.98098598530951,2.06031360105224));
#45467=CARTESIAN_POINT('Ctrl Pts',(-2.23689675946619,1.91313348487431,2.06529049361511));
#45468=CARTESIAN_POINT('Ctrl Pts',(-2.29561286624946,1.84227969896945,2.07026738617798));
#45469=CARTESIAN_POINT('Ctrl Pts',(-2.35093969040451,1.76874152212265,2.07524427874085));
#45470=CARTESIAN_POINT('Ctrl Pts',(-2.4062167139959,1.69526953817076,2.08021669152274));
#45471=CARTESIAN_POINT('Ctrl Pts',(-2.45811023643264,1.6191183219238,2.08518910430462));
#45472=CARTESIAN_POINT('Ctrl Pts',(-2.5063507344052,1.540639476369,2.09016151708651));
#45473=CARTESIAN_POINT('Ctrl Pts',(-2.55456216243829,1.46220792251692,2.09513093347025));
#45474=CARTESIAN_POINT('Ctrl Pts',(-2.59912469775304,1.38145191262434,2.10010034985399));
#45475=CARTESIAN_POINT('Ctrl Pts',(-2.63981161566819,1.29875272233913,2.10506976623773));
#45476=CARTESIAN_POINT('Ctrl Pts',(-2.68048611712413,1.21607876943182,2.1100376661007));
#45477=CARTESIAN_POINT('Ctrl Pts',(-2.71728714955538,1.13146322434496,2.11500556596368));
#45478=CARTESIAN_POINT('Ctrl Pts',(-2.75003414804036,1.04531152515026,2.11997346582666));
#45479=CARTESIAN_POINT('Ctrl Pts',(-2.7827967723525,0.959118717102081,2.1249437362136));
#45480=CARTESIAN_POINT('Ctrl Pts',(-2.81150132898006,0.871388716150235,
2.12991400660054));
#45481=CARTESIAN_POINT('Ctrl Pts',(-2.8360158662163,0.782545849499835,2.13488427698748));
#45482=CARTESIAN_POINT('Ctrl Pts',(-2.86053553442199,0.693684387759097,
2.13985558766759));
#45483=CARTESIAN_POINT('Ctrl Pts',(-2.88086332994899,0.603710041624636,
2.14482689834769));
#45484=CARTESIAN_POINT('Ctrl Pts',(-2.89691807202127,0.513059142786233,
2.1497982090278));
#45485=CARTESIAN_POINT('Ctrl Pts',(-2.91299333472207,0.422292377033777,
2.15477587386914));
#45486=CARTESIAN_POINT('Ctrl Pts',(-2.92478456986051,0.330847784809518,
2.15975353871048));
#45487=CARTESIAN_POINT('Ctrl Pts',(-2.93226235225871,0.239168345577429,
2.16473120355182));
#45488=CARTESIAN_POINT('Ctrl Pts',(-2.93881858631446,0.158787314183534,
2.16909543000468));
#45489=CARTESIAN_POINT('Ctrl Pts',(-2.94205981200293,0.0782260192227659,
2.17345965645754));
#45490=CARTESIAN_POINT('Ctrl Pts',(-2.94199916389813,-0.00221802224694258,
2.1778238829104));
#45491=CARTESIAN_POINT('',(-2.94199896327432,0.00246983659489641,3.17782388291039));
#45492=CARTESIAN_POINT('Ctrl Pts',(-2.94409804542743,-0.00221960462873976,
2.1778238829104));
#45493=CARTESIAN_POINT('Ctrl Pts',(-2.94538405566721,-0.155139230593375,
2.18611406173884));
#45494=CARTESIAN_POINT('Ctrl Pts',(-2.86548296735221,-1.27410865528918,
2.24684934579097));
#45495=CARTESIAN_POINT('Ctrl Pts',(-1.43246863664449,-3.15699631612263,
2.36002973506688));
#45496=CARTESIAN_POINT('Ctrl Pts',(1.84914966771388,-2.93244645384978,2.51736505073795));
#45497=CARTESIAN_POINT('Ctrl Pts',(3.46611704321809,-0.0680333465830152,
2.67470036640911));
#45498=CARTESIAN_POINT('Ctrl Pts',(1.96279813083212,2.85762464397294,2.8320356820802));
#45499=CARTESIAN_POINT('Ctrl Pts',(-1.30748115680007,3.21077697834342,2.98937099775136));
#45500=CARTESIAN_POINT('Ctrl Pts',(-2.84098251749962,1.35199077004515,3.1046337313614));
#45501=CARTESIAN_POINT('Ctrl Pts',(-2.94470877622731,0.1939857347123,3.16745135974775));
#45502=CARTESIAN_POINT('Ctrl Pts',(-2.94300132914192,0.00247067809074119,
3.17782388291039));
#45503=CARTESIAN_POINT('',(-2.9419998880025,-0.000811784004742896,4.17782388295008));
#45504=CARTESIAN_POINT('Ctrl Pts',(-2.94199896327432,0.00246983659489641,
3.17782388291039));
#45505=CARTESIAN_POINT('Ctrl Pts',(-2.94207609672993,-0.0894093374798007,
3.18280182766136));
#45506=CARTESIAN_POINT('Ctrl Pts',(-2.93784490838638,-0.181424757288704,
3.18777977241232));
#45507=CARTESIAN_POINT('Ctrl Pts',(-2.92929377041212,-0.273133679037821,
3.19275771716329));
#45508=CARTESIAN_POINT('Ctrl Pts',(-2.92075064746702,-0.364756641504857,
3.19773099605897));
#45509=CARTESIAN_POINT('Ctrl Pts',(-2.907895662613,-0.456073223823022,3.20270427495465));
#45510=CARTESIAN_POINT('Ctrl Pts',(-2.89076924187452,-0.546641738465148,
3.20767755385033));
#45511=CARTESIAN_POINT('Ctrl Pts',(-2.87365122672512,-0.637165802388218,
3.21264839187764));
#45512=CARTESIAN_POINT('Ctrl Pts',(-2.85226602192575,-0.72694207935163,
3.21761922990495));
#45513=CARTESIAN_POINT('Ctrl Pts',(-2.82670563595407,-0.815536171892771,
3.22259006793226));
#45514=CARTESIAN_POINT('Ctrl Pts',(-2.80115020374067,-0.904113094359864,
3.22755994258092));
#45515=CARTESIAN_POINT('Ctrl Pts',(-2.77142132448528,-0.991507848683996,
3.23252981722959));
#45516=CARTESIAN_POINT('Ctrl Pts',(-2.73766131238054,-1.07729965130174,
3.23749969187825));
#45517=CARTESIAN_POINT('Ctrl Pts',(-2.70389781671987,-1.16310030642056,
3.24247007934771));
#45518=CARTESIAN_POINT('Ctrl Pts',(-2.66610253151236,-1.24729725700392,
3.24744046681717));
#45519=CARTESIAN_POINT('Ctrl Pts',(-2.62446600623389,-1.32948944415619,
3.25241085428663));
#45520=CARTESIAN_POINT('Ctrl Pts',(-2.58278806857674,-1.41176338102114,
3.25738618538591));
#45521=CARTESIAN_POINT('Ctrl Pts',(-2.53726147319968,-1.49202816704452,
3.26236151648519));
#45522=CARTESIAN_POINT('Ctrl Pts',(-2.48812260874791,-1.56990760359885,
3.26733684758447));
#45523=CARTESIAN_POINT('Ctrl Pts',(-2.43895604182231,-1.6478309453813,3.27231498357111));
#45524=CARTESIAN_POINT('Ctrl Pts',(-2.38617341628882,-1.72336588853971,
3.27729311955775));
#45525=CARTESIAN_POINT('Ctrl Pts',(-2.33005296738425,-1.79616735556124,
3.28227125554439));
#45526=CARTESIAN_POINT('Ctrl Pts',(-2.27384547617015,-1.86908173700078,
3.28725711257499));
#45527=CARTESIAN_POINT('Ctrl Pts',(-2.21429012675598,-1.93925383529866,
3.2922429696056));
#45528=CARTESIAN_POINT('Ctrl Pts',(-2.15170342491838,-2.00637393603349,
3.2972288266362));
#45529=CARTESIAN_POINT('Ctrl Pts',(-2.12319673533208,-2.03694547632034,
3.29949976078867));
#45530=CARTESIAN_POINT('Ctrl Pts',(-2.0940616444288,-2.06688439207575,3.30177069494113));
#45531=CARTESIAN_POINT('Ctrl Pts',(-2.06433029953457,-2.09616421456515,
3.3040416290936));
#45532=CARTESIAN_POINT('Ctrl Pts',(-1.99810235268668,-2.16138637435783,
3.30910024002693));
#45533=CARTESIAN_POINT('Ctrl Pts',(-1.92866513756462,-2.22358024361117,
3.31415885096025));
#45534=CARTESIAN_POINT('Ctrl Pts',(-1.85632664537554,-2.28241437641564,
3.31921746189358));
#45535=CARTESIAN_POINT('Ctrl Pts',(-1.78408593506831,-2.34116898154338,
3.32426923496671));
#45536=CARTESIAN_POINT('Ctrl Pts',(-1.70895208219965,-2.39657259833702,
3.32932100803984));
#45537=CARTESIAN_POINT('Ctrl Pts',(-1.63126976314557,-2.44833064757336,
3.33437278111297));
#45538=CARTESIAN_POINT('Ctrl Pts',(-1.54989587537742,-2.50254830921043,
3.33966462126512));
#45539=CARTESIAN_POINT('Ctrl Pts',(-1.46572565031327,-2.55276498127177,
3.34495646141728));
#45540=CARTESIAN_POINT('Ctrl Pts',(-1.37919431714492,-2.5986894842507,3.35024830156943));
#45541=CARTESIAN_POINT('Ctrl Pts',(-1.29673416140652,-2.64245330400467,
3.35529116809087));
#45542=CARTESIAN_POINT('Ctrl Pts',(-1.21213047463835,-2.68231944494002,
3.3603340346123));
#45543=CARTESIAN_POINT('Ctrl Pts',(-1.12578816507906,-2.7180811259725,3.36537690113373));
#45544=CARTESIAN_POINT('Ctrl Pts',(-1.03947456896874,-2.75383091432793,
3.37041809063157));
#45545=CARTESIAN_POINT('Ctrl Pts',(-0.951423907716638,-2.78547878548452,
3.3754592801294));
#45546=CARTESIAN_POINT('Ctrl Pts',(-0.862062377406132,-2.81286552424052,
3.38050046962724));
#45547=CARTESIAN_POINT('Ctrl Pts',(-0.772705752737703,-2.84025075955832,
3.38554138238103));
#45548=CARTESIAN_POINT('Ctrl Pts',(-0.68203882572377,-2.86337519832434,
3.39058229513482));
#45549=CARTESIAN_POINT('Ctrl Pts',(-0.590503227705854,-2.88212941036119,
3.39562320788861));
#45550=CARTESIAN_POINT('Ctrl Pts',(-0.498947239694171,-2.90088779998879,
3.40066524352991));
#45551=CARTESIAN_POINT('Ctrl Pts',(-0.406522630247812,-2.91527394084624,
3.40570727917121));
#45552=CARTESIAN_POINT('Ctrl Pts',(-0.313680384700831,-2.9252296689754,
3.41074931481251));
#45553=CARTESIAN_POINT('Ctrl Pts',(-0.220737005413307,-2.93519624195239,
3.4157968427803));
#45554=CARTESIAN_POINT('Ctrl Pts',(-0.127375523015461,-2.94072272327685,
3.42084437074808));
#45555=CARTESIAN_POINT('Ctrl Pts',(-0.0340508628673662,-2.94180294016067,
3.42589189871587));
#45556=CARTESIAN_POINT('Ctrl Pts',(0.0593331289896063,-2.94288384379882,
3.43094263567965));
#45557=CARTESIAN_POINT('Ctrl Pts',(0.152679809900273,-2.93951287148972,
3.43599337264342));
#45558=CARTESIAN_POINT('Ctrl Pts',(0.24553757471319,-2.93173588500123,3.4410441096072));
#45559=CARTESIAN_POINT('Ctrl Pts',(0.33853809684408,-2.92394694235879,3.44610261145379));
#45560=CARTESIAN_POINT('Ctrl Pts',(0.43104776463672,-2.91173852448358,3.45116111330039));
#45561=CARTESIAN_POINT('Ctrl Pts',(0.522623673943699,-2.89520785012641,
3.45621961514698));
#45562=CARTESIAN_POINT('Ctrl Pts',(0.553745348809922,-2.88958997227451,
3.45793872501956));
#45563=CARTESIAN_POINT('Ctrl Pts',(0.584759300125497,-2.88347332283188,
3.45965783489214));
#45564=CARTESIAN_POINT('Ctrl Pts',(0.615648561873941,-2.87686302215843,
3.46137694476471));
#45565=CARTESIAN_POINT('Ctrl Pts',(0.706542552901808,-2.85741171202365,
3.46643555570228));
#45566=CARTESIAN_POINT('Ctrl Pts',(0.79667193421986,-2.83361467773313,3.47149416663984));
#45567=CARTESIAN_POINT('Ctrl Pts',(0.885590508863522,-2.80554690757628,
3.47655277757741));
#45568=CARTESIAN_POINT('Ctrl Pts',(0.974388889872346,-2.77751707738114,
3.48160455065418));
#45569=CARTESIAN_POINT('Ctrl Pts',(1.06197929791018,-2.74522811605334,3.48665632373094));
#45570=CARTESIAN_POINT('Ctrl Pts',(1.14792615578853,-2.70880592528453,3.49170809680771));
#45571=CARTESIAN_POINT('Ctrl Pts',(1.23795732434584,-2.67065290285555,3.49699993695888));
#45572=CARTESIAN_POINT('Ctrl Pts',(1.32618438167442,-2.6279641773414,3.50229177711006));
#45573=CARTESIAN_POINT('Ctrl Pts',(1.4121247963118,-2.58094315312084,3.50758361726123));
#45574=CARTESIAN_POINT('Ctrl Pts',(1.49402183545367,-2.5361344018793,3.51262648378476));
#45575=CARTESIAN_POINT('Ctrl Pts',(1.57384208259694,-2.48739200595837,3.51766935030828));
#45576=CARTESIAN_POINT('Ctrl Pts',(1.65119017222557,-2.43494045412731,3.52271221683181));
#45577=CARTESIAN_POINT('Ctrl Pts',(1.72851253945697,-2.38250634525648,3.52775340633117));
#45578=CARTESIAN_POINT('Ctrl Pts',(1.80336401640768,-2.32636577968637,3.53279459583053));
#45579=CARTESIAN_POINT('Ctrl Pts',(1.87537726051578,-2.26678718249869,3.53783578532989));
#45580=CARTESIAN_POINT('Ctrl Pts',(1.94738655133499,-2.2072118559789,3.54287669808462));
#45581=CARTESIAN_POINT('Ctrl Pts',(2.01655757819793,-2.14419915586197,3.54791761083935));
#45582=CARTESIAN_POINT('Ctrl Pts',(2.08255609327364,-2.07805777551271,3.55295852359408));
#45583=CARTESIAN_POINT('Ctrl Pts',(2.1485693098279,-2.01190166186099,3.55800055923575));
#45584=CARTESIAN_POINT('Ctrl Pts',(2.211408298451,-1.94261579748505,3.56304259487742));
#45585=CARTESIAN_POINT('Ctrl Pts',(2.27077648720559,-1.87054487921414,3.5680846305191));
#45586=CARTESIAN_POINT('Ctrl Pts',(2.33020934615421,-1.79839545357478,3.57313215848637));
#45587=CARTESIAN_POINT('Ctrl Pts',(2.38616357782505,-1.72345526165858,3.57817968645365));
#45588=CARTESIAN_POINT('Ctrl Pts',(2.43838386875336,-1.64610088044548,3.58322721442093));
#45589=CARTESIAN_POINT('Ctrl Pts',(2.49063735903756,-1.56869732073135,3.58827795138368));
#45590=CARTESIAN_POINT('Ctrl Pts',(2.53915195290377,-1.48887689420251,3.59332868834643));
#45591=CARTESIAN_POINT('Ctrl Pts',(2.58371762390874,-1.40704201781731,3.59837942530919));
#45592=CARTESIAN_POINT('Ctrl Pts',(2.62835180910919,-1.32508133045268,3.60343792715401));
#45593=CARTESIAN_POINT('Ctrl Pts',(2.66902476244129,-1.24110041006272,3.60849642899883));
#45594=CARTESIAN_POINT('Ctrl Pts',(2.7055741373795,-1.15552264674613,3.61355493084364));
#45595=CARTESIAN_POINT('Ctrl Pts',(2.71799528358231,-1.12643941586566,3.61527404070771));
#45596=CARTESIAN_POINT('Ctrl Pts',(2.72994060057553,-1.09717189167846,3.61699315057177));
#45597=CARTESIAN_POINT('Ctrl Pts',(2.7414050356843,-1.06773706048107,3.61871226043584));
#45598=CARTESIAN_POINT('Ctrl Pts',(2.77514000445211,-0.981122839919069,
3.62377087143782));
#45599=CARTESIAN_POINT('Ctrl Pts',(2.80482480636004,-0.892757592239818,
3.62882948243979));
#45600=CARTESIAN_POINT('Ctrl Pts',(2.83027671647024,-0.803055233596317,
3.63388809344177));
#45601=CARTESIAN_POINT('Ctrl Pts',(2.85569422255346,-0.713474128027892,
3.63893986658409));
#45602=CARTESIAN_POINT('Ctrl Pts',(2.87689008777899,-0.62255992597192,3.6439916397264));
#45603=CARTESIAN_POINT('Ctrl Pts',(2.89372995174022,-0.530745670167476,
3.64904341286872));
#45604=CARTESIAN_POINT('Ctrl Pts',(2.91137006848068,-0.434568278559255,
3.65433525300364));
#45605=CARTESIAN_POINT('Ctrl Pts',(2.92422973198416,-0.33740362490082,3.65962709313857));
#45606=CARTESIAN_POINT('Ctrl Pts',(2.93221349554032,-0.239766587687357,
3.6649189332735));
#45607=CARTESIAN_POINT('Ctrl Pts',(2.93982163438892,-0.146723234053386,
3.66996179986491));
#45608=CARTESIAN_POINT('Ctrl Pts',(2.94300223870384,-0.053251436215734,
3.67500466645633));
#45609=CARTESIAN_POINT('Ctrl Pts',(2.94172540372301,0.040195137650254,3.68004753304774));
#45610=CARTESIAN_POINT('Ctrl Pts',(2.94044899335824,0.133610635521468,3.68508872261571));
#45611=CARTESIAN_POINT('Ctrl Pts',(2.93471809501812,0.227000483602088,3.69012991218367));
#45612=CARTESIAN_POINT('Ctrl Pts',(2.92455491072272,0.319910259553554,3.69517110175163));
#45613=CARTESIAN_POINT('Ctrl Pts',(2.91439228435121,0.412814935077624,3.70021201457561));
#45614=CARTESIAN_POINT('Ctrl Pts',(2.8997979045185,0.505239150647992,3.70525292739959));
#45615=CARTESIAN_POINT('Ctrl Pts',(2.88084580525227,0.596733982910627,3.71029384022357));
#45616=CARTESIAN_POINT('Ctrl Pts',(2.86188948431516,0.688249196085401,3.71533587593503));
#45617=CARTESIAN_POINT('Ctrl Pts',(2.83857360614135,0.778834181212185,3.72037791164649));
#45618=CARTESIAN_POINT('Ctrl Pts',(2.81102299374745,0.86805168545608,3.72541994735795));
#45619=CARTESIAN_POINT('Ctrl Pts',(2.78344237027186,0.957366374973706,3.73046747539544));
#45620=CARTESIAN_POINT('Ctrl Pts',(2.75161793717882,1.04531018701869,3.73551500343292));
#45621=CARTESIAN_POINT('Ctrl Pts',(2.71572383253706,1.13146279894224,3.74056253147041));
#45622=CARTESIAN_POINT('Ctrl Pts',(2.67980690800608,1.21767018289814,3.74561326850368));
#45623=CARTESIAN_POINT('Ctrl Pts',(2.63981535049567,1.30208369989305,3.75066400553696));
#45624=CARTESIAN_POINT('Ctrl Pts',(2.59596978338854,1.38430664367893,3.75571474257024));
#45625=CARTESIAN_POINT('Ctrl Pts',(2.55205680915813,1.46665599504657,3.7607732444855));
#45626=CARTESIAN_POINT('Ctrl Pts',(2.5042782264363,1.54680767233615,3.76583174640075));
#45627=CARTESIAN_POINT('Ctrl Pts',(2.45289839477102,1.62439326055292,3.77089024831601));
#45628=CARTESIAN_POINT('Ctrl Pts',(2.43543718865496,1.65076037588944,3.77260935757966));
#45629=CARTESIAN_POINT('Ctrl Pts',(2.41756040143675,1.67683140096625,3.77432846684332));
#45630=CARTESIAN_POINT('Ctrl Pts',(2.39927944231628,1.70259277505764,3.77604757610697));
#45631=CARTESIAN_POINT('Ctrl Pts',(2.34548631689361,1.77839759571429,3.78110618707074));
#45632=CARTESIAN_POINT('Ctrl Pts',(2.28800353010066,1.85178242755046,3.78616479803451));
#45633=CARTESIAN_POINT('Ctrl Pts',(2.22707632263131,1.92236704434273,3.79122340899828));
#45634=CARTESIAN_POINT('Ctrl Pts',(2.16623147210298,1.99285625001469,3.79627518210189));
#45635=CARTESIAN_POINT('Ctrl Pts',(2.1019517406955,2.06055243035501,3.8013269552055));
#45636=CARTESIAN_POINT('Ctrl Pts',(2.03452493941518,2.12510523760534,3.80637872830911));
#45637=CARTESIAN_POINT('Ctrl Pts',(1.96389392600361,2.19272568093168,3.81167056845365));
#45638=CARTESIAN_POINT('Ctrl Pts',(1.88980960211925,2.25689618708895,3.81696240859819));
#45639=CARTESIAN_POINT('Ctrl Pts',(1.81264952932897,2.31725391008916,3.82225424874273));
#45640=CARTESIAN_POINT('Ctrl Pts',(1.73911972880963,2.37477188760673,3.82729711529453));
#45641=CARTESIAN_POINT('Ctrl Pts',(1.6627974297708,2.42882741253796,3.83233998184632));
#45642=CARTESIAN_POINT('Ctrl Pts',(1.58404510922458,2.47914604086603,3.83738284839812));
#45643=CARTESIAN_POINT('Ctrl Pts',(1.50531897805058,2.52944793555021,3.8424240379262));
#45644=CARTESIAN_POINT('Ctrl Pts',(1.42416480392375,2.5760151645365,3.84746522745428));
#45645=CARTESIAN_POINT('Ctrl Pts',(1.34097434662436,2.61861639071006,3.85250641698236));
#45646=CARTESIAN_POINT('Ctrl Pts',(1.25778845619858,2.66121527822096,3.85754732976625));
#45647=CARTESIAN_POINT('Ctrl Pts',(1.17256689933829,2.69984839441936,3.86258824255015));
#45648=CARTESIAN_POINT('Ctrl Pts',(1.08572534462498,2.73433071811713,3.86762915533404));
#45649=CARTESIAN_POINT('Ctrl Pts',(0.998864445541836,2.76882072291671,3.87267119100526));
#45650=CARTESIAN_POINT('Ctrl Pts',(0.910383243580881,2.79915793569936,3.87771322667648));
#45651=CARTESIAN_POINT('Ctrl Pts',(0.820715587876747,2.82520617368293,3.8827552623477));
#45652=CARTESIAN_POINT('Ctrl Pts',(0.73095025654504,2.85128278620102,3.88780279034494));
#45653=CARTESIAN_POINT('Ctrl Pts',(0.639996317987379,2.87306097605417,3.89285031834218));
#45654=CARTESIAN_POINT('Ctrl Pts',(0.548300598314234,2.8904550600015,3.89789784633942));
#45655=CARTESIAN_POINT('Ctrl Pts',(0.456546582545437,2.90786020234048,3.90294858333241));
#45656=CARTESIAN_POINT('Ctrl Pts',(0.364050284881002,2.92087562833285,3.9079993203254));
#45657=CARTESIAN_POINT('Ctrl Pts',(0.271264367783776,2.92946746743685,3.91305005731839));
#45658=CARTESIAN_POINT('Ctrl Pts',(0.178335803837062,2.93807251542877,3.91810855919362));
#45659=CARTESIAN_POINT('Ctrl Pts',(0.0851171732932596,2.94224038400668,
3.92316706106885));
#45660=CARTESIAN_POINT('Ctrl Pts',(-0.00793844137284537,2.94198928977462,
3.92822556294408));
#45661=CARTESIAN_POINT('Ctrl Pts',(-0.0395629826910187,2.94190395650435,
3.92994467255541));
#45662=CARTESIAN_POINT('Ctrl Pts',(-0.0711687407238937,2.94130869726534,
3.93166378216675));
#45663=CARTESIAN_POINT('Ctrl Pts',(-0.10273811524122,2.94020558459382,3.93338289177808));
#45664=CARTESIAN_POINT('Ctrl Pts',(-0.195633404254339,2.93695959153877,
3.93844150274621));
#45665=CARTESIAN_POINT('Ctrl Pts',(-0.288536322850242,2.92930112879298,
3.94350011371434));
#45666=CARTESIAN_POINT('Ctrl Pts',(-0.380994436567301,2.91722594930608,
3.94855872468246));
#45667=CARTESIAN_POINT('Ctrl Pts',(-0.47332757217121,2.9051670921633,3.95361049779041));
#45668=CARTESIAN_POINT('Ctrl Pts',(-0.565216662209034,2.88870343982036,
3.95866227089836));
#45669=CARTESIAN_POINT('Ctrl Pts',(-0.656210818995895,2.86788273139484,
3.96371404400631));
#45670=CARTESIAN_POINT('Ctrl Pts',(-0.751529140190257,2.84607259497206,
3.96900588414976));
#45671=CARTESIAN_POINT('Ctrl Pts',(-0.845864871754567,2.81948104272493,
3.97429772429322));
#45672=CARTESIAN_POINT('Ctrl Pts',(-0.938707334299334,2.78822390430407,
3.97958956443667));
#45673=CARTESIAN_POINT('Ctrl Pts',(-1.02718169041233,2.75843736999724,3.98463243099269));
#45674=CARTESIAN_POINT('Ctrl Pts',(-1.11429963138459,2.72441447358109,3.9896752975487));
#45675=CARTESIAN_POINT('Ctrl Pts',(-1.19963260938906,2.68630705662819,3.99471816410471));
#45676=CARTESIAN_POINT('Ctrl Pts',(-1.28493720959873,2.64821231243656,3.99975935363696));
#45677=CARTESIAN_POINT('Ctrl Pts',(-1.36845762219716,2.60603592702048,4.00480054316921));
#45678=CARTESIAN_POINT('Ctrl Pts',(-1.44978520169076,2.5599779039981,4.00984173270145));
#45679=CARTESIAN_POINT('Ctrl Pts',(-1.53110831657547,2.5139224094053,4.01488264548945));
#45680=CARTESIAN_POINT('Ctrl Pts',(-1.61023845257691,2.4639859196289,4.01992355827746));
#45681=CARTESIAN_POINT('Ctrl Pts',(-1.68679250191346,2.41041387638898,4.02496447106546));
#45682=CARTESIAN_POINT('Ctrl Pts',(-1.76336360402821,2.3568298997219,4.03000650674073));
#45683=CARTESIAN_POINT('Ctrl Pts',(-1.8373571171338,2.29960901531408,4.03504854241601));
#45684=CARTESIAN_POINT('Ctrl Pts',(-1.90842072792448,2.2390387056119,4.04009057809128));
#45685=CARTESIAN_POINT('Ctrl Pts',(-1.97956174882022,2.1784024162334,4.04513810609247));
#45686=CARTESIAN_POINT('Ctrl Pts',(-2.04776616034983,2.11440970762616,4.05018563409367));
#45687=CARTESIAN_POINT('Ctrl Pts',(-2.11271669250956,2.04738667017041,4.05523316209486));
#45688=CARTESIAN_POINT('Ctrl Pts',(-2.17770851735284,1.98032102242365,4.06028389909172));
#45689=CARTESIAN_POINT('Ctrl Pts',(-2.23944205214108,1.91022154244694,4.06533463608858));
#45690=CARTESIAN_POINT('Ctrl Pts',(-2.29764009351157,1.8374476865174,4.07038537308545));
#45691=CARTESIAN_POINT('Ctrl Pts',(-2.35592760715734,1.76456194980429,4.07544387496443));
#45692=CARTESIAN_POINT('Ctrl Pts',(-2.41066852027046,1.68899398929134,4.08050237684342));
#45693=CARTESIAN_POINT('Ctrl Pts',(-2.46162890373495,1.61113225412958,4.0855608787224));
#45694=CARTESIAN_POINT('Ctrl Pts',(-2.47894756552178,1.58467128649691,4.087279988298));
#45695=CARTESIAN_POINT('Ctrl Pts',(-2.4958299886724,1.55794560555479,4.08899909787361));
#45696=CARTESIAN_POINT('Ctrl Pts',(-2.51226822610567,1.5309710513592,4.09071820744921));
#45697=CARTESIAN_POINT('Ctrl Pts',(-2.56203265636791,1.44930941783119,4.0959225676451));
#45698=CARTESIAN_POINT('Ctrl Pts',(-2.60788739691094,1.36509504662174,4.10112692784099));
#45699=CARTESIAN_POINT('Ctrl Pts',(-2.64957065136526,1.27872567950435,4.10633128803687));
#45700=CARTESIAN_POINT('Ctrl Pts',(-2.691186862575,1.19249522866591,4.11152727755254));
#45701=CARTESIAN_POINT('Ctrl Pts',(-2.72864475943488,1.10411704200888,4.11672326706821));
#45702=CARTESIAN_POINT('Ctrl Pts',(-2.76172698456252,1.01401580990595,4.12191925658388));
#45703=CARTESIAN_POINT('Ctrl Pts',(-2.79474985883382,0.924076223075112,
4.1271059242832));
#45704=CARTESIAN_POINT('Ctrl Pts',(-2.82341255694188,0.832420128498015,
4.13229259198251));
#45705=CARTESIAN_POINT('Ctrl Pts',(-2.84754514273931,0.739493515902438,
4.13747925968183));
#45706=CARTESIAN_POINT('Ctrl Pts',(-2.87165210534374,0.646665569755197,
4.14266042034644));
#45707=CARTESIAN_POINT('Ctrl Pts',(-2.89123842083447,0.552570181823066,
4.14784158101105));
#45708=CARTESIAN_POINT('Ctrl Pts',(-2.90618344854901,0.457669928419829,
4.15302274167566));
#45709=CARTESIAN_POINT('Ctrl Pts',(-2.92111279866343,0.36286922707175,4.1581984672105));
#45710=CARTESIAN_POINT('Ctrl Pts',(-2.93141049285336,0.267265743357151,
4.16337419274534));
#45711=CARTESIAN_POINT('Ctrl Pts',(-2.93700682387777,0.171332765387806,
4.16854991828018));
#45712=CARTESIAN_POINT('Ctrl Pts',(-2.94034936175837,0.114034579940489,
4.17164123982359));
#45713=CARTESIAN_POINT('Ctrl Pts',(-2.94201573484075,0.0566190577374391,
4.17473256136699));
#45714=CARTESIAN_POINT('Ctrl Pts',(-2.9419998880027,-0.000811783267522774,
4.1778238829104));
#45715=CARTESIAN_POINT('',(-2.94199963779692,-0.00145986396196984,5.17782388287747));
#45716=CARTESIAN_POINT('Ctrl Pts',(-2.9419998880025,-0.000811784004750149,
4.17782388295008));
#45717=CARTESIAN_POINT('Ctrl Pts',(-2.94197217039502,-0.10126362543284,
4.18323088963934));
#45718=CARTESIAN_POINT('Ctrl Pts',(-2.9367954789962,-0.20157521002038,4.1886378963286));
#45719=CARTESIAN_POINT('Ctrl Pts',(-2.92653799146242,-0.301229786918777,
4.19404490301786));
#45720=CARTESIAN_POINT('Ctrl Pts',(-2.91624122272408,-0.401265992535323,
4.19947261592148));
#45721=CARTESIAN_POINT('Ctrl Pts',(-2.90082476492119,-0.500639823046012,
4.20490032882511));
#45722=CARTESIAN_POINT('Ctrl Pts',(-2.88040829698104,-0.598842251918488,
4.21032804172873));
#45723=CARTESIAN_POINT('Ctrl Pts',(-2.85995051621559,-0.697243393898416,
4.21576673763664));
#45724=CARTESIAN_POINT('Ctrl Pts',(-2.83447260958186,-0.794468079685589,
4.22120543354456));
#45725=CARTESIAN_POINT('Ctrl Pts',(-2.80414401228342,-0.890022672955613,
4.22664412945247));
#45726=CARTESIAN_POINT('Ctrl Pts',(-2.77372602620075,-0.985858898403873,
4.23209885506364));
#45727=CARTESIAN_POINT('Ctrl Pts',(-2.73842887446513,-1.08001487435536,
4.23755358067482));
#45728=CARTESIAN_POINT('Ctrl Pts',(-2.69847051350961,-1.1720157369759,4.24300830628599));
#45729=CARTESIAN_POINT('Ctrl Pts',(-2.68615100624589,-1.20038039629173,
4.24469004523077));
#45730=CARTESIAN_POINT('Ctrl Pts',(-2.67338875796325,-1.22854038584006,
4.24637178417555));
#45731=CARTESIAN_POINT('Ctrl Pts',(-2.66019101498198,-1.25648229745156,
4.24805352312033));
#45732=CARTESIAN_POINT('Ctrl Pts',(-2.62049267319382,-1.34053057441395,
4.25311213409063));
#45733=CARTESIAN_POINT('Ctrl Pts',(-2.57673813346106,-1.42284184093946,
4.25817074506094));
#45734=CARTESIAN_POINT('Ctrl Pts',(-2.52910231826078,-1.5029988236083,4.26322935603124));
#45735=CARTESIAN_POINT('Ctrl Pts',(-2.4815308936694,-1.58304745593404,4.26828112914144));
#45736=CARTESIAN_POINT('Ctrl Pts',(-2.43008884431785,-1.66094721385083,
4.27333290225164));
#45737=CARTESIAN_POINT('Ctrl Pts',(-2.37499823449402,-1.73630279218524,
4.27838467536184));
#45738=CARTESIAN_POINT('Ctrl Pts',(-2.31728964501402,-1.81523936865509,
4.28367651550474));
#45739=CARTESIAN_POINT('Ctrl Pts',(-2.25557733499436,-1.89138351938762,
4.28896835564764));
#45740=CARTESIAN_POINT('Ctrl Pts',(-2.19016954749073,-1.96431192870284,
4.29426019579054));
#45741=CARTESIAN_POINT('Ctrl Pts',(-2.12783910375923,-2.03380915964032,
4.29930306234897));
#45742=CARTESIAN_POINT('Ctrl Pts',(-2.06215336565251,-2.10038600949863,
4.30434592890741));
#45743=CARTESIAN_POINT('Ctrl Pts',(-1.99342119354542,-2.16370884019176,
4.30938879546584));
#45744=CARTESIAN_POINT('Ctrl Pts',(-1.92471187857332,-2.22701061264614,
4.31442998500057));
#45745=CARTESIAN_POINT('Ctrl Pts',(-1.85295846800584,-2.2870602161998,4.3194711745353));
#45746=CARTESIAN_POINT('Ctrl Pts',(-1.77850619629435,-2.34356133048457,
4.32451236407003));
#45747=CARTESIAN_POINT('Ctrl Pts',(-1.70405801175985,-2.40005934304996,
4.32955327686057));
#45748=CARTESIAN_POINT('Ctrl Pts',(-1.62691161381304,-2.45300898635414,
4.33459418965111));
#45749=CARTESIAN_POINT('Ctrl Pts',(-1.54744388146588,-2.50215535762946,
4.33963510244165));
#45750=CARTESIAN_POINT('Ctrl Pts',(-1.46795844730319,-2.55131267649284,
4.3446771381195));
#45751=CARTESIAN_POINT('Ctrl Pts',(-1.38615102853373,-2.59666480803702,
4.34971917379735));
#45752=CARTESIAN_POINT('Ctrl Pts',(-1.30242495026298,-2.63800175301922,
4.35476120947519));
#45753=CARTESIAN_POINT('Ctrl Pts',(-1.21860766856898,-2.67938372663487,
4.35980873747901));
#45754=CARTESIAN_POINT('Ctrl Pts',(-1.1328679538705,-2.71674158842498,4.36485626548283));
#45755=CARTESIAN_POINT('Ctrl Pts',(-1.0456307447518,-2.74991278873163,4.36990379348665));
#45756=CARTESIAN_POINT('Ctrl Pts',(-0.958338074062372,-2.78310507782472,
4.37495453048619));
#45757=CARTESIAN_POINT('Ctrl Pts',(-0.869546434149082,-2.81210526918745,
4.38000526748574));
#45758=CARTESIAN_POINT('Ctrl Pts',(-0.779695576409692,-2.83680080515484,
4.38505600448528));
#45759=CARTESIAN_POINT('Ctrl Pts',(-0.689706584112763,-2.86153430744798,
4.39011450636697));
#45760=CARTESIAN_POINT('Ctrl Pts',(-0.598655555219479,-2.8819498497887,
4.39517300824865));
#45761=CARTESIAN_POINT('Ctrl Pts',(-0.506991769194499,-2.89798608450231,
4.40023151013034));
#45762=CARTESIAN_POINT('Ctrl Pts',(-0.4758402358018,-2.90343592814109,4.40195061968405));
#45763=CARTESIAN_POINT('Ctrl Pts',(-0.44461796584669,-2.90838042674006,
4.40366972923775));
#45764=CARTESIAN_POINT('Ctrl Pts',(-0.413342650666822,-2.91281854105945,
4.40538883879146));
#45765=CARTESIAN_POINT('Ctrl Pts',(-0.321312650505731,-2.92587803092167,
4.41044744976291));
#45766=CARTESIAN_POINT('Ctrl Pts',(-0.228503016871154,-2.93459446671002,
4.41550606073436));
#45767=CARTESIAN_POINT('Ctrl Pts',(-0.135358460381505,-2.93888449708442,
4.42056467170581));
#45768=CARTESIAN_POINT('Ctrl Pts',(-0.0423398098866227,-2.94316872850973,
4.42561644481716));
#45769=CARTESIAN_POINT('Ctrl Pts',(0.0510124249545995,-2.94303842499226,
4.43066821792851));
#45770=CARTESIAN_POINT('Ctrl Pts',(0.144245959569578,-2.93846168992346,
4.43571999103986));
#45771=CARTESIAN_POINT('Ctrl Pts',(0.241910076749521,-2.93366746226807,
4.44101183118247));
#45772=CARTESIAN_POINT('Ctrl Pts',(0.339443446913503,-2.92399365216437,
4.44630367132509));
#45773=CARTESIAN_POINT('Ctrl Pts',(0.436323001411083,-2.90946494023207,
4.4515955114677));
#45774=CARTESIAN_POINT('Ctrl Pts',(0.528644510095479,-2.89561978361686,
4.45663837802728));
#45775=CARTESIAN_POINT('Ctrl Pts',(0.620371837137919,-2.87736627422707,
4.46168124458686));
#45776=CARTESIAN_POINT('Ctrl Pts',(0.711056476639062,-2.85477892086754,
4.46672411114644));
#45777=CARTESIAN_POINT('Ctrl Pts',(0.801710958631962,-2.83219907901491,
4.47176530068231));
#45778=CARTESIAN_POINT('Ctrl Pts',(0.891323012636902,-2.80528836375621,
4.47680649021819));
#45779=CARTESIAN_POINT('Ctrl Pts',(0.979455300315797,-2.77417218547863,
4.48184767975407));
#45780=CARTESIAN_POINT('Ctrl Pts',(1.06758274983116,-2.74305771537365,4.48688859254574));
#45781=CARTESIAN_POINT('Ctrl Pts',(1.15423017707609,-2.70773838925117,4.49192950533742));
#45782=CARTESIAN_POINT('Ctrl Pts',(1.238977436356,-2.66838882327908,4.4969704181291));
#45783=CARTESIAN_POINT('Ctrl Pts',(1.32374357349118,-2.62903049200392,4.50201245380809));
#45784=CARTESIAN_POINT('Ctrl Pts',(1.40660830047679,-2.58564032460755,4.50705448948708));
#45785=CARTESIAN_POINT('Ctrl Pts',(1.48717443441246,-2.53843971794289,4.51209652516606));
#45786=CARTESIAN_POINT('Ctrl Pts',(1.56782832962084,-2.49118769531582,4.51714405317101));
#45787=CARTESIAN_POINT('Ctrl Pts',(1.64617825205445,-2.44011717375445,4.52219158117595));
#45788=CARTESIAN_POINT('Ctrl Pts',(1.72185476556907,-2.38549369445553,4.52723910918089));
#45789=CARTESIAN_POINT('Ctrl Pts',(1.79757939087379,-2.33083548795726,4.53228984618155));
#45790=CARTESIAN_POINT('Ctrl Pts',(1.87062687767098,-2.2726201025847,4.53734058318221));
#45791=CARTESIAN_POINT('Ctrl Pts',(1.94066139969039,-2.2111529417369,4.54239132018287));
#45792=CARTESIAN_POINT('Ctrl Pts',(2.01080359110695,-2.14959128274786,4.54744982206565));
#45793=CARTESIAN_POINT('Ctrl Pts',(2.07792325526939,-2.08476817792938,4.55250832394844));
#45794=CARTESIAN_POINT('Ctrl Pts',(2.14172209911554,-2.01702514861867,4.55756682583122));
#45795=CARTESIAN_POINT('Ctrl Pts',(2.16340385467871,-1.99400297902942,4.55928593537501));
#45796=CARTESIAN_POINT('Ctrl Pts',(2.18470242359527,-1.97064384466696,4.56100504491879));
#45797=CARTESIAN_POINT('Ctrl Pts',(2.20560720960889,-1.94696195055817,4.56272415446258));
#45798=CARTESIAN_POINT('Ctrl Pts',(2.26712113714525,-1.87727617060409,4.56778276543495));
#45799=CARTESIAN_POINT('Ctrl Pts',(2.32543628793261,-1.80455101993097,4.57284137640732));
#45800=CARTESIAN_POINT('Ctrl Pts',(2.38023850294436,-1.72911210426079,4.57789998737968));
#45801=CARTESIAN_POINT('Ctrl Pts',(2.43496664033275,-1.65377516139557,4.58295176049197));
#45802=CARTESIAN_POINT('Ctrl Pts',(2.48619102059477,-1.57573209892987,4.58800353360426));
#45803=CARTESIAN_POINT('Ctrl Pts',(2.53363629687119,-1.4953431429531,4.59305530671655));
#45804=CARTESIAN_POINT('Ctrl Pts',(2.58333623627569,-1.41113399602856,4.59834714685893));
#45805=CARTESIAN_POINT('Ctrl Pts',(2.62888866287606,-1.32435083333337,4.60363898700131));
#45806=CARTESIAN_POINT('Ctrl Pts',(2.67002656204015,-1.23544411366927,4.60893082714369));
#45807=CARTESIAN_POINT('Ctrl Pts',(2.70922898132806,-1.15072032921247,4.61397369370425));
#45808=CARTESIAN_POINT('Ctrl Pts',(2.74442264027815,-1.06406873081819,4.61901656026481));
#45809=CARTESIAN_POINT('Ctrl Pts',(2.77542314380754,-0.975904899474069,
4.62405942682536));
#45810=CARTESIAN_POINT('Ctrl Pts',(2.80641333800627,-0.887770387333999,
4.62910061636223));
#45811=CARTESIAN_POINT('Ctrl Pts',(2.83321300063944,-0.79812505893049,4.6341418058991));
#45812=CARTESIAN_POINT('Ctrl Pts',(2.85568639250246,-0.707403157807695,
4.63918299543597));
#45813=CARTESIAN_POINT('Ctrl Pts',(2.87815855065257,-0.616686237009219,
4.64422390822865));
#45814=CARTESIAN_POINT('Ctrl Pts',(2.89630480428302,-0.52489329104853,4.64926482102133));
#45815=CARTESIAN_POINT('Ctrl Pts',(2.91003996678476,-0.432471261143845,
4.65430573381401));
#45816=CARTESIAN_POINT('Ctrl Pts',(2.92377818885934,-0.340028643792029,
4.65934776949402));
#45817=CARTESIAN_POINT('Ctrl Pts',(2.93310330347559,-0.246957102247369,
4.66438980517402));
#45818=CARTESIAN_POINT('Ctrl Pts',(2.937981824019,-0.153710122418809,4.66943184085402));
#45819=CARTESIAN_POINT('Ctrl Pts',(2.94286565877014,-0.0603615679801721,
4.67447936885999));
#45820=CARTESIAN_POINT('Ctrl Pts',(2.94329320945978,0.0331623632958987,
4.67952689686595));
#45821=CARTESIAN_POINT('Ctrl Pts',(2.93928311813365,0.126407086251162,4.68457442487192));
#45822=CARTESIAN_POINT('Ctrl Pts',(2.93527047736829,0.219711090089497,4.68962516187361));
#45823=CARTESIAN_POINT('Ctrl Pts',(2.92681461807625,0.312735091659688,4.6946758988753));
#45824=CARTESIAN_POINT('Ctrl Pts',(2.91398595840712,0.405030658353332,4.69972663587699));
#45825=CARTESIAN_POINT('Ctrl Pts',(2.9011375762638,0.497468118041193,4.70478513776081));
#45826=CARTESIAN_POINT('Ctrl Pts',(2.88390305840322,0.589174473506708,4.70984363964463));
#45827=CARTESIAN_POINT('Ctrl Pts',(2.86240362911597,0.679712780535806,4.71490214152845));
#45828=CARTESIAN_POINT('Ctrl Pts',(2.85509714297926,0.710481824509529,4.71662125106353));
#45829=CARTESIAN_POINT('Ctrl Pts',(2.84729850129208,0.741116108795763,4.71834036059862));
#45830=CARTESIAN_POINT('Ctrl Pts',(2.83901374189667,0.771598971825321,4.72005947013371));
#45831=CARTESIAN_POINT('Ctrl Pts',(2.81463520526548,0.861297122069784,4.72511808110523));
#45832=CARTESIAN_POINT('Ctrl Pts',(2.78595910130138,0.949994841375823,4.73017669207676));
#45833=CARTESIAN_POINT('Ctrl Pts',(2.75308463646161,1.03725068545604,4.73523530304829));
#45834=CARTESIAN_POINT('Ctrl Pts',(2.72025460891749,1.12438858347209,4.74028707615972));
#45835=CARTESIAN_POINT('Ctrl Pts',(2.683237653453,1.21008806851943,4.74533884927116));
#45836=CARTESIAN_POINT('Ctrl Pts',(2.64218323512074,1.29392107643663,4.75039062238259));
#45837=CARTESIAN_POINT('Ctrl Pts',(2.59917785578772,1.38173794128485,4.75568246252518));
#45838=CARTESIAN_POINT('Ctrl Pts',(2.55174189366301,1.46750606120558,4.76097430266778));
#45839=CARTESIAN_POINT('Ctrl Pts',(2.50010476144967,1.55075471360776,4.76626614281037));
#45840=CARTESIAN_POINT('Ctrl Pts',(2.4508970831639,1.63008663483463,4.77130900937005));
#45841=CARTESIAN_POINT('Ctrl Pts',(2.39787485317142,1.70713036435466,4.77635187592973));
#45842=CARTESIAN_POINT('Ctrl Pts',(2.34128378431755,1.78150336550109,4.78139474248941));
#45843=CARTESIAN_POINT('Ctrl Pts',(2.28471153503033,1.85585163363432,4.7864359320254));
#45844=CARTESIAN_POINT('Ctrl Pts',(2.22457307297802,1.92753058592167,4.79147712156138));
#45845=CARTESIAN_POINT('Ctrl Pts',(2.16115645395047,1.99618806267051,4.79651831109737));
#45846=CARTESIAN_POINT('Ctrl Pts',(2.09774331628004,2.06484177035692,4.80155922388916));
#45847=CARTESIAN_POINT('Ctrl Pts',(2.03105268037183,2.13047400731676,4.80660013668095));
#45848=CARTESIAN_POINT('Ctrl Pts',(1.96141100583973,2.19276785505689,4.81164104947274));
#45849=CARTESIAN_POINT('Ctrl Pts',(1.89175381829319,2.25507557904807,4.81668308515185));
#45850=CARTESIAN_POINT('Ctrl Pts',(1.81914461679895,2.31404314185766,4.82172512083095));
#45851=CARTESIAN_POINT('Ctrl Pts',(1.74394375652461,2.36939320799204,4.82676715651006));
#45852=CARTESIAN_POINT('Ctrl Pts',(1.66866097940884,2.42480356735412,4.83181468451513));
#45853=CARTESIAN_POINT('Ctrl Pts',(1.59078126643307,2.47658830279768,4.83686221252019));
#45854=CARTESIAN_POINT('Ctrl Pts',(1.51069455579244,2.52451301424633,4.84190974052526));
#45855=CARTESIAN_POINT('Ctrl Pts',(1.43055692955278,2.57246819411318,4.84696047752605));
#45856=CARTESIAN_POINT('Ctrl Pts',(1.348209902331,2.61655825568513,4.85201121452685));
#45857=CARTESIAN_POINT('Ctrl Pts',(1.26406674449931,2.65659542750697,4.85706195152764));
#45858=CARTESIAN_POINT('Ctrl Pts',(1.17979422699146,2.69669415151812,4.86212045341056));
#45859=CARTESIAN_POINT('Ctrl Pts',(1.09372047547981,2.73272737974587,4.86717895529349));
#45860=CARTESIAN_POINT('Ctrl Pts',(1.00627710243888,2.764556093319,4.87223745717641));
#45861=CARTESIAN_POINT('Ctrl Pts',(0.976559857980167,2.7753729411734,4.87395656671921));
#45862=CARTESIAN_POINT('Ctrl Pts',(0.946684539921142,2.7857046189537,4.87567567626202));
#45863=CARTESIAN_POINT('Ctrl Pts',(0.916668384784554,2.7955470077136,4.87739478580483));
#45864=CARTESIAN_POINT('Ctrl Pts',(0.82834355851648,2.82450898746502,4.88245339677659));
#45865=CARTESIAN_POINT('Ctrl Pts',(0.738491153007888,2.84933134782435,4.88751200774835));
#45866=CARTESIAN_POINT('Ctrl Pts',(0.647534432040966,2.86985420523785,4.89257061872011));
#45867=CARTESIAN_POINT('Ctrl Pts',(0.556700659712732,2.89034932135467,4.89762239183178));
#45868=CARTESIAN_POINT('Ctrl Pts',(0.464765966952342,2.90655638762517,4.90267416494344));
#45869=CARTESIAN_POINT('Ctrl Pts',(0.37217007850815,2.91836485598755,4.90772593805511));
#45870=CARTESIAN_POINT('Ctrl Pts',(0.275173909307494,2.93073447859739,4.91301777819765));
#45871=CARTESIAN_POINT('Ctrl Pts',(0.177452609881884,2.93827692751991,4.91830961834018));
#45872=CARTESIAN_POINT('Ctrl Pts',(0.0795254971590513,2.94092497274269,
4.92360145848272));
#45873=CARTESIAN_POINT('Ctrl Pts',(-0.0137942836275936,2.9434484311888,
4.92864432504264));
#45874=CARTESIAN_POINT('Ctrl Pts',(-0.107300451681992,2.94152758026219,
4.93368719160255));
#45875=CARTESIAN_POINT('Ctrl Pts',(-0.200538383141079,2.93515729678788,
4.93873005816247));
#45876=CARTESIAN_POINT('Ctrl Pts',(-0.293745307985457,2.92878913177462,
4.94377124769869));
#45877=CARTESIAN_POINT('Ctrl Pts',(-0.386683731975325,2.91797450436237,
4.94881243723492));
#45878=CARTESIAN_POINT('Ctrl Pts',(-0.478901119425166,2.90276036176143,
4.95385362677114));
#45879=CARTESIAN_POINT('Ctrl Pts',(-0.57111344445348,2.88754705436527,4.95889453956317));
#45880=CARTESIAN_POINT('Ctrl Pts',(-0.66260437472947,2.86793478462953,4.9639354523552));
#45881=CARTESIAN_POINT('Ctrl Pts',(-0.752929691607653,2.84402195481955,
4.96897636514722));
#45882=CARTESIAN_POINT('Ctrl Pts',(-0.843275128880084,2.82010379831291,
4.97401840082657));
#45883=CARTESIAN_POINT('Ctrl Pts',(-0.932454009061602,2.79188329272425,
4.97906043650592));
#45884=CARTESIAN_POINT('Ctrl Pts',(-1.02003653602754,2.75950891739254,4.98410247218527));
#45885=CARTESIAN_POINT('Ctrl Pts',(-1.10771446727399,2.72709927641946,4.98915000019057));
#45886=CARTESIAN_POINT('Ctrl Pts',(-1.19379215891537,2.69052688901294,4.99419752819588));
#45887=CARTESIAN_POINT('Ctrl Pts',(-1.27785940882091,2.64998855304846,4.99924505620118));
#45888=CARTESIAN_POINT('Ctrl Pts',(-1.36198010497682,2.6094244445976,5.00429579320221));
#45889=CARTESIAN_POINT('Ctrl Pts',(-1.44408742599362,2.5648895789537,5.00934653020324));
#45890=CARTESIAN_POINT('Ctrl Pts',(-1.52379728570548,2.51662588242206,5.01439726720427));
#45891=CARTESIAN_POINT('Ctrl Pts',(-1.603629689447,2.46828798643905,5.01945576908742));
#45892=CARTESIAN_POINT('Ctrl Pts',(-1.6810569091271,2.41621006511714,5.02451427097058));
#45893=CARTESIAN_POINT('Ctrl Pts',(-1.75572549254014,2.36067617322764,5.02957277285373));
#45894=CARTESIAN_POINT('Ctrl Pts',(-1.78110128108464,2.34180322515193,5.03129188239447));
#45895=CARTESIAN_POINT('Ctrl Pts',(-1.80615875942737,2.32253145897469,5.03301099193521));
#45896=CARTESIAN_POINT('Ctrl Pts',(-1.83088500911839,2.30287300635219,5.03473010147595));
#45897=CARTESIAN_POINT('Ctrl Pts',(-1.90280242283027,2.24569550924469,5.03973020919962));
#45898=CARTESIAN_POINT('Ctrl Pts',(-1.97217831547442,2.18503475459089,5.04473031692329));
#45899=CARTESIAN_POINT('Ctrl Pts',(-2.03865087933601,2.12114747063529,5.04973042464695));
#45900=CARTESIAN_POINT('Ctrl Pts',(-2.10503315455134,2.05734696378061,5.05472374080232));
#45901=CARTESIAN_POINT('Ctrl Pts',(-2.16851960902195,1.99032894428582,5.05971705695769));
#45902=CARTESIAN_POINT('Ctrl Pts',(-2.22878016815274,1.92039135648155,5.06471037311306));
#45903=CARTESIAN_POINT('Ctrl Pts',(-2.28897401414869,1.85053119503695,5.06969816127833));
#45904=CARTESIAN_POINT('Ctrl Pts',(-2.34594876853345,1.777758232264,5.0746859494436));
#45905=CARTESIAN_POINT('Ctrl Pts',(-2.39941098219119,1.70240739499695,5.07967373760888));
#45906=CARTESIAN_POINT('Ctrl Pts',(-2.45284117464076,1.62710168913545,5.084658538337));
#45907=CARTESIAN_POINT('Ctrl Pts',(-2.50276274098691,1.54922154370341,5.08964333906513));
#45908=CARTESIAN_POINT('Ctrl Pts',(-2.54892297361249,1.46913432830032,5.09462813979326));
#45909=CARTESIAN_POINT('Ctrl Pts',(-2.59506912288116,1.38907154728101,5.09961141967272));
#45910=CARTESIAN_POINT('Ctrl Pts',(-2.63745599128222,1.30680342723575,5.10459469955219));
#45911=CARTESIAN_POINT('Ctrl Pts',(-2.67587531393081,1.22272454146291,5.10957797943166));
#45912=CARTESIAN_POINT('Ctrl Pts',(-2.71429420418152,1.13864660197256,5.11456120322581));
#45913=CARTESIAN_POINT('Ctrl Pts',(-2.74874545046826,1.05275835133024,5.11954442701997));
#45914=CARTESIAN_POINT('Ctrl Pts',(-2.77906824043815,0.965475900780554,
5.12452765081413));
#45915=CARTESIAN_POINT('Ctrl Pts',(-2.80941650208858,0.878120131426771,
5.12951506060451));
#45916=CARTESIAN_POINT('Ctrl Pts',(-2.83562923411632,0.789368253785789,
5.1345024703949));
#45917=CARTESIAN_POINT('Ctrl Pts',(-2.85759517427401,0.699652642363268,
5.13948988018529));
#45918=CARTESIAN_POINT('Ctrl Pts',(-2.87957120535488,0.609895816527108,
5.14447958113958));
#45919=CARTESIAN_POINT('Ctrl Pts',(-2.89729647349492,0.519174821433264,
5.14946928209386));
#45920=CARTESIAN_POINT('Ctrl Pts',(-2.91071106298119,0.427931195215936,
5.15445898304815));
#45921=CARTESIAN_POINT('Ctrl Pts',(-2.924145156996,0.336554902701618,5.15945593892178));
#45922=CARTESIAN_POINT('Ctrl Pts',(-2.9332560154029,0.244654913917933,5.16445289479541));
#45923=CARTESIAN_POINT('Ctrl Pts',(-2.93803572033691,0.152676475019436,
5.16944985066904));
#45924=CARTESIAN_POINT('Ctrl Pts',(-2.94070570609601,0.101296499604001,
5.17224119473852));
#45925=CARTESIAN_POINT('Ctrl Pts',(-2.94202511937368,0.0498920369940975,
5.17503253880799));
#45926=CARTESIAN_POINT('Ctrl Pts',(-2.94199963779692,-0.00145986396196948,
5.17782388287747));
#45927=CARTESIAN_POINT('',(-2.94199890533048,0.00253791927304355,6.17782385433891));
#45928=CARTESIAN_POINT('Ctrl Pts',(-2.94199963779662,-0.00145986456779249,
5.1778238829104));
#45929=CARTESIAN_POINT('Ctrl Pts',(-2.9419563018159,-0.0887929243620846,
5.18257106098929));
#45930=CARTESIAN_POINT('Ctrl Pts',(-2.93802453262175,-0.176025039555883,
5.18731823906819));
#45931=CARTESIAN_POINT('Ctrl Pts',(-2.93022946613174,-0.262905450330198,
5.19206541714709));
#45932=CARTESIAN_POINT('Ctrl Pts',(-2.92192301370534,-0.355485545677367,
5.19712402811885));
#45933=CARTESIAN_POINT('Ctrl Pts',(-2.90921023997664,-0.447832661136409,
5.20218263909061));
#45934=CARTESIAN_POINT('Ctrl Pts',(-2.89211157404499,-0.539494803751654,
5.20724125006237));
#45935=CARTESIAN_POINT('Ctrl Pts',(-2.87503602083856,-0.631033044190861,
5.21229302317404));
#45936=CARTESIAN_POINT('Ctrl Pts',(-2.85358643783142,-0.721887720013586,
5.2173447962857));
#45937=CARTESIAN_POINT('Ctrl Pts',(-2.82783507861033,-0.811611217382376,
5.22239656939736));
#45938=CARTESIAN_POINT('Ctrl Pts',(-2.80085998027575,-0.905598495633074,
5.2276884095399));
#45939=CARTESIAN_POINT('Ctrl Pts',(-2.76916415693882,-0.998343930454374,
5.23298024968244));
#45940=CARTESIAN_POINT('Ctrl Pts',(-2.73289111167492,-1.08934391802048,
5.23827208982498));
#45941=CARTESIAN_POINT('Ctrl Pts',(-2.69832466180862,-1.17606248507637,
5.24331495638489));
#45942=CARTESIAN_POINT('Ctrl Pts',(-2.65960211330447,-1.26119565939655,
5.2483578229448));
#45943=CARTESIAN_POINT('Ctrl Pts',(-2.61689844920908,-1.34432381014661,
5.25340068950471));
#45944=CARTESIAN_POINT('Ctrl Pts',(-2.57420898637316,-1.42742431632652,
5.25844187904093));
#45945=CARTESIAN_POINT('Ctrl Pts',(-2.52754124069688,-1.50852073013917,
5.26348306857715));
#45946=CARTESIAN_POINT('Ctrl Pts',(-2.47711720041013,-1.58721591960019,
5.26852425811337));
#45947=CARTESIAN_POINT('Ctrl Pts',(-2.42669592823206,-1.66590678896239,
5.27356517090539));
#45948=CARTESIAN_POINT('Ctrl Pts',(-2.37251901085926,-1.74219632344063,
5.27860608369741));
#45949=CARTESIAN_POINT('Ctrl Pts',(-2.31485241453424,-1.81571536836725,
5.28364699648943));
#45950=CARTESIAN_POINT('Ctrl Pts',(-2.25717297270046,-1.88925079001099,
5.28868903216876));
#45951=CARTESIAN_POINT('Ctrl Pts',(-2.19600258157004,-1.96001414814933,
5.29373106784809));
#45952=CARTESIAN_POINT('Ctrl Pts',(-2.13164750644185,-2.02766932912649,
5.29877310352742));
#45953=CARTESIAN_POINT('Ctrl Pts',(-2.06722232886441,-2.09539820738208,
5.30382063153272));
#45954=CARTESIAN_POINT('Ctrl Pts',(-1.99960584947404,-2.16001183004599,
5.30886815953802));
#45955=CARTESIAN_POINT('Ctrl Pts',(-1.92914097326535,-2.22121117980007,
5.31391568754332));
#45956=CARTESIAN_POINT('Ctrl Pts',(-1.85863129859563,-2.28244943740203,
5.31896642454435));
#45957=CARTESIAN_POINT('Ctrl Pts',(-1.78526996943886,-2.34026882694231,
5.32401716154537));
#45958=CARTESIAN_POINT('Ctrl Pts',(-1.70943102234009,-2.39441215747443,
5.3290678985464));
#45959=CARTESIAN_POINT('Ctrl Pts',(-1.63347548226001,-2.44863872666643,
5.33412640042955));
#45960=CARTESIAN_POINT('Ctrl Pts',(-1.55503509370221,-2.49917771834094,
5.3391849023127));
#45961=CARTESIAN_POINT('Ctrl Pts',(-1.47451048334426,-2.54581673230967,
5.34424340419586));
#45962=CARTESIAN_POINT('Ctrl Pts',(-1.44714454988593,-2.56166679537929,
5.34596251373663));
#45963=CARTESIAN_POINT('Ctrl Pts',(-1.41953808366408,-2.5770668348358,5.3476816232774));
#45964=CARTESIAN_POINT('Ctrl Pts',(-1.39170733449789,-2.59200977912985,
5.34940073281817));
#45965=CARTESIAN_POINT('Ctrl Pts',(-1.30981323191402,-2.63598053268787,
5.35445934378994));
#45966=CARTESIAN_POINT('Ctrl Pts',(-1.22569074274824,-2.67614284295641,
5.35951795476172));
#45967=CARTESIAN_POINT('Ctrl Pts',(-1.13972862276579,-2.71226522789502,
5.36457656573349));
#45968=CARTESIAN_POINT('Ctrl Pts',(-1.05388270008591,-2.74833878523732,
5.36962833884518));
#45969=CARTESIAN_POINT('Ctrl Pts',(-0.966202493368399,-2.78038309955491,
5.37468011195686));
#45970=CARTESIAN_POINT('Ctrl Pts',(-0.877101598400064,-2.80821238265272,
5.37973188506854));
#45971=CARTESIAN_POINT('Ctrl Pts',(-0.783766509451114,-2.83736415059222,
5.38502372521107));
#45972=CARTESIAN_POINT('Ctrl Pts',(-0.688872789287524,-2.86189011174939,
5.39031556535361));
#45973=CARTESIAN_POINT('Ctrl Pts',(-0.592919977901535,-2.88163320008034,
5.39560740549614));
#45974=CARTESIAN_POINT('Ctrl Pts',(-0.501481610370096,-2.90044740407222,
5.40065027205608));
#45975=CARTESIAN_POINT('Ctrl Pts',(-0.409082038246236,-2.91491848571425,
5.40569313861601));
#45976=CARTESIAN_POINT('Ctrl Pts',(-0.316167974458782,-2.92496184794377,
5.41073600517595));
#45977=CARTESIAN_POINT('Ctrl Pts',(-0.223284809582627,-2.93500187021649,
5.4157771947122));
#45978=CARTESIAN_POINT('Ctrl Pts',(-0.129887932960033,-2.94061705115688,
5.42081838424845));
#45979=CARTESIAN_POINT('Ctrl Pts',(-0.0364311131634972,-2.94177442608941,
5.42585957378469));
#45980=CARTESIAN_POINT('Ctrl Pts',(0.0570205761708374,-2.94293173748598,
5.43090048657674));
#45981=CARTESIAN_POINT('Ctrl Pts',(0.150531759252712,-2.93963172451159,
5.43594139936879));
#45982=CARTESIAN_POINT('Ctrl Pts',(0.243647852296875,-2.93189353900702,
5.44098231216084));
#45983=CARTESIAN_POINT('Ctrl Pts',(0.336784687393946,-2.9241536297848,5.44602434784021));
#45984=CARTESIAN_POINT('Ctrl Pts',(0.429525816372355,-2.91197362149412,
5.45106638351958));
#45985=CARTESIAN_POINT('Ctrl Pts',(0.521422092640471,-2.895424494147,5.45610841919894));
#45986=CARTESIAN_POINT('Ctrl Pts',(0.613418472187497,-2.87885733971568,
5.46115594720427));
#45987=CARTESIAN_POINT('Ctrl Pts',(0.704567725897267,-2.85791164643231,
5.4662034752096));
#45988=CARTESIAN_POINT('Ctrl Pts',(0.794431543773405,-2.83270939601255,
5.47125100321493));
#45989=CARTESIAN_POINT('Ctrl Pts',(0.884352493102186,-2.80749112311333,
5.47630174021598));
#45990=CARTESIAN_POINT('Ctrl Pts',(0.972985959899025,-2.77801104533038,
5.48135247721703));
#45991=CARTESIAN_POINT('Ctrl Pts',(1.05991145033037,-2.7444401464522,5.48640321421808));
#45992=CARTESIAN_POINT('Ctrl Pts',(1.14697057792937,-2.7108176364779,5.49146171610126));
#45993=CARTESIAN_POINT('Ctrl Pts',(1.23231608443701,-2.67309193230147,5.49652021798444));
#45994=CARTESIAN_POINT('Ctrl Pts',(1.31555026542164,-2.63148085669439,5.50157871986762));
#45995=CARTESIAN_POINT('Ctrl Pts',(1.34383703449613,-2.61733951628935,5.5032978294082));
#45996=CARTESIAN_POINT('Ctrl Pts',(1.37188019230894,-2.60274981128296,5.50501693894877));
#45997=CARTESIAN_POINT('Ctrl Pts',(1.39966489685727,-2.58772142559927,5.50673604848934));
#45998=CARTESIAN_POINT('Ctrl Pts',(1.48142350965003,-2.54349925422885,5.51179465946113));
#45999=CARTESIAN_POINT('Ctrl Pts',(1.5612265244099,-2.4953216330254,5.51685327043291));
#46000=CARTESIAN_POINT('Ctrl Pts',(1.63866682646632,-2.44338597684419,5.5219118814047));
#46001=CARTESIAN_POINT('Ctrl Pts',(1.71600245038998,-2.39152052348202,5.52696365451639));
#46002=CARTESIAN_POINT('Ctrl Pts',(1.7909813437599,-2.3359073750442,5.53201542762808));
#46003=CARTESIAN_POINT('Ctrl Pts',(1.86322089796477,-2.27678982020461,5.53706720073978));
#46004=CARTESIAN_POINT('Ctrl Pts',(1.9388933726321,-2.21486291990417,5.5423590408823));
#46005=CARTESIAN_POINT('Ctrl Pts',(2.01155926553294,-2.14909051759071,5.54765088102483));
#46006=CARTESIAN_POINT('Ctrl Pts',(2.08081269827853,-2.07980347982275,5.55294272116736));
#46007=CARTESIAN_POINT('Ctrl Pts',(2.14680785511398,-2.01377629903364,5.55798558772731));
#46008=CARTESIAN_POINT('Ctrl Pts',(2.2097040218404,-1.94455805473551,5.56302845428725));
#46009=CARTESIAN_POINT('Ctrl Pts',(2.26918489791011,-1.87247534005035,5.5680713208472));
#46010=CARTESIAN_POINT('Ctrl Pts',(2.3286459933972,-1.80041659673527,5.57311251038345));
#46011=CARTESIAN_POINT('Ctrl Pts',(2.38469377324528,-1.72549561707018,5.5781536999197));
#46012=CARTESIAN_POINT('Ctrl Pts',(2.43705118247127,-1.64807327932206,5.58319488945595));
#46013=CARTESIAN_POINT('Ctrl Pts',(2.48940571745324,-1.57065519179744,5.588235802248));
#46014=CARTESIAN_POINT('Ctrl Pts',(2.53807003696105,-1.49073638641421,5.59327671504006));
#46015=CARTESIAN_POINT('Ctrl Pts',(2.58281016747385,-1.40870708055072,5.59831762783212));
#46016=CARTESIAN_POINT('Ctrl Pts',(2.62756026406366,-1.32665950226891,5.6033596635115));
#46017=CARTESIAN_POINT('Ctrl Pts',(2.66838422376378,-1.2425008787025,5.60840169919087));
#46018=CARTESIAN_POINT('Ctrl Pts',(2.70509435179791,-1.1566453855314,5.61344373487025));
#46019=CARTESIAN_POINT('Ctrl Pts',(2.7418444684402,-1.07069636935017,5.61849126287558));
#46020=CARTESIAN_POINT('Ctrl Pts',(2.77447163567374,-0.983047202341485,
5.62353879088092));
#46021=CARTESIAN_POINT('Ctrl Pts',(2.80283671623168,-0.894131054232894,
5.62858631888626));
#46022=CARTESIAN_POINT('Ctrl Pts',(2.83121983005702,-0.805158377158289,
5.63363705588731));
#46023=CARTESIAN_POINT('Ctrl Pts',(2.85533534863092,-0.714917542795669,
5.63868779288837));
#46024=CARTESIAN_POINT('Ctrl Pts',(2.87509486000279,-0.623853785742722,
5.64373852988943));
#46025=CARTESIAN_POINT('Ctrl Pts',(2.89488474917432,-0.532650029450143,
5.64879703177262));
#46026=CARTESIAN_POINT('Ctrl Pts',(2.91030519268119,-0.44062126134618,5.65385553365581));
#46027=CARTESIAN_POINT('Ctrl Pts',(2.92131943191379,-0.348219437600584,
5.658914035539));
#46028=CARTESIAN_POINT('Ctrl Pts',(2.92506257250821,-0.316817085594656,
5.66063314507947));
#46029=CARTESIAN_POINT('Ctrl Pts',(2.92829726282772,-0.285371657139726,
5.66235225461995));
#46030=CARTESIAN_POINT('Ctrl Pts',(2.93102342983173,-0.253900873920183,
5.66407136416043));
#46031=CARTESIAN_POINT('Ctrl Pts',(2.93904538421723,-0.161295693426321,
5.6691299751322));
#46032=CARTESIAN_POINT('Ctrl Pts',(2.94268823470643,-0.0681488524178615,
5.67418858610397));
#46033=CARTESIAN_POINT('Ctrl Pts',(2.9418930026344,0.0250910551940078,5.67924719707574));
#46034=CARTESIAN_POINT('Ctrl Pts',(2.94109884549889,0.118204927922627,5.68429897018742));
#46035=CARTESIAN_POINT('Ctrl Pts',(2.93587853159832,0.211411177996739,5.6893507432991));
#46036=CARTESIAN_POINT('Ctrl Pts',(2.9262248734342,0.304256454483673,5.69440251641078));
#46037=CARTESIAN_POINT('Ctrl Pts',(2.91611246049209,0.401513862980918,5.69969435655332));
#46038=CARTESIAN_POINT('Ctrl Pts',(2.9011348536606,0.498374650664969,5.70498619669585));
#46039=CARTESIAN_POINT('Ctrl Pts',(2.88134521813328,0.594317872809211,5.71027803683838));
#46040=CARTESIAN_POINT('Ctrl Pts',(2.8624866569247,0.685747102259055,5.71532090339832));
#46041=CARTESIAN_POINT('Ctrl Pts',(2.83925870008827,0.77634266039385,5.72036376995825));
#46042=CARTESIAN_POINT('Ctrl Pts',(2.81176020120084,0.865660771285745,5.72540663651818));
#46043=CARTESIAN_POINT('Ctrl Pts',(2.78427084703965,0.954949179113599,5.73044782605442));
#46044=CARTESIAN_POINT('Ctrl Pts',(2.75251390281918,1.04296056084126,5.73548901559066));
#46045=CARTESIAN_POINT('Ctrl Pts',(2.71663843904049,1.12926506699165,5.7405302051269));
#46046=CARTESIAN_POINT('Ctrl Pts',(2.68076494470297,1.21556483531763,5.74557111791895));
#46047=CARTESIAN_POINT('Ctrl Pts',(2.6407735508614,1.3001575056006,5.75061203071099));
#46048=CARTESIAN_POINT('Ctrl Pts',(2.59686152313343,1.38263307846627,5.75565294350304));
#46049=CARTESIAN_POINT('Ctrl Pts',(2.55293971379227,1.46512702315838,5.7606949791824));
#46050=CARTESIAN_POINT('Ctrl Pts',(2.50509574440028,1.54550254305695,5.76573701486176));
#46051=CARTESIAN_POINT('Ctrl Pts',(2.45357233957565,1.62337511822415,5.77077905054113));
#46052=CARTESIAN_POINT('Ctrl Pts',(2.40199280993323,1.7013325205511,5.77582657854645));
#46053=CARTESIAN_POINT('Ctrl Pts',(2.34672609052198,1.77678116695695,5.78087410655178));
#46054=CARTESIAN_POINT('Ctrl Pts',(2.28805747168708,1.84936665003371,5.7859216345571));
#46055=CARTESIAN_POINT('Ctrl Pts',(2.22935155393146,1.92199827975978,5.79097237155815));
#46056=CARTESIAN_POINT('Ctrl Pts',(2.16723972525796,1.99176279195139,5.79602310855919));
#46057=CARTESIAN_POINT('Ctrl Pts',(2.10204524627031,2.05834151263399,5.80107384556024));
#46058=CARTESIAN_POINT('Ctrl Pts',(2.03675053885168,2.12502258984761,5.80613234744341));
#46059=CARTESIAN_POINT('Ctrl Pts',(1.96836404656305,2.18850780000787,5.81119084932659));
#46060=CARTESIAN_POINT('Ctrl Pts',(1.89724304764583,2.24851791590807,5.81624935120976));
#46061=CARTESIAN_POINT('Ctrl Pts',(1.87307289003801,2.26891208895757,5.81796846075037));
#46062=CARTESIAN_POINT('Ctrl Pts',(1.84858716292389,2.28890527179614,5.81968757029097));
#46063=CARTESIAN_POINT('Ctrl Pts',(1.82380062797807,2.308487658487,5.82140667983157));
#46064=CARTESIAN_POINT('Ctrl Pts',(1.75086435796854,2.36611032523885,5.82646529080335));
#46065=CARTESIAN_POINT('Ctrl Pts',(1.67506765815133,2.42037324670824,5.83152390177514));
#46066=CARTESIAN_POINT('Ctrl Pts',(1.59675277995121,2.47098048549925,5.83658251274692));
#46067=CARTESIAN_POINT('Ctrl Pts',(1.51854376207185,2.52151931712862,5.84163428585861));
#46068=CARTESIAN_POINT('Ctrl Pts',(1.43782369934923,2.56841204795329,5.8466860589703));
#46069=CARTESIAN_POINT('Ctrl Pts',(1.3549672957654,2.61140338274388,5.85173783208199));
#46070=CARTESIAN_POINT('Ctrl Pts',(1.26817344480329,2.6564377233993,5.85702967222452));
#46071=CARTESIAN_POINT('Ctrl Pts',(1.17903555827229,2.69719036849075,5.86232151236705));
#46072=CARTESIAN_POINT('Ctrl Pts',(1.08801798429798,2.73341926272648,5.86761335250958));
#46073=CARTESIAN_POINT('Ctrl Pts',(1.00128265824887,2.7679436388082,5.87265621906952));
#46074=CARTESIAN_POINT('Ctrl Pts',(0.912840971376588,2.79836010072875,5.87769908562946));
#46075=CARTESIAN_POINT('Ctrl Pts',(0.823117940895417,2.82450718805531,5.8827419521894));
#46076=CARTESIAN_POINT('Ctrl Pts',(0.733424748135756,2.85064558007246,5.88778314172565));
#46077=CARTESIAN_POINT('Ctrl Pts',(0.64245148327543,2.87251729469475,5.8928243312619));
#46078=CARTESIAN_POINT('Ctrl Pts',(0.550639145268767,2.89001047259308,5.89786552079815));
#46079=CARTESIAN_POINT('Ctrl Pts',(0.458831847447836,2.90750269017532,5.9029064335902));
#46080=CARTESIAN_POINT('Ctrl Pts',(0.366186003252556,2.92061676659582,5.90794734638225));
#46081=CARTESIAN_POINT('Ctrl Pts',(0.273152533946754,2.92929201227847,5.91298825917431));
#46082=CARTESIAN_POINT('Ctrl Pts',(0.180098340992911,2.93796919041338,5.91803029485367));
#46083=CARTESIAN_POINT('Ctrl Pts',(0.0866567923861568,2.94220553319126,
5.92307233053304));
#46084=CARTESIAN_POINT('Ctrl Pts',(-0.00671747469381417,2.94199233097806,
5.92811436621241));
#46085=CARTESIAN_POINT('Ctrl Pts',(-0.100193455038841,2.94177889652216,
5.93316189421774));
#46086=CARTESIAN_POINT('Ctrl Pts',(-0.19360156413738,2.93710624485276,5.93820942222307));
#46087=CARTESIAN_POINT('Ctrl Pts',(-0.286488909607947,2.92801777738313,
5.9432569502284));
#46088=CARTESIAN_POINT('Ctrl Pts',(-0.379435308756739,2.91892353186666,
5.94830768722946));
#46089=CARTESIAN_POINT('Ctrl Pts',(-0.471859847441745,2.90540794562666,
5.95335842423052));
#46090=CARTESIAN_POINT('Ctrl Pts',(-0.563318599866555,2.88756578367392,
5.95840916123158));
#46091=CARTESIAN_POINT('Ctrl Pts',(-0.654917958787383,2.86969619160863,
5.96346766311476));
#46092=CARTESIAN_POINT('Ctrl Pts',(-0.745548138939165,2.8474868538804,5.96852616499795));
#46093=CARTESIAN_POINT('Ctrl Pts',(-0.83477945612792,2.82108263963089,5.97358466688113));
#46094=CARTESIAN_POINT('Ctrl Pts',(-0.865104325473564,2.81210928394684,
5.97530377642165));
#46095=CARTESIAN_POINT('Ctrl Pts',(-0.895267799915388,2.80265185290961,
5.97702288596217));
#46096=CARTESIAN_POINT('Ctrl Pts',(-0.92525357189597,2.79271728388209,5.97874199550269));
#46097=CARTESIAN_POINT('Ctrl Pts',(-1.01348899352736,2.76348405662225,5.98380060647447));
#46098=CARTESIAN_POINT('Ctrl Pts',(-1.10049113970499,2.73001420585981,5.98885921744625));
#46099=CARTESIAN_POINT('Ctrl Pts',(-1.18582463229285,2.69243086103386,5.99391782841803));
#46100=CARTESIAN_POINT('Ctrl Pts',(-1.27104277731053,2.65489831862292,5.99896960152971));
#46101=CARTESIAN_POINT('Ctrl Pts',(-1.35459634924793,2.61326350930902,6.00402137464139));
#46102=CARTESIAN_POINT('Ctrl Pts',(-1.43606607063285,2.56769901678081,6.00907314775307));
#46103=CARTESIAN_POINT('Ctrl Pts',(-1.52140734239911,2.51996923848232,6.0143649878956));
#46104=CARTESIAN_POINT('Ctrl Pts',(-1.6044613313798,2.46792718037965,6.01965682803813));
#46105=CARTESIAN_POINT('Ctrl Pts',(-1.68477052443031,2.41182758090433,6.02494866818066));
#46106=CARTESIAN_POINT('Ctrl Pts',(-1.76130128370913,2.35836738811688,6.0299915347406));
#46107=CARTESIAN_POINT('Ctrl Pts',(-1.83533925988745,2.30122308642386,6.03503440130054));
#46108=CARTESIAN_POINT('Ctrl Pts',(-1.9065158833466,2.24066088164789,6.04007726786048));
#46109=CARTESIAN_POINT('Ctrl Pts',(-1.97766883675966,2.18011881705433,6.04511845739672));
#46110=CARTESIAN_POINT('Ctrl Pts',(-2.04596199107264,2.11616139454657,6.05015964693297));
#46111=CARTESIAN_POINT('Ctrl Pts',(-2.11105941727713,2.04909544353735,6.05520083646921));
#46112=CARTESIAN_POINT('Ctrl Pts',(-2.17615326985392,1.98203317422116,6.06024174926127));
#46113=CARTESIAN_POINT('Ctrl Pts',(-2.23805143504587,1.91186303389857,6.06528266205332));
#46114=CARTESIAN_POINT('Ctrl Pts',(-2.29645526665579,1.83892827708121,6.07032357484537));
#46115=CARTESIAN_POINT('Ctrl Pts',(-2.35487210799712,1.76597727369972,6.07536561052474));
#46116=CARTESIAN_POINT('Ctrl Pts',(-2.40979279324933,1.69026077657013,6.0804076462041));
#46117=CARTESIAN_POINT('Ctrl Pts',(-2.46096004854542,1.61215372699483,6.08544968188347));
#46118=CARTESIAN_POINT('Ctrl Pts',(-2.51218304070308,1.53396159484504,6.0904972098888));
#46119=CARTESIAN_POINT('Ctrl Pts',(-2.55964420000958,1.45337408417339,6.09554473789412));
#46120=CARTESIAN_POINT('Ctrl Pts',(-2.60313073720987,1.37079333416574,6.10059226589945));
#46121=CARTESIAN_POINT('Ctrl Pts',(-2.64664492123288,1.28816008295881,6.1056430029005));
#46122=CARTESIAN_POINT('Ctrl Pts',(-2.68617926538312,1.20353147045019,6.11069373990156));
#46123=CARTESIAN_POINT('Ctrl Pts',(-2.72156881188788,1.11733039077938,6.11574447690261));
#46124=CARTESIAN_POINT('Ctrl Pts',(-2.75701276543406,1.03099678763269,6.12080297878579));
#46125=CARTESIAN_POINT('Ctrl Pts',(-2.78829905578336,0.943086308889602,
6.12586148066897));
#46126=CARTESIAN_POINT('Ctrl Pts',(-2.81531240535529,0.854037505179129,
6.13091998255216));
#46127=CARTESIAN_POINT('Ctrl Pts',(-2.82449277299058,0.823774662232998,
6.13263909209271));
#46128=CARTESIAN_POINT('Ctrl Pts',(-2.8331800730815,0.793380435653022,6.13435820163326));
#46129=CARTESIAN_POINT('Ctrl Pts',(-2.84137113266297,0.762872260912386,
6.13607731117381));
#46130=CARTESIAN_POINT('Ctrl Pts',(-2.8719532099979,0.648967173299931,6.14249576539131));
#46131=CARTESIAN_POINT('Ctrl Pts',(-2.89569962933492,0.53315563976223,6.1489142196088));
#46132=CARTESIAN_POINT('Ctrl Pts',(-2.91241724655161,0.416160764595568,
6.15533267382629));
#46133=CARTESIAN_POINT('Ctrl Pts',(-2.92884290384954,0.301209112084665,
6.16163903483411));
#46134=CARTESIAN_POINT('Ctrl Pts',(-2.93848311852094,0.185114923026029,
6.16794539584194));
#46135=CARTESIAN_POINT('Ctrl Pts',(-2.94120044838797,0.0685851470977758,
6.17425175684976));
#46136=CARTESIAN_POINT('Ctrl Pts',(-2.94171350534655,0.0465832498869957,
6.17544245601281));
#46137=CARTESIAN_POINT('Ctrl Pts',(-2.94197990287227,0.0245658899272368,
6.17663315517586));
#46138=CARTESIAN_POINT('Ctrl Pts',(-2.94199890533048,0.00253791927304354,
6.17782385433891));
#46139=CARTESIAN_POINT('',(-2.93846014819028,-0.00170708260597003,7.1778238829104));
#46140=CARTESIAN_POINT('Ctrl Pts',(-2.94109090649655,0.00253660757586993,
6.1778238829104));
#46141=CARTESIAN_POINT('Ctrl Pts',(-2.9349800243151,-0.710047628629508,
6.21635346422191));
#46142=CARTESIAN_POINT('Ctrl Pts',(-2.31871586625516,-2.40205366998755,
6.30732815075713));
#46143=CARTESIAN_POINT('Ctrl Pts',(0.49761738400481,-3.43088509381354,6.45074794251606));
#46144=CARTESIAN_POINT('Ctrl Pts',(3.13924192099676,-1.47097102258829,6.6080832581872));
#46145=CARTESIAN_POINT('Ctrl Pts',(2.9548415774069,1.81314832273499,6.76541857385831));
#46146=CARTESIAN_POINT('Ctrl Pts',(0.110418200862219,3.46502574430695,6.92275388952942));
#46147=CARTESIAN_POINT('Ctrl Pts',(-2.46168690535804,2.18289276465007,7.06022232588014));
#46148=CARTESIAN_POINT('Ctrl Pts',(-2.93520341737875,0.60217681128353,7.14524565700712));
#46149=CARTESIAN_POINT('Ctrl Pts',(-2.93846014819028,-0.00170708260597003,
7.1778238829104));
#46150=CARTESIAN_POINT('',(-2.94242797829922,-0.000395178309583312,8.17782384089891));
#46151=CARTESIAN_POINT('Ctrl Pts',(-2.93846014819028,-0.00170708260597003,
7.1778238829104));
#46152=CARTESIAN_POINT('Ctrl Pts',(-2.94044617033292,-0.369968033311824,
7.19769076223082));
#46153=CARTESIAN_POINT('Ctrl Pts',(-2.7064938607242,-1.70794280458433,7.27000274677496));
#46154=CARTESIAN_POINT('Ctrl Pts',(-0.715046473049612,-3.39224175569136,
7.39475983654279));
#46155=CARTESIAN_POINT('Ctrl Pts',(2.44013696723815,-2.46258546444226,7.55209515221394));
#46156=CARTESIAN_POINT('Ctrl Pts',(3.39864746673817,0.683952471759658,7.70943046788504));
#46157=CARTESIAN_POINT('Ctrl Pts',(1.297609660921,3.21477911452055,7.86676578355616));
#46158=CARTESIAN_POINT('Ctrl Pts',(-1.94654513937998,2.85436050058246,8.02289677247183));
#46159=CARTESIAN_POINT('Ctrl Pts',(-2.94475147365309,0.9427053576651,8.12658265616376));
#46160=CARTESIAN_POINT('Ctrl Pts',(-2.94656694648226,-0.000388257878349857,
8.17782343463199));
#46161=CARTESIAN_POINT('',(-2.94199919951374,0.00217026738102695,9.17782384908627));
#46162=CARTESIAN_POINT('Ctrl Pts',(-2.94199997336302,-0.000395893941740302,
8.1778238829104));
#46163=CARTESIAN_POINT('Ctrl Pts',(-2.94199699558754,-0.0225245866073216,
8.17902806023974));
#46164=CARTESIAN_POINT('Ctrl Pts',(-2.94174435529623,-0.0446513335979655,
8.18023223756908));
#46165=CARTESIAN_POINT('Ctrl Pts',(-2.94124216062025,-0.0667723939207123,
8.18143641489842));
#46166=CARTESIAN_POINT('Ctrl Pts',(-2.93913249832053,-0.159700434032431,
8.18649502590215));
#46167=CARTESIAN_POINT('Ctrl Pts',(-2.93261078956895,-0.252690066630103,
8.19155363690589));
#46168=CARTESIAN_POINT('Ctrl Pts',(-2.92166725446723,-0.345288943022986,
8.19661224790961));
#46169=CARTESIAN_POINT('Ctrl Pts',(-2.9107385120351,-0.437762651033725,
8.20166402105332));
#46170=CARTESIAN_POINT('Ctrl Pts',(-2.89539987318824,-0.529846216297979,
8.20671579419702));
#46171=CARTESIAN_POINT('Ctrl Pts',(-2.87569355922515,-0.621088201007697,
8.21176756734073));
#46172=CARTESIAN_POINT('Ctrl Pts',(-2.85505077496562,-0.716666126402669,
8.21705940747526));
#46173=CARTESIAN_POINT('Ctrl Pts',(-2.82961491564589,-0.811320011255229,
8.2223512476098));
#46174=CARTESIAN_POINT('Ctrl Pts',(-2.79949555676382,-0.904537797805956,
8.22764308774433));
#46175=CARTESIAN_POINT('Ctrl Pts',(-2.7707932708266,-0.993369820243381,
8.23268595433622));
#46176=CARTESIAN_POINT('Ctrl Pts',(-2.7378383509055,-1.08089733868883,8.2377288209281));
#46177=CARTESIAN_POINT('Ctrl Pts',(-2.70077738617931,-1.16668998037288,
8.24277168751999));
#46178=CARTESIAN_POINT('Ctrl Pts',(-2.66372874621288,-1.25245409139922,
8.24781287708809));
#46179=CARTESIAN_POINT('Ctrl Pts',(-2.6225769500208,-1.33648406574942,8.25285406665619));
#46180=CARTESIAN_POINT('Ctrl Pts',(-2.57751698862641,-1.41836884248853,
8.25789525622429));
#46181=CARTESIAN_POINT('Ctrl Pts',(-2.53245950087213,-1.50024912402921,
8.26293616904806));
#46182=CARTESIAN_POINT('Ctrl Pts',(-2.48349448850748,-1.57998405433466,
8.26797708187183));
#46183=CARTESIAN_POINT('Ctrl Pts',(-2.43086268957996,-1.65718755257456,
8.27301799469561));
#46184=CARTESIAN_POINT('Ctrl Pts',(-2.37821916667063,-1.73440824825837,
8.27806003040652));
#46185=CARTESIAN_POINT('Ctrl Pts',(-2.32190748464932,-1.80909602620733,
8.28310206611743));
#46186=CARTESIAN_POINT('Ctrl Pts',(-2.26221079575508,-1.88089508361556,
8.28814410182835));
#46187=CARTESIAN_POINT('Ctrl Pts',(-2.20244907883106,-1.95277235225007,
8.29319162986479));
#46188=CARTESIAN_POINT('Ctrl Pts',(-2.13929527959758,-2.02175427932885,
8.29823915790124));
#46189=CARTESIAN_POINT('Ctrl Pts',(-2.07307158391174,-2.08751963056103,
8.30328668593768));
#46190=CARTESIAN_POINT('Ctrl Pts',(-2.00680578612355,-2.1533267925004,8.30833742296963));
#46191=CARTESIAN_POINT('Ctrl Pts',(-1.93746653482207,-2.21591301108361,
8.31338816000158));
#46192=CARTESIAN_POINT('Ctrl Pts',(-1.86540986927196,-2.27499670760702,
8.31843889703353));
#46193=CARTESIAN_POINT('Ctrl Pts',(-1.79324242553851,-2.33417123798342,
8.32349739894704));
#46194=CARTESIAN_POINT('Ctrl Pts',(-1.71834958445942,-2.38983223599387,
8.32855590086054));
#46195=CARTESIAN_POINT('Ctrl Pts',(-1.64111690523925,-2.44174103936882,
8.33361440277404));
#46196=CARTESIAN_POINT('Ctrl Pts',(-1.61486972441552,-2.45938201417745,
8.33533351203921));
#46197=CARTESIAN_POINT('Ctrl Pts',(-1.58835251507917,-2.47659002051337,
8.33705262130437));
#46198=CARTESIAN_POINT('Ctrl Pts',(-1.56158101890186,-2.49335691817386,
8.33877173056953));
#46199=CARTESIAN_POINT('Ctrl Pts',(-1.48280383701224,-2.54269480119604,
8.34383034150308));
#46200=CARTESIAN_POINT('Ctrl Pts',(-1.40154908211522,-2.58838144079867,
8.34888895243663));
#46201=CARTESIAN_POINT('Ctrl Pts',(-1.31818919554193,-2.6301599276007,8.35394756337018));
#46202=CARTESIAN_POINT('Ctrl Pts',(-1.2349419887612,-2.67188194130255,8.35899933644377));
#46203=CARTESIAN_POINT('Ctrl Pts',(-1.14959569804075,-2.70970610388165,
8.36405110951736));
#46204=CARTESIAN_POINT('Ctrl Pts',(-1.06255059870906,-2.74341944025755,
8.36910288259095));
#46205=CARTESIAN_POINT('Ctrl Pts',(-0.971368998709515,-2.77873487990525,
8.37439472274302));
#46206=CARTESIAN_POINT('Ctrl Pts',(-0.878323541763301,-2.8095388389535,
8.37968656289509));
#46207=CARTESIAN_POINT('Ctrl Pts',(-0.783902172583036,-2.8356412650086,
8.38497840304716));
#46208=CARTESIAN_POINT('Ctrl Pts',(-0.693923195902074,-2.86051560866321,
8.39002126956961));
#46209=CARTESIAN_POINT('Ctrl Pts',(-0.602695321896114,-2.88112065717945,
8.39506413609205));
#46210=CARTESIAN_POINT('Ctrl Pts',(-0.510658622135931,-2.89734219098094,
8.4001070026145));
#46211=CARTESIAN_POINT('Ctrl Pts',(-0.418652529511199,-2.91355833025303,
8.40514819211355));
#46212=CARTESIAN_POINT('Ctrl Pts',(-0.325838581377534,-2.92539377442687,
8.4101893816126));
#46213=CARTESIAN_POINT('Ctrl Pts',(-0.232667334874957,-2.93278535035931,
8.41523057111165));
#46214=CARTESIAN_POINT('Ctrl Pts',(-0.139501203151212,-2.94017652051983,
8.42027148386685));
#46215=CARTESIAN_POINT('Ctrl Pts',(-0.0459782536247714,-2.94312427300938,
8.42531239662205));
#46216=CARTESIAN_POINT('Ctrl Pts',(0.0474466652067634,-2.94161738061917,
8.43035330937725));
#46217=CARTESIAN_POINT('Ctrl Pts',(0.14089239489094,-2.94011015256138,8.43539534502016));
#46218=CARTESIAN_POINT('Ctrl Pts',(0.234239607738917,-2.9341463162658,8.44043738066306));
#46219=CARTESIAN_POINT('Ctrl Pts',(0.3270354216065,-2.923766720006,8.44547941630597));
#46220=CARTESIAN_POINT('Ctrl Pts',(0.419932318640967,-2.91337581717517,
8.45052694427562));
#46221=CARTESIAN_POINT('Ctrl Pts',(0.512276177259232,-2.89855960388633,
8.45557447224527));
#46222=CARTESIAN_POINT('Ctrl Pts',(0.603621524189472,-2.87941053959577,
8.46062200021492));
#46223=CARTESIAN_POINT('Ctrl Pts',(0.695024944471082,-2.8602493011729,8.4656727371807));
#46224=CARTESIAN_POINT('Ctrl Pts',(0.785428161133795,-2.83674983911359,
8.47072347414649));
#46225=CARTESIAN_POINT('Ctrl Pts',(0.87440020723099,-2.80905469466054,8.47577421111227));
#46226=CARTESIAN_POINT('Ctrl Pts',(0.963509036838297,-2.78131697235031,
8.48083271296109));
#46227=CARTESIAN_POINT('Ctrl Pts',(1.05118188944844,-2.74937084542327,8.48589121480991));
#46228=CARTESIAN_POINT('Ctrl Pts',(1.13700741094499,-2.71340711052657,8.49094971665872));
#46229=CARTESIAN_POINT('Ctrl Pts',(1.16617484128498,-2.7011849915802,8.49266882651937));
#46230=CARTESIAN_POINT('Ctrl Pts',(1.19512912467167,-2.68849925012339,8.49438793638002));
#46231=CARTESIAN_POINT('Ctrl Pts',(1.22385480592929,-2.67535855802615,8.49610704624066));
#46232=CARTESIAN_POINT('Ctrl Pts',(1.30838229812822,-2.63669107652149,8.50116565717601));
#46233=CARTESIAN_POINT('Ctrl Pts',(1.39122251621103,-2.59394645723791,8.50622426811136));
#46234=CARTESIAN_POINT('Ctrl Pts',(1.47195607870599,-2.54729450640488,8.51128287904671));
#46235=CARTESIAN_POINT('Ctrl Pts',(1.55258051147071,-2.50070561626994,8.51633465212145));
#46236=CARTESIAN_POINT('Ctrl Pts',(1.63110356743534,-2.45022011065338,8.52138642519618));
#46237=CARTESIAN_POINT('Ctrl Pts',(1.70712725519738,-2.39605520273684,8.52643819827092));
#46238=CARTESIAN_POINT('Ctrl Pts',(1.78676369124228,-2.33931630526747,8.53173003842262));
#46239=CARTESIAN_POINT('Ctrl Pts',(1.8636568749786,-2.27853983593225,8.53702187857433));
#46240=CARTESIAN_POINT('Ctrl Pts',(1.93737975263415,-2.21402883768103,8.54231371872603));
#46241=CARTESIAN_POINT('Ctrl Pts',(2.00763407267695,-2.15255299108432,8.54735658524801));
#46242=CARTESIAN_POINT('Ctrl Pts',(2.07500926457794,-2.08768638549101,8.55239945176999));
#46243=CARTESIAN_POINT('Ctrl Pts',(2.13916793791325,-2.0197337778539,8.55744231829197));
#46244=CARTESIAN_POINT('Ctrl Pts',(2.20330527504356,-1.95180376810872,8.56248350778996));
#46245=CARTESIAN_POINT('Ctrl Pts',(2.26422791513643,-1.88079011717847,8.56752469728795));
#46246=CARTESIAN_POINT('Ctrl Pts',(2.32163533784804,-1.8070344097596,8.57256588678595));
#46247=CARTESIAN_POINT('Ctrl Pts',(2.37903960908429,-1.7332827512822,8.57760679953951));
#46248=CARTESIAN_POINT('Ctrl Pts',(2.43292877501671,-1.65678968546736,8.58264771229308));
#46249=CARTESIAN_POINT('Ctrl Pts',(2.48304334279859,-1.57792894573349,8.58768862504665));
#46250=CARTESIAN_POINT('Ctrl Pts',(2.53316907383721,-1.49905063939727,8.59273066068734));
#46251=CARTESIAN_POINT('Ctrl Pts',(2.57951829953034,-1.41780398556084,8.59777269632804));
#46252=CARTESIAN_POINT('Ctrl Pts',(2.62187610376823,-1.33458971091835,8.60281473196874));
#46253=CARTESIAN_POINT('Ctrl Pts',(2.66428004866875,-1.25128479036439,8.60786225993534));
#46254=CARTESIAN_POINT('Ctrl Pts',(2.70268369366719,-1.16600836662952,8.61290978790194));
#46255=CARTESIAN_POINT('Ctrl Pts',(2.73691930436214,-1.07918335856789,8.61795731586855));
#46256=CARTESIAN_POINT('Ctrl Pts',(2.77117668054832,-0.992303150995767,
8.6230080528308));
#46257=CARTESIAN_POINT('Ctrl Pts',(2.80126060462734,-0.903872817919549,
8.62805878979304));
#46258=CARTESIAN_POINT('Ctrl Pts',(2.82705314929468,-0.81433070128972,8.63310952675529));
#46259=CARTESIAN_POINT('Ctrl Pts',(2.852885346804,-0.724650924749004,8.63816802859988));
#46260=CARTESIAN_POINT('Ctrl Pts',(2.87441289581222,-0.633856383383457,
8.64322653044447));
#46261=CARTESIAN_POINT('Ctrl Pts',(2.89156895864927,-0.54239557278429,8.64828503228906));
#46262=CARTESIAN_POINT('Ctrl Pts',(2.89739937206662,-0.511313013671278,
8.65000414216331));
#46263=CARTESIAN_POINT('Ctrl Pts',(2.9027253431409,-0.480153543002247,8.65172325203756));
#46264=CARTESIAN_POINT('Ctrl Pts',(2.90754561634846,-0.448934838092175,
8.6534423619118));
#46265=CARTESIAN_POINT('Ctrl Pts',(2.92172963584773,-0.357071431160895,
8.65850097309995));
#46266=CARTESIAN_POINT('Ctrl Pts',(2.93158046042886,-0.264375334532386,
8.6635595842881));
#46267=CARTESIAN_POINT('Ctrl Pts',(2.93700930629233,-0.171290206235695,
8.66861819547625));
#46268=CARTESIAN_POINT('Ctrl Pts',(2.94243081384023,-0.0783309035864636,
8.67366996880491));
#46269=CARTESIAN_POINT('Ctrl Pts',(2.94344219588367,0.0150159471495223,
8.67872174213356));
#46270=CARTESIAN_POINT('Ctrl Pts',(2.94000602687925,0.108298485278775,8.68377351546222));
#46271=CARTESIAN_POINT('Ctrl Pts',(2.93640656670854,0.206013929480568,8.68906535555059));
#46272=CARTESIAN_POINT('Ctrl Pts',(2.92792629014359,0.303658312521264,8.69435719563895));
#46273=CARTESIAN_POINT('Ctrl Pts',(2.91458347896305,0.400708303078024,8.69964903572731));
#46274=CARTESIAN_POINT('Ctrl Pts',(2.90186842747084,0.493192233979073,8.70469190250415));
#46275=CARTESIAN_POINT('Ctrl Pts',(2.88473808584657,0.58513594071538,8.70973476928099));
#46276=CARTESIAN_POINT('Ctrl Pts',(2.86326147221195,0.6760900396742,8.71477763605784));
#46277=CARTESIAN_POINT('Ctrl Pts',(2.8417920007054,0.767013891507716,8.7198188258105));
#46278=CARTESIAN_POINT('Ctrl Pts',(2.81597923070519,0.856948358768648,8.72486001556315));
#46279=CARTESIAN_POINT('Ctrl Pts',(2.78594321468515,0.945454602056485,8.72990120531581));
#46280=CARTESIAN_POINT('Ctrl Pts',(2.75590884754489,1.03395598663885,8.73494211832352));
#46281=CARTESIAN_POINT('Ctrl Pts',(2.7216518382119,1.12102888389986,8.73998303133123));
#46282=CARTESIAN_POINT('Ctrl Pts',(2.68334165152275,1.20625104402158,8.74502394433894));
#46283=CARTESIAN_POINT('Ctrl Pts',(2.64502293106542,1.29149218776677,8.75006598023293));
#46284=CARTESIAN_POINT('Ctrl Pts',(2.60264942190965,1.37488137180379,8.75510801612691));
#46285=CARTESIAN_POINT('Ctrl Pts',(2.55643764690833,1.4560187352743,8.7601500520209));
#46286=CARTESIAN_POINT('Ctrl Pts',(2.51017553311329,1.53724448221424,8.76519758023811));
#46287=CARTESIAN_POINT('Ctrl Pts',(2.46006702862052,1.61621312783523,8.77024510845532));
#46288=CARTESIAN_POINT('Ctrl Pts',(2.40637313666205,1.69255201608436,8.77529263667252));
#46289=CARTESIAN_POINT('Ctrl Pts',(2.35264510851053,1.76893943720998,8.78034337388411));
#46290=CARTESIAN_POINT('Ctrl Pts',(2.29532742646195,1.84269342327889,8.7853941110957));
#46291=CARTESIAN_POINT('Ctrl Pts',(2.23472136401146,1.9134744380918,8.79044484830729));
#46292=CARTESIAN_POINT('Ctrl Pts',(2.17402212730053,1.9843642698851,8.79550335039727));
#46293=CARTESIAN_POINT('Ctrl Pts',(2.1100247236143,2.05227168693138,8.80056185248724));
#46294=CARTESIAN_POINT('Ctrl Pts',(2.04306700070858,2.11689424171725,8.80562035457722));
#46295=CARTESIAN_POINT('Ctrl Pts',(2.02031173978954,2.13885590695306,8.80733946224578));
#46296=CARTESIAN_POINT('Ctrl Pts',(1.99721485376002,2.16043853602434,8.80905856991435));
#46297=CARTESIAN_POINT('Ctrl Pts',(1.97379041694743,2.18163135977793,8.81077767758291));
#46298=CARTESIAN_POINT('Ctrl Pts',(1.90486215393261,2.24399292438677,8.81583628823288));
#46299=CARTESIAN_POINT('Ctrl Pts',(1.8328556274808,2.30319312272707,8.82089489888285));
#46300=CARTESIAN_POINT('Ctrl Pts',(1.75809257682032,2.35891383719908,8.82595350953281));
#46301=CARTESIAN_POINT('Ctrl Pts',(1.68343058537718,2.41455923248943,8.83100528232332));
#46302=CARTESIAN_POINT('Ctrl Pts',(1.60601982680215,2.46673422837125,8.83605705511383));
#46303=CARTESIAN_POINT('Ctrl Pts',(1.52621713276797,2.51515909310833,8.84110882790434));
#46304=CARTESIAN_POINT('Ctrl Pts',(1.44262210114271,2.56588517633318,8.84640066812725));
#46305=CARTESIAN_POINT('Ctrl Pts',(1.35640252290727,2.61249553642561,8.85169250835015));
#46306=CARTESIAN_POINT('Ctrl Pts',(1.26800555770157,2.6547176696662,8.85698434857305));
#46307=CARTESIAN_POINT('Ctrl Pts',(1.18376755107093,2.69495330820428,8.86202721481567));
#46308=CARTESIAN_POINT('Ctrl Pts',(1.09755284862545,2.73120406339136,8.86707008105828));
#46309=CARTESIAN_POINT('Ctrl Pts',(1.00977474512091,2.76328047148964,8.87211294730089));
#46310=CARTESIAN_POINT('Ctrl Pts',(0.922025832511028,2.79534621247377,8.87715413652189));
#46311=CARTESIAN_POINT('Ctrl Pts',(0.832714967510445,2.82324021269868,8.88219532574288));
#46312=CARTESIAN_POINT('Ctrl Pts',(0.742274701086023,2.84682143242734,8.88723651496388));
#46313=CARTESIAN_POINT('Ctrl Pts',(0.651839399481275,2.87040135763854,8.89227742744315));
#46314=CARTESIAN_POINT('Ctrl Pts',(0.560275248446931,2.88966886187587,8.89731833992241));
#46315=CARTESIAN_POINT('Ctrl Pts',(0.468028113920198,2.90453329892778,8.90235925240168));
#46316=CARTESIAN_POINT('Ctrl Pts',(0.375760430851592,2.91940104711243,8.90740128777112));
#46317=CARTESIAN_POINT('Ctrl Pts',(0.282809899369842,2.92986370997426,8.91244332314057));
#46318=CARTESIAN_POINT('Ctrl Pts',(0.189629561890907,2.93588225738994,8.91748535851001));
#46319=CARTESIAN_POINT('Ctrl Pts',(0.0963477222794635,2.94190736086041,
8.92253288621138));
#46320=CARTESIAN_POINT('Ctrl Pts',(0.00283601960583585,2.94347865885932,
8.92758041391275));
#46321=CARTESIAN_POINT('Ctrl Pts',(-0.0904507670271132,2.94060923258161,
8.93262794161412));
#46322=CARTESIAN_POINT('Ctrl Pts',(-0.183796861346238,2.93773798204733,
8.93767867831431));
#46323=CARTESIAN_POINT('Ctrl Pts',(-0.276917313935894,2.9304204214277,8.94272941501451));
#46324=CARTESIAN_POINT('Ctrl Pts',(-0.36936286457646,2.91872147939331,8.9477801517147));
#46325=CARTESIAN_POINT('Ctrl Pts',(-0.461950538931314,2.90700455166806,
8.95283865330412));
#46326=CARTESIAN_POINT('Ctrl Pts',(-0.553860805277309,2.89089287552825,
8.95789715489354));
#46327=CARTESIAN_POINT('Ctrl Pts',(-0.64465526958578,2.87050232248561,8.96295565648295));
#46328=CARTESIAN_POINT('Ctrl Pts',(-0.675511418131734,2.86357267167033,
8.96467476873998));
#46329=CARTESIAN_POINT('Ctrl Pts',(-0.706238835613273,2.85614925247111,
8.96639388099701));
#46330=CARTESIAN_POINT('Ctrl Pts',(-0.736820787785887,2.84823789854123,
8.96811299325404));
#46331=CARTESIAN_POINT('Ctrl Pts',(-0.826810370879999,2.82495817336733,
8.97317160411147));
#46332=CARTESIAN_POINT('Ctrl Pts',(-0.915852156281128,2.79736896745877,
8.97823021496891));
#46333=CARTESIAN_POINT('Ctrl Pts',(-1.00350351945997,2.76556408105678,8.98328882582634));
#46334=CARTESIAN_POINT('Ctrl Pts',(-1.09103640187716,2.7338021861957,8.98834059882016));
#46335=CARTESIAN_POINT('Ctrl Pts',(-1.17718218424931,2.69783608528959,8.99339237181398));
#46336=CARTESIAN_POINT('Ctrl Pts',(-1.26151100651736,2.65780999705313,8.99844414480779));
#46337=CARTESIAN_POINT('Ctrl Pts',(-1.34984725001926,2.61588181423509,9.00373598497935));
#46338=CARTESIAN_POINT('Ctrl Pts',(-1.43618908692142,2.56949832423015,9.00902782515091));
#46339=CARTESIAN_POINT('Ctrl Pts',(-1.5200630241403,2.51888316573863,9.01431966532246));
#46340=CARTESIAN_POINT('Ctrl Pts',(-1.59999080899302,2.47064938022265,9.01936253175669));
#46341=CARTESIAN_POINT('Ctrl Pts',(-1.67767722455368,2.41857334437907,9.02440539819091));
#46342=CARTESIAN_POINT('Ctrl Pts',(-1.75273675775916,2.36289607431218,9.02944826462513));
#46343=CARTESIAN_POINT('Ctrl Pts',(-1.82777132960363,2.3072373199538,9.03448945403308));
#46344=CARTESIAN_POINT('Ctrl Pts',(-1.900180399401,2.24797997455053,9.03953064344102));
#46345=CARTESIAN_POINT('Ctrl Pts',(-1.96960831094362,2.1854077654895,9.04457183284897));
#46346=CARTESIAN_POINT('Ctrl Pts',(-2.03903241109631,2.12283899146033,9.04961274551031));
#46347=CARTESIAN_POINT('Ctrl Pts',(-2.10547534975239,2.0569560125236,9.05465365817165));
#46348=CARTESIAN_POINT('Ctrl Pts',(-2.16861623959636,1.98808138801181,9.059694570833));
#46349=CARTESIAN_POINT('Ctrl Pts',(-2.23177119434668,1.91919142137947,9.06473660637944));
#46350=CARTESIAN_POINT('Ctrl Pts',(-2.29162234038641,1.84730881225314,9.06977864192589));
#46351=CARTESIAN_POINT('Ctrl Pts',(-2.34788795590304,1.7727904970767,9.07482067747234));
#46352=CARTESIAN_POINT('Ctrl Pts',(-2.40421486193528,1.69819100859542,9.07986820534221));
#46353=CARTESIAN_POINT('Ctrl Pts',(-2.45694817535026,1.62095043798711,9.08491573321209));
#46354=CARTESIAN_POINT('Ctrl Pts',(-2.50584874474712,1.54145582760236,9.08996326108197));
#46355=CARTESIAN_POINT('Ctrl Pts',(-2.55478040295481,1.46191067807391,9.09501399794595));
#46356=CARTESIAN_POINT('Ctrl Pts',(-2.59987425261999,1.38010902333081,9.10006473480993));
#46357=CARTESIAN_POINT('Ctrl Pts',(-2.64093748212801,1.29646180641443,9.10511547167391));
#46358=CARTESIAN_POINT('Ctrl Pts',(-2.68206384125354,1.21268599228655,9.11017397341879));
#46359=CARTESIAN_POINT('Ctrl Pts',(-2.71914703754702,1.1270593588051,9.11523247516368));
#46360=CARTESIAN_POINT('Ctrl Pts',(-2.75204278401172,1.04001178597601,9.12029097690856));
#46361=CARTESIAN_POINT('Ctrl Pts',(-2.76322226593535,1.01042903223055,9.12201008758076));
#46362=CARTESIAN_POINT('Ctrl Pts',(-2.77391854663788,0.980682282963654,
9.12372919825296));
#46363=CARTESIAN_POINT('Ctrl Pts',(-2.78412729667365,0.950788723069774,
9.12544830892516));
#46364=CARTESIAN_POINT('Ctrl Pts',(-2.81929552746703,0.847808082942463,
9.13137049143208));
#46365=CARTESIAN_POINT('Ctrl Pts',(-2.84877409654376,0.742792724543732,
9.137292673939));
#46366=CARTESIAN_POINT('Ctrl Pts',(-2.87235963900125,0.636328613403945,
9.14321485644592));
#46367=CARTESIAN_POINT('Ctrl Pts',(-2.89572986727888,0.530836421091849,
9.14908297490611));
#46368=CARTESIAN_POINT('Ctrl Pts',(-2.9133141094229,0.423921925118199,9.15495109336631));
#46369=CARTESIAN_POINT('Ctrl Pts',(-2.92496101254477,0.316175702882257,
9.1608192118265));
#46370=CARTESIAN_POINT('Ctrl Pts',(-2.93621114687264,0.212100013337014,
9.16648742424642));
#46371=CARTESIAN_POINT('Ctrl Pts',(-2.94192168493498,0.107248485242721,
9.17215563666635));
#46372=CARTESIAN_POINT('Ctrl Pts',(-2.94199919951374,0.00217026738102695,
9.17782384908627));
#46373=CARTESIAN_POINT('',(-2.93989309841074,-0.00232834448912937,10.1778238829104));
#46374=CARTESIAN_POINT('Ctrl Pts',(-2.93938212312892,0.00216771032458683,
9.1778238829104));
#46375=CARTESIAN_POINT('Ctrl Pts',(-2.93484702512206,-0.645845798130107,
9.21281046347236));
#46376=CARTESIAN_POINT('Ctrl Pts',(-2.40612385725697,-2.27196315558581,
9.30024214925803));
#46377=CARTESIAN_POINT('Ctrl Pts',(0.267550388642242,-3.45644520972621,
9.44011894026741));
#46378=CARTESIAN_POINT('Ctrl Pts',(3.03407913010763,-1.67718692077773,9.59745425593852));
#46379=CARTESIAN_POINT('Ctrl Pts',(3.06925466623265,1.61191643161126,9.75478957160967));
#46380=CARTESIAN_POINT('Ctrl Pts',(0.341406797652991,3.44993374993849,9.91212488728076));
#46381=CARTESIAN_POINT('Ctrl Pts',(-2.3788716582907,2.31375700223615,10.053136324381));
#46382=CARTESIAN_POINT('Ctrl Pts',(-2.93479827488144,0.666407318052135,
10.1417026562576));
#46383=CARTESIAN_POINT('Ctrl Pts',(-2.93989309841074,-0.00232834448912937,
10.1778238829104));
#46384=CARTESIAN_POINT('',(-2.14415473270596,2.01243073062332,11.058));
#46385=CARTESIAN_POINT('Ctrl Pts',(-2.93989309841074,-0.00232834448912937,
10.1778238829104));
#46386=CARTESIAN_POINT('Ctrl Pts',(-2.94219554736775,-0.304542880453153,
10.1941477614813));
#46387=CARTESIAN_POINT('Ctrl Pts',(-2.76120346070747,-1.57501837043084,
10.262916745276));
#46388=CARTESIAN_POINT('Ctrl Pts',(-0.93982089220685,-3.33696855340065,
10.384130834294));
#46389=CARTESIAN_POINT('Ctrl Pts',(2.27033791967618,-2.61992335659031,10.5414661499654));
#46390=CARTESIAN_POINT('Ctrl Pts',(3.43675322554089,0.455595550491127,10.6988014656364));
#46391=CARTESIAN_POINT('Ctrl Pts',(1.50917870869015,3.12106661837876,10.8561367813075));
#46392=CARTESIAN_POINT('Ctrl Pts',(-0.991414248907668,3.01120383063971,
10.9758696260954));
#46393=CARTESIAN_POINT('Ctrl Pts',(-1.95802372783935,2.21436813426865,11.0431573656595));
#46394=CARTESIAN_POINT('Ctrl Pts',(-2.14415473270596,2.01243073062332,11.058));
#46395=CARTESIAN_POINT('',(0.261592048850261,2.93034701016421,11.0579991307071));
#46396=CARTESIAN_POINT('Origin',(0.,0.,11.058));
#46397=CARTESIAN_POINT('',(-2.94199895080427,-0.00248464616942429,10.3221761170896));
#46398=CARTESIAN_POINT('Ctrl Pts',(0.261592048850261,2.93034701016421,11.0579991307071));
#46399=CARTESIAN_POINT('Ctrl Pts',(0.360090029576933,2.92155409639102,11.0526819206525));
#46400=CARTESIAN_POINT('Ctrl Pts',(0.458023157418216,2.90780150422239,11.0473647105979));
#46401=CARTESIAN_POINT('Ctrl Pts',(0.554897463885622,2.88919587507896,11.0420475005432));
#46402=CARTESIAN_POINT('Ctrl Pts',(0.652086440068712,2.87052981063286,11.0367130189846));
#46403=CARTESIAN_POINT('Ctrl Pts',(0.74820935947663,2.84697925549818,11.0313785374259));
#46404=CARTESIAN_POINT('Ctrl Pts',(0.842784692145053,2.8187014674644,11.0260440558672));
#46405=CARTESIAN_POINT('Ctrl Pts',(0.937521801343244,2.79037530865265,11.0207004493719));
#46406=CARTESIAN_POINT('Ctrl Pts',(1.03070570050046,2.75730590422185,11.0153568428766));
#46407=CARTESIAN_POINT('Ctrl Pts',(1.12187471940277,2.71969871749886,11.0100132363813));
#46408=CARTESIAN_POINT('Ctrl Pts',(1.21330895958217,2.68198212709674,11.0046540847134));
#46409=CARTESIAN_POINT('Ctrl Pts',(1.30271626992542,2.63970151287218,10.9992949330454));
#46410=CARTESIAN_POINT('Ctrl Pts',(1.38965816406483,2.59310898094314,10.9939357813775));
#46411=CARTESIAN_POINT('Ctrl Pts',(1.4393916051184,2.56645661773934,10.9908701815742));
#46412=CARTESIAN_POINT('Ctrl Pts',(1.48831883990037,2.53839411919676,10.9878045817709));
#46413=CARTESIAN_POINT('Ctrl Pts',(1.53636235385959,2.50897483399954,10.9847389819675));
#46414=CARTESIAN_POINT('Ctrl Pts',(1.61577682077707,2.46034565060939,10.9796716387593));
#46415=CARTESIAN_POINT('Ctrl Pts',(1.6930151158665,2.40785972230369,10.974604295551));
#46416=CARTESIAN_POINT('Ctrl Pts',(1.76768054498651,2.35173754719276,10.9695369523427));
#46417=CARTESIAN_POINT('Ctrl Pts',(1.84224573176959,2.29569071910725,10.964476412314));
#46418=CARTESIAN_POINT('Ctrl Pts',(1.91424456807512,2.23601760989157,10.9594158722854));
#46419=CARTESIAN_POINT('Ctrl Pts',(1.9833073995402,2.17298314741028,10.9543553322567));
#46420=CARTESIAN_POINT('Ctrl Pts',(2.05538509733032,2.10719698080364,10.9490738795982));
#46421=CARTESIAN_POINT('Ctrl Pts',(2.12426418350433,2.03774953659513,10.9437924269398));
#46422=CARTESIAN_POINT('Ctrl Pts',(2.1895606759417,1.96499059701814,10.9385109742814));
#46423=CARTESIAN_POINT('Ctrl Pts',(2.25201606205986,1.89539746122778,10.9334593221522));
#46424=CARTESIAN_POINT('Ctrl Pts',(2.31119377002267,1.82277534227604,10.928407670023));
#46425=CARTESIAN_POINT('Ctrl Pts',(2.36679481678367,1.74746853912909,10.9233560178939));
#46426=CARTESIAN_POINT('Ctrl Pts',(2.4223772273332,1.6721869771168,10.9183060589641));
#46427=CARTESIAN_POINT('Ctrl Pts',(2.4743850971487,1.59422287358881,10.9132561000343));
#46428=CARTESIAN_POINT('Ctrl Pts',(2.52256048898002,1.51395263447602,10.9082061411045));
#46429=CARTESIAN_POINT('Ctrl Pts',(2.57073297109809,1.43368724355169,10.9031564871838));
#46430=CARTESIAN_POINT('Ctrl Pts',(2.61507320902485,1.35111637250567,10.8981068332631));
#46431=CARTESIAN_POINT('Ctrl Pts',(2.65536786073502,1.26664340845225,10.8930571793424));
#46432=CARTESIAN_POINT('Ctrl Pts',(2.69567115051051,1.18215233571813,10.8880064429148));
#46433=CARTESIAN_POINT('Ctrl Pts',(2.73192694188803,1.09575875826061,10.8829557064872));
#46434=CARTESIAN_POINT('Ctrl Pts',(2.76396938171704,1.00788752196399,10.8779049700595));
#46435=CARTESIAN_POINT('Ctrl Pts',(2.79604586983052,0.919922913724862,10.8728488667213));
#46436=CARTESIAN_POINT('Ctrl Pts',(2.82389991975566,0.830477927843595,10.867792763383));
#46437=CARTESIAN_POINT('Ctrl Pts',(2.84741517562019,0.739993795682003,10.8627366600447));
#46438=CARTESIAN_POINT('Ctrl Pts',(2.87094510473528,0.649453202457388,10.8576774017558));
#46439=CARTESIAN_POINT('Ctrl Pts',(2.89013075876966,0.557872603141818,10.8526181434669));
#46440=CARTESIAN_POINT('Ctrl Pts',(2.90490706649581,0.465702625097528,10.8475588851781));
#46441=CARTESIAN_POINT('Ctrl Pts',(2.91970550359378,0.373394610965105,10.8424920500161));
#46442=CARTESIAN_POINT('Ctrl Pts',(2.9300813658763,0.280495893871383,10.8374252148542));
#46443=CARTESIAN_POINT('Ctrl Pts',(2.936021514527,0.18746110592485,10.8323583796922));
#46444=CARTESIAN_POINT('Ctrl Pts',(2.93788084085319,0.158340280731397,10.8307724092795));
#46445=CARTESIAN_POINT('Ctrl Pts',(2.93930596103553,0.129206111948713,10.8291864388668));
#46446=CARTESIAN_POINT('Ctrl Pts',(2.94029751889039,0.100072475771473,10.8276004684541));
#46447=CARTESIAN_POINT('Ctrl Pts',(2.94346584595508,0.00698170195448691,
10.8225328135939));
#46448=CARTESIAN_POINT('Ctrl Pts',(2.94221421656088,-0.0864148034031075,
10.8174651587337));
#46449=CARTESIAN_POINT('Ctrl Pts',(2.9365089388319,-0.179664276249695,10.8123975038735));
#46450=CARTESIAN_POINT('Ctrl Pts',(2.93081115286242,-0.272791300609757,
10.8073365034924));
#46451=CARTESIAN_POINT('Ctrl Pts',(2.92067136891433,-0.365771239389406,
10.8022755031113));
#46452=CARTESIAN_POINT('Ctrl Pts',(2.90610787884632,-0.458149535094561,
10.7972145027302));
#46453=CARTESIAN_POINT('Ctrl Pts',(2.89091029493816,-0.55454997851267,10.7919331465723));
#46454=CARTESIAN_POINT('Ctrl Pts',(2.87089499576309,-0.650294708301221,
10.7866517904144));
#46455=CARTESIAN_POINT('Ctrl Pts',(2.84614326728887,-0.744870795551974,
10.7813704342565));
#46456=CARTESIAN_POINT('Ctrl Pts',(2.82246417805881,-0.835348339832311,
10.7763179505946));
#46457=CARTESIAN_POINT('Ctrl Pts',(2.79445075226464,-0.924755946327105,
10.7712654669328));
#46458=CARTESIAN_POINT('Ctrl Pts',(2.76222642396159,-1.01265452290915,10.7662129832709));
#46459=CARTESIAN_POINT('Ctrl Pts',(2.73001203106244,-1.10052599860482,10.7611620573907));
#46460=CARTESIAN_POINT('Ctrl Pts',(2.69358946727219,-1.18688895518827,10.7561111315104));
#46461=CARTESIAN_POINT('Ctrl Pts',(2.65313154084007,-1.2713209771728,10.7510602056302));
#46462=CARTESIAN_POINT('Ctrl Pts',(2.61267497758725,-1.35575015432579,10.7460094499345));
#46463=CARTESIAN_POINT('Ctrl Pts',(2.56818351321817,-1.43824812881357,10.7409586942389));
#46464=CARTESIAN_POINT('Ctrl Pts',(2.51987699422717,-1.51841494130051,10.7359079385433));
#46465=CARTESIAN_POINT('Ctrl Pts',(2.47155883699479,-1.59860106796563,10.7308559659951));
#46466=CARTESIAN_POINT('Ctrl Pts',(2.41942402710974,-1.67645453945573,10.7258039934469));
#46467=CARTESIAN_POINT('Ctrl Pts',(2.36373642214545,-1.75160330172761,10.7207520208986));
#46468=CARTESIAN_POINT('Ctrl Pts',(2.30798751091064,-1.82683479498335,10.7156944866532));
#46469=CARTESIAN_POINT('Ctrl Pts',(2.24867826160286,-1.89935528174567,10.7106369524078));
#46470=CARTESIAN_POINT('Ctrl Pts',(2.18611341615223,-1.96882506376753,10.7055794181624));
#46471=CARTESIAN_POINT('Ctrl Pts',(2.12350812171701,-2.0383397589051,10.7005186141555));
#46472=CARTESIAN_POINT('Ctrl Pts',(2.05764335060496,-2.10479950960304,10.6954578101485));
#46473=CARTESIAN_POINT('Ctrl Pts',(1.98885985606428,-2.16790232089363,10.6903970061416));
#46474=CARTESIAN_POINT('Ctrl Pts',(1.9199712252722,-2.23110158545511,10.6853284666457));
#46475=CARTESIAN_POINT('Ctrl Pts',(1.8481553052694,-2.29093338834345,10.6802599271498));
#46476=CARTESIAN_POINT('Ctrl Pts',(1.77378471914451,-2.34713693041744,10.6751913876539));
#46477=CARTESIAN_POINT('Ctrl Pts',(1.75065309294903,-2.36461802602068,10.6736149100828));
#46478=CARTESIAN_POINT('Ctrl Pts',(1.72727452462674,-2.38174844474552,10.6720384325117));
#46479=CARTESIAN_POINT('Ctrl Pts',(1.70366073469359,-2.3985212321477,10.6704619549406));
#46480=CARTESIAN_POINT('Ctrl Pts',(1.62797700284765,-2.45227910615473,10.6654092418398));
#46481=CARTESIAN_POINT('Ctrl Pts',(1.54961172748861,-2.50254685608309,10.6603565287391));
#46482=CARTESIAN_POINT('Ctrl Pts',(1.46892045792133,-2.54904623110295,10.6553038156384));
#46483=CARTESIAN_POINT('Ctrl Pts',(1.38833960322827,-2.59548197814086,10.6502580164787));
#46484=CARTESIAN_POINT('Ctrl Pts',(1.30543946062863,-2.63815937727123,10.6452122173191));
#46485=CARTESIAN_POINT('Ctrl Pts',(1.22060601730583,-2.67684234696719,10.6401664181594));
#46486=CARTESIAN_POINT('Ctrl Pts',(1.13174887977234,-2.71736006997648,10.6348812941289));
#46487=CARTESIAN_POINT('Ctrl Pts',(1.04077090544082,-2.75349478101027,10.6295961700984));
#46488=CARTESIAN_POINT('Ctrl Pts',(0.948146751141357,-2.78502813958856,
10.6243110460678));
#46489=CARTESIAN_POINT('Ctrl Pts',(0.8598755379332,-2.81507956450342,10.619274300376));
#46490=CARTESIAN_POINT('Ctrl Pts',(0.7701098414749,-2.84095216925188,10.6142375546841));
#46491=CARTESIAN_POINT('Ctrl Pts',(0.679281289723433,-2.86250605753624,
10.6092008089923));
#46492=CARTESIAN_POINT('Ctrl Pts',(0.588483774261536,-2.88405258081582,
10.604165784366));
#46493=CARTESIAN_POINT('Ctrl Pts',(0.49662455678125,-2.90128321708858,10.5991307597398));
#46494=CARTESIAN_POINT('Ctrl Pts',(0.404148771699878,-2.91410840058044,
10.5940957351136));
#46495=CARTESIAN_POINT('Ctrl Pts',(0.311678736658876,-2.92693278661681,
10.5890610235595));
#46496=CARTESIAN_POINT('Ctrl Pts',(0.218592650212067,-2.93535220400183,
10.5840263120055));
#46497=CARTESIAN_POINT('Ctrl Pts',(0.125343007597342,-2.93932868703833,
10.5789916004514));
#46498=CARTESIAN_POINT('Ctrl Pts',(0.0320730981095047,-2.94330603432347,
10.5739557946534));
#46499=CARTESIAN_POINT('Ctrl Pts',(-0.0613599944895516,-2.94283851101469,
10.5689199888553));
#46500=CARTESIAN_POINT('Ctrl Pts',(-0.154502669429059,-2.93794025213912,
10.5638841830573));
#46501=CARTESIAN_POINT('Ctrl Pts',(-0.247746501442313,-2.93303667353729,
10.5588429081509));
#46502=CARTESIAN_POINT('Ctrl Pts',(-0.340698842298211,-2.92369277946677,
10.5538016332446));
#46503=CARTESIAN_POINT('Ctrl Pts',(-0.432910463523054,-2.90997466150004,
10.5487603583382));
#46504=CARTESIAN_POINT('Ctrl Pts',(-0.525180571250394,-2.8962478426263,
10.5437158859332));
#46505=CARTESIAN_POINT('Ctrl Pts',(-0.616708588991816,-2.87814136307095,
10.5386714135281));
#46506=CARTESIAN_POINT('Ctrl Pts',(-0.707056849449534,-2.85577215681617,
10.5336269411231));
#46507=CARTESIAN_POINT('Ctrl Pts',(-0.797544146141969,-2.83336852676402,
10.5285747058187));
#46508=CARTESIAN_POINT('Ctrl Pts',(-0.886847637795464,-2.80668920528993,
10.5235224705143));
#46509=CARTESIAN_POINT('Ctrl Pts',(-0.974546437944797,-2.77590043774792,
10.51847023521));
#46510=CARTESIAN_POINT('Ctrl Pts',(-1.00432649978491,-2.76544543266438,
10.5167546372823));
#46511=CARTESIAN_POINT('Ctrl Pts',(-1.03392171338596,-2.75451697308154,
10.5150390393547));
#46512=CARTESIAN_POINT('Ctrl Pts',(-1.06331621815642,-2.74312278620654,
10.513323441427));
#46513=CARTESIAN_POINT('Ctrl Pts',(-1.15002978885464,-2.70951001957381,
10.5082624402857));
#46514=CARTESIAN_POINT('Ctrl Pts',(-1.23529755708651,-2.6717235695059,10.5032014391445));
#46515=CARTESIAN_POINT('Ctrl Pts',(-1.31869056571622,-2.62990859002571,
10.4981404380032));
#46516=CARTESIAN_POINT('Ctrl Pts',(-1.4019713265358,-2.58814989391933,10.4930862490193));
#46517=CARTESIAN_POINT('Ctrl Pts',(-1.48338195050866,-2.54237364151342,
10.4880320600354));
#46518=CARTESIAN_POINT('Ctrl Pts',(-1.56251207205325,-2.49277356065244,
10.4829778710514));
#46519=CARTESIAN_POINT('Ctrl Pts',(-1.64522515283805,-2.44092762114034,
10.477694831754));
#46520=CARTESIAN_POINT('Ctrl Pts',(-1.72544586872966,-2.38490355231225,
10.4724117924566));
#46521=CARTESIAN_POINT('Ctrl Pts',(-1.80273259262423,-2.32497724709089,
10.4671287531592));
#46522=CARTESIAN_POINT('Ctrl Pts',(-1.87654180176376,-2.26774732489783,
10.4620834241202));
#46523=CARTESIAN_POINT('Ctrl Pts',(-1.94767494127508,-2.20695902974395,
10.4570380950812));
#46524=CARTESIAN_POINT('Ctrl Pts',(-2.01577695263679,-2.14289693574338,
10.4519927660422));
#46525=CARTESIAN_POINT('Ctrl Pts',(-2.08385644498234,-2.07885602489585,
10.4469491053217));
#46526=CARTESIAN_POINT('Ctrl Pts',(-2.14890647874785,-2.01154376905216,
10.4419054446012));
#46527=CARTESIAN_POINT('Ctrl Pts',(-2.21060663169751,-1.94128367836723,
10.4368617838807));
#46528=CARTESIAN_POINT('Ctrl Pts',(-2.27230346586229,-1.87102736689702,
10.4318183944532));
#46529=CARTESIAN_POINT('Ctrl Pts',(-2.33065048599045,-1.79782386866528,
10.4267750050258));
#46530=CARTESIAN_POINT('Ctrl Pts',(-2.38536632740192,-1.72203120880462,
10.4217316155984));
#46531=CARTESIAN_POINT('Ctrl Pts',(-2.44009437491711,-1.64622164098742,
10.416687101083));
#46532=CARTESIAN_POINT('Ctrl Pts',(-2.49118937616854,-1.56782212316922,
10.4116425865677));
#46533=CARTESIAN_POINT('Ctrl Pts',(-2.53841286756387,-1.48722026404502,
10.4065980720523));
#46534=CARTESIAN_POINT('Ctrl Pts',(-2.58568753408577,-1.40653105834352,
10.4015480909003));
#46535=CARTESIAN_POINT('Ctrl Pts',(-2.62908209378073,-1.32363513043131,
10.3964981097482));
#46536=CARTESIAN_POINT('Ctrl Pts',(-2.66840386797062,-1.23894503405092,
10.3914481285962));
#46537=CARTESIAN_POINT('Ctrl Pts',(-2.70775060717982,-1.15420116873627,
10.3863949412593));
#46538=CARTESIAN_POINT('Ctrl Pts',(-2.74301924617896,-1.06766127635864,
10.3813417539225));
#46539=CARTESIAN_POINT('Ctrl Pts',(-2.77406590736742,-0.979756266416189,
10.3762885665856));
#46540=CARTESIAN_POINT('Ctrl Pts',(-2.80515990044789,-0.891717241726933,
10.37122767546));
#46541=CARTESIAN_POINT('Ctrl Pts',(-2.83201894283078,-0.802309368669151,
10.3661667843344));
#46542=CARTESIAN_POINT('Ctrl Pts',(-2.85454955267706,-0.711976721045849,
10.3611058932088));
#46543=CARTESIAN_POINT('Ctrl Pts',(-2.86185211042732,-0.682698357943202,
10.3594655714437));
#46544=CARTESIAN_POINT('Ctrl Pts',(-2.86870036250045,-0.653322905436628,
10.3578252496786));
#46545=CARTESIAN_POINT('Ctrl Pts',(-2.87509229263909,-0.623865617587072,
10.3561849279135));
#46546=CARTESIAN_POINT('Ctrl Pts',(-2.90197412367268,-0.499980372050345,
10.3492864087535));
#46547=CARTESIAN_POINT('Ctrl Pts',(-2.92085641814638,-0.374303537995701,
10.3423878895935));
#46548=CARTESIAN_POINT('Ctrl Pts',(-2.9315534651542,-0.247706037355537,
10.3354893704335));
#46549=CARTESIAN_POINT('Ctrl Pts',(-2.93843477274814,-0.166267081175227,
10.3310516193189));
#46550=CARTESIAN_POINT('Ctrl Pts',(-2.94192972963076,-0.0844474714313159,
10.3266138682042));
#46551=CARTESIAN_POINT('Ctrl Pts',(-2.94199895080427,-0.00248464616942429,
10.3221761170896));
#46552=CARTESIAN_POINT('',(-2.93787859032851,0.00118007037484616,9.3221761170896));
#46553=CARTESIAN_POINT('Ctrl Pts',(-2.9424244111198,-0.00248111071493722,
10.3221759062437));
#46554=CARTESIAN_POINT('Ctrl Pts',(-2.93565894065101,0.755679485053147,
10.2811327422958));
#46555=CARTESIAN_POINT('Ctrl Pts',(-2.25296184349933,2.49216616011857,10.1877100738435));
#46556=CARTESIAN_POINT('Ctrl Pts',(0.655114493273779,3.40289939669596,10.0419079008864));
#46557=CARTESIAN_POINT('Ctrl Pts',(3.20077001198984,1.32799366090116,9.88476938737303));
#46558=CARTESIAN_POINT('Ctrl Pts',(2.87168850378309,-1.93961114588259,9.72763087385946));
#46559=CARTESIAN_POINT('Ctrl Pts',(-0.0366657672895371,-3.46516125435104,
9.57049236034596));
#46560=CARTESIAN_POINT('Ctrl Pts',(-2.50974118686153,-2.10044319083052,
9.43534077475601));
#46561=CARTESIAN_POINT('Ctrl Pts',(-2.93580007289335,-0.56247072784923,
9.35256869367055));
#46562=CARTESIAN_POINT('Ctrl Pts',(-2.93787859032851,0.00118007037484616,
9.3221761170896));
#46563=CARTESIAN_POINT('',(-2.94622250669394,0.000937675328142526,8.3221761170896));
#46564=CARTESIAN_POINT('Ctrl Pts',(-2.93787859032851,0.00118007037484616,
9.3221761170896));
#46565=CARTESIAN_POINT('Ctrl Pts',(-2.93938225399168,0.408942454113454,
9.30018918916604));
#46566=CARTESIAN_POINT('Ctrl Pts',(-2.67122390572782,1.78622760720654,9.22582275673799));
#46567=CARTESIAN_POINT('Ctrl Pts',(-0.582935293544531,3.41596954985009,
9.09907681980543));
#46568=CARTESIAN_POINT('Ctrl Pts',(2.52967359714472,2.36841856552379,8.9419383062919));
#46569=CARTESIAN_POINT('Ctrl Pts',(3.37023102179741,-0.80635131037091,8.7847997927784));
#46570=CARTESIAN_POINT('Ctrl Pts',(1.18377939294799,-3.25688886436588,8.62766127926488));
#46571=CARTESIAN_POINT('Ctrl Pts',(-2.00528952627767,-2.7910698384739,8.47345338736861));
#46572=CARTESIAN_POINT('Ctrl Pts',(-2.94237161798714,-0.909460413780999,
8.37162499997686));
#46573=CARTESIAN_POINT('Ctrl Pts',(-2.94622250669394,0.000937675328142526,
8.3221761170896));
#46574=CARTESIAN_POINT('',(-2.93998607517527,-0.0023358300504342,7.3221761170896));
#46575=CARTESIAN_POINT('Ctrl Pts',(-2.94622250669394,0.000937675328142526,
8.3221761170896));
#46576=CARTESIAN_POINT('Ctrl Pts',(-2.94645073222768,0.0548930361868928,
8.31924549547236));
#46577=CARTESIAN_POINT('Ctrl Pts',(-2.92084742177771,1.07298108248981,8.26393536935057));
#46578=CARTESIAN_POINT('Ctrl Pts',(-1.74654067132516,2.9930342700521,8.15624573872437));
#46579=CARTESIAN_POINT('Ctrl Pts',(1.53565755714061,3.10651158777757,7.99910722521081));
#46580=CARTESIAN_POINT('Ctrl Pts',(3.43858888024392,0.429842977951656,7.84196871169733));
#46581=CARTESIAN_POINT('Ctrl Pts',(2.25311553735072,-2.63289362024366,7.6848301981838));
#46582=CARTESIAN_POINT('Ctrl Pts',(-0.956017138014639,-3.33086920560932,
7.52769168467029));
#46583=CARTESIAN_POINT('Ctrl Pts',(-2.76420883197108,-1.56637023902252,
7.40680699097222));
#46584=CARTESIAN_POINT('Ctrl Pts',(-2.94227697960606,-0.300857412821767,
7.33830180177866));
#46585=CARTESIAN_POINT('Ctrl Pts',(-2.93998607517527,-0.0023358300504342,
7.3221761170896));
#46586=CARTESIAN_POINT('',(-2.93949980478958,0.00219056232359141,6.3221761170896));
#46587=CARTESIAN_POINT('Ctrl Pts',(-2.93998607517527,-0.0023358300504342,
7.3221761170896));
#46588=CARTESIAN_POINT('Ctrl Pts',(-2.93483565594967,0.668801419715884,
7.28592229727415));
#46589=CARTESIAN_POINT('Ctrl Pts',(-2.3759760729603,2.31735690151427,7.1972889729542));
#46590=CARTESIAN_POINT('Ctrl Pts',(0.345621576330101,3.44807252913396,7.05627614412975));
#46591=CARTESIAN_POINT('Ctrl Pts',(3.06802702248428,1.61116995727812,6.89913763061623));
#46592=CARTESIAN_POINT('Ctrl Pts',(3.03485183459052,-1.67282180255627,6.74199911710273));
#46593=CARTESIAN_POINT('Ctrl Pts',(0.275892655912197,-3.45435112336391,
6.5848606035892));
#46594=CARTESIAN_POINT('Ctrl Pts',(-2.40179787617368,-2.2778948585372,6.44491960358484));
#46595=CARTESIAN_POINT('Ctrl Pts',(-2.93486858555413,-0.649377666932483,
6.35735810808496));
#46596=CARTESIAN_POINT('Ctrl Pts',(-2.93949980478958,0.00219056232359141,
6.3221761170896));
#46597=CARTESIAN_POINT('',(-2.94644869531747,-0.000604754645607275,5.3221761170896));
#46598=CARTESIAN_POINT('Ctrl Pts',(-2.93949980478958,0.00219056232359141,
6.3221761170896));
#46599=CARTESIAN_POINT('Ctrl Pts',(-2.94176361798241,0.320687415620876,
6.30497860358046));
#46600=CARTESIAN_POINT('Ctrl Pts',(-2.74834588968967,1.60657553764138,6.23540158556681));
#46601=CARTESIAN_POINT('Ctrl Pts',(-0.88853140270286,3.34950300605666,6.11344506304867));
#46602=CARTESIAN_POINT('Ctrl Pts',(2.30584575575064,2.5868385708981,5.95630654953516));
#46603=CARTESIAN_POINT('Ctrl Pts',(3.42920337545963,-0.49922204570182,5.79916803602163));
#46604=CARTESIAN_POINT('Ctrl Pts',(1.47258603363213,-3.13690114838419,5.64202952250812));
#46605=CARTESIAN_POINT('Ctrl Pts',(-1.80664989208077,-2.95713959911128,
5.48489100899462));
#46606=CARTESIAN_POINT('Ctrl Pts',(-2.9306284478891,-1.03309719749912,5.37827320718843));
#46607=CARTESIAN_POINT('Ctrl Pts',(-2.94654631348559,-0.0348197596345374,
5.32403490988676));
#46608=CARTESIAN_POINT('Ctrl Pts',(-2.94644869531747,-0.000604754645607275,
5.3221761170896));
#46609=CARTESIAN_POINT('',(-2.93815144027097,-0.00144838940242836,4.32217611708959));
#46610=CARTESIAN_POINT('Ctrl Pts',(-2.94644869531747,-0.000604754645607275,
5.3221761170896));
#46611=CARTESIAN_POINT('Ctrl Pts',(-2.94379550054715,0.929335583914262,
5.27165540538226));
#46612=CARTESIAN_POINT('Ctrl Pts',(-1.9707214474043,2.82822213535154,5.16875518917042));
#46613=CARTESIAN_POINT('Ctrl Pts',(1.24933397805705,3.23230924456063,5.01347546845408));
#46614=CARTESIAN_POINT('Ctrl Pts',(3.38583301773346,0.738101088738995,4.85633695494055));
#46615=CARTESIAN_POINT('Ctrl Pts',(2.48131063733585,-2.41904029776208,4.69919844142705));
#46616=CARTESIAN_POINT('Ctrl Pts',(-0.651826904677944,-3.40349528097658,
4.54205992791354));
#46617=CARTESIAN_POINT('Ctrl Pts',(-2.68938574184905,-1.74603534949716,
4.41638581980104));
#46618=CARTESIAN_POINT('Ctrl Pts',(-2.93991718809614,-0.389242894153138,
4.34309121619307));
#46619=CARTESIAN_POINT('Ctrl Pts',(-2.93815144027097,-0.00144838940242836,
4.32217611708959));
#46620=CARTESIAN_POINT('',(-2.94188729812012,0.00254759896953657,3.32217611708959));
#46621=CARTESIAN_POINT('Ctrl Pts',(-2.93815144027097,-0.00144838940242836,
4.32217611708959));
#46622=CARTESIAN_POINT('Ctrl Pts',(-2.93549507201127,0.581944663119171,
4.29071171168856));
#46623=CARTESIAN_POINT('Ctrl Pts',(-2.48662477666494,2.1402933973268,4.20686780178306));
#46624=CARTESIAN_POINT('Ctrl Pts',(0.0333505152944463,3.46519064195022,
4.07064438737298));
#46625=CARTESIAN_POINT('Ctrl Pts',(2.91027678633436,1.88120904397026,3.91350587385948));
#46626=CARTESIAN_POINT('Ctrl Pts',(3.17330745213008,-1.39240017768036,3.75636736034596));
#46627=CARTESIAN_POINT('Ctrl Pts',(0.586198762341217,-3.41541058398189,
3.59922884683245));
#46628=CARTESIAN_POINT('Ctrl Pts',(-2.28155114480077,-2.45331685892863,
3.45449843241366));
#46629=CARTESIAN_POINT('Ctrl Pts',(-2.93534805643284,-0.736191897535303,
3.36214752249938));
#46630=CARTESIAN_POINT('Ctrl Pts',(-2.94188729812012,0.00254759896953657,
3.32217611708959));
#46631=CARTESIAN_POINT('',(-2.94199938418253,-0.00190354132858995,2.32217611708959));
#46632=CARTESIAN_POINT('Ctrl Pts',(-2.94188729812012,0.00254759896953657,
3.32217611708959));
#46633=CARTESIAN_POINT('Ctrl Pts',(-2.94391723822425,0.231870355671395,
3.30976801799487));
#46634=CARTESIAN_POINT('Ctrl Pts',(-2.8154264390555,1.42700723566272,3.24498041439567));
#46635=CARTESIAN_POINT('Ctrl Pts',(-1.18688998506612,3.25575653825376,3.1278133062919));
#46636=CARTESIAN_POINT('Ctrl Pts',(2.06323722577403,2.78418938435942,2.9706747927784));
#46637=CARTESIAN_POINT('Ctrl Pts',(3.4602462989487,-0.188026617557372,2.81353627926488));
#46638=CARTESIAN_POINT('Ctrl Pts',(1.74939887098719,-2.99136460950402,2.65639776575137));
#46639=CARTESIAN_POINT('Ctrl Pts',(-1.53268946892132,-3.1079769880761,2.49925925223785));
#46640=CARTESIAN_POINT('Ctrl Pts',(-2.88363156232728,-1.21157661749859,
2.38785203601727));
#46641=CARTESIAN_POINT('Ctrl Pts',(-2.94579921760659,-0.124453265927633,
2.32882432430118));
#46642=CARTESIAN_POINT('Ctrl Pts',(-2.94487182720719,-0.00190539986535287,
2.32217611708959));
#46643=CARTESIAN_POINT('',(-2.94199999670507,-0.000139238540415516,1.32217611711858));
#46644=CARTESIAN_POINT('Ctrl Pts',(-2.94199938418253,-0.00190354132858995,
2.32217611708959));
#46645=CARTESIAN_POINT('Ctrl Pts',(-2.94205878758215,0.0899067926258124,
2.31719052791049));
#46646=CARTESIAN_POINT('Ctrl Pts',(-2.93781632057424,0.181878623548529,
2.31220493873139));
#46647=CARTESIAN_POINT('Ctrl Pts',(-2.92925308992623,0.273569616656554,
2.30721934955229));
#46648=CARTESIAN_POINT('Ctrl Pts',(-2.92050500409423,0.367239950985021,
2.30212613603806));
#46649=CARTESIAN_POINT('Ctrl Pts',(-2.90724736516512,0.460616705008599,
2.29703292252383));
#46650=CARTESIAN_POINT('Ctrl Pts',(-2.88951627230318,0.553226637188741,
2.29193970900961));
#46651=CARTESIAN_POINT('Ctrl Pts',(-2.87219424854482,0.643699991424419,
2.28696399960541));
#46652=CARTESIAN_POINT('Ctrl Pts',(-2.85060304408045,0.73344104896173,2.28198829020122));
#46653=CARTESIAN_POINT('Ctrl Pts',(-2.82482866310374,0.822014004812291,
2.27701258079702));
#46654=CARTESIAN_POINT('Ctrl Pts',(-2.79906463001987,0.910551400411887,
2.27203886903955));
#46655=CARTESIAN_POINT('Ctrl Pts',(-2.76912088217163,0.997921187859738,
2.26706515728208));
#46656=CARTESIAN_POINT('Ctrl Pts',(-2.73513396050232,1.08370024365914,2.26209144552461));
#46657=CARTESIAN_POINT('Ctrl Pts',(-2.70115061564178,1.16947027200728,2.25711825720424));
#46658=CARTESIAN_POINT('Ctrl Pts',(-2.66312511112893,1.25364947741371,2.25214506888387));
#46659=CARTESIAN_POINT('Ctrl Pts',(-2.62124258581226,1.33583356235881,2.2471718805635));
#46660=CARTESIAN_POINT('Ctrl Pts',(-2.57759754955394,1.42147613859236,2.24198940928411));
#46661=CARTESIAN_POINT('Ctrl Pts',(-2.5297639388273,1.50495148822779,2.23680693800472));
#46662=CARTESIAN_POINT('Ctrl Pts',(-2.4780040829923,1.58583093823821,2.23162446672534));
#46663=CARTESIAN_POINT('Ctrl Pts',(-2.42827199765954,1.6635418136782,2.2266450265831));
#46664=CARTESIAN_POINT('Ctrl Pts',(-2.37491586195325,1.73885602980887,2.22166558644086));
#46665=CARTESIAN_POINT('Ctrl Pts',(-2.31821134187879,1.81142490166844,2.21668614629863));
#46666=CARTESIAN_POINT('Ctrl Pts',(-2.26146982595984,1.88404111978356,2.21170345741021));
#46667=CARTESIAN_POINT('Ctrl Pts',(-2.20137587817613,1.95390808672331,2.20672076852179));
#46668=CARTESIAN_POINT('Ctrl Pts',(-2.13824331096343,2.02071263249383,2.20173807963337));
#46669=CARTESIAN_POINT('Ctrl Pts',(-2.07501857247312,2.08761471049859,2.19674811619837));
#46670=CARTESIAN_POINT('Ctrl Pts',(-2.008746697179,2.15144513885915,2.19175815276337));
#46671=CARTESIAN_POINT('Ctrl Pts',(-1.93977543542689,2.21193021140235,2.18676818932838));
#46672=CARTESIAN_POINT('Ctrl Pts',(-1.9315469049486,2.21914630764678,2.18617286795586));
#46673=CARTESIAN_POINT('Ctrl Pts',(-1.92327998722939,2.22631483862489,2.18557754658335));
#46674=CARTESIAN_POINT('Ctrl Pts',(-1.91497529975521,2.23343538105033,2.18498222521083));
#46675=CARTESIAN_POINT('Ctrl Pts',(-1.84439708423493,2.2939500216658,2.17992282709816));
#46676=CARTESIAN_POINT('Ctrl Pts',(-1.77082529385272,2.3512207736073,2.17486342898548));
#46677=CARTESIAN_POINT('Ctrl Pts',(-1.69459024701272,2.40493823095924,2.1698040308728));
#46678=CARTESIAN_POINT('Ctrl Pts',(-1.61845798842576,2.45858326068338,2.1647514543824));
#46679=CARTESIAN_POINT('Ctrl Pts',(-1.53966996865168,2.50868426408285,2.15969887789199));
#46680=CARTESIAN_POINT('Ctrl Pts',(-1.45859054654746,2.55497115786507,2.15464630140159));
#46681=CARTESIAN_POINT('Ctrl Pts',(-1.37380640461788,2.60337301458856,2.14936286016391));
#46682=CARTESIAN_POINT('Ctrl Pts',(-1.2865168312337,2.64760356830585,2.14407941892623));
#46683=CARTESIAN_POINT('Ctrl Pts',(-1.19717389059228,2.68740370537888,2.13879597768856));
#46684=CARTESIAN_POINT('Ctrl Pts',(-1.11188488670734,2.72539791086476,2.13375227264582));
#46685=CARTESIAN_POINT('Ctrl Pts',(-1.02472524270107,2.75935477790647,2.12870856760308));
#46686=CARTESIAN_POINT('Ctrl Pts',(-0.936113283859184,2.78909589648373,
2.12366486256034));
#46687=CARTESIAN_POINT('Ctrl Pts',(-0.847530646881758,2.81882717366871,
2.11862282648912));
#46688=CARTESIAN_POINT('Ctrl Pts',(-0.75749706931278,2.84434533342064,2.1135807904179));
#46689=CARTESIAN_POINT('Ctrl Pts',(-0.666448831070414,2.86552088730215,
2.10853875434668));
#46690=CARTESIAN_POINT('Ctrl Pts',(-0.575405464769122,2.88669530809143,
2.10349698807204));
#46691=CARTESIAN_POINT('Ctrl Pts',(-0.483347977108855,2.90352748529881,
2.09845522179739));
#46692=CARTESIAN_POINT('Ctrl Pts',(-0.390724613048398,2.91593866135044,
2.09341345552275));
#46693=CARTESIAN_POINT('Ctrl Pts',(-0.298080512743564,2.92835261597939,
2.0883705605124));
#46694=CARTESIAN_POINT('Ctrl Pts',(-0.204870723203345,2.93634354517789,
2.08332766550206));
#46695=CARTESIAN_POINT('Ctrl Pts',(-0.111549287758481,2.93988448011152,
2.07828477049171));
#46696=CARTESIAN_POINT('Ctrl Pts',(-0.0181264186579392,2.94342926378551,
2.07323639421896));
#46697=CARTESIAN_POINT('Ctrl Pts',(0.0754078955767428,2.9425143834227,2.06818801794621));
#46698=CARTESIAN_POINT('Ctrl Pts',(0.168599266171156,2.93716500854932,2.06313964167345));
#46699=CARTESIAN_POINT('Ctrl Pts',(0.261849944904348,2.93181222926773,2.05808805255171));
#46700=CARTESIAN_POINT('Ctrl Pts',(0.354756805729905,2.92201938341522,2.05303646342997));
#46701=CARTESIAN_POINT('Ctrl Pts',(0.446872353772485,2.90786332200017,2.04798487430823));
#46702=CARTESIAN_POINT('Ctrl Pts',(0.539128802992504,2.89368560728375,2.04292555820803));
#46703=CARTESIAN_POINT('Ctrl Pts',(0.630591090874431,2.87513144513155,2.03786624210784));
#46704=CARTESIAN_POINT('Ctrl Pts',(0.720823945817723,2.85232831895905,2.03280692600764));
#46705=CARTESIAN_POINT('Ctrl Pts',(0.750330239293404,2.84487165881645,2.03115252123753));
#46706=CARTESIAN_POINT('Ctrl Pts',(0.779705209996882,2.83696104752962,2.02949811646742));
#46707=CARTESIAN_POINT('Ctrl Pts',(0.808934084771822,2.82860206577284,2.02784371169731));
#46708=CARTESIAN_POINT('Ctrl Pts',(0.898320175890856,2.80303910070057,2.02278430463265));
#46709=CARTESIAN_POINT('Ctrl Pts',(0.986648264179951,2.77319068607448,2.01772489756798));
#46710=CARTESIAN_POINT('Ctrl Pts',(1.07347815233169,2.73916203545291,2.01266549050331));
#46711=CARTESIAN_POINT('Ctrl Pts',(1.16019096843477,2.70517926539075,2.00761290499701));
#46712=CARTESIAN_POINT('Ctrl Pts',(1.24540918999726,2.6670276205544,2.00256031949071));
#46713=CARTESIAN_POINT('Ctrl Pts',(1.32870668331679,2.6248623868137,1.9975077339844));
#46714=CARTESIAN_POINT('Ctrl Pts',(1.41581005317874,2.58077061641979,1.99222429499271));
#46715=CARTESIAN_POINT('Ctrl Pts',(1.50081251730368,2.53228987076498,1.98694085600102));
#46716=CARTESIAN_POINT('Ctrl Pts',(1.5832487812635,2.47965467285823,1.98165741700933));
#46717=CARTESIAN_POINT('Ctrl Pts',(1.66194467455955,2.42940768543889,1.97661370285788));
#46718=CARTESIAN_POINT('Ctrl Pts',(1.73830173591452,2.37537527927245,1.97156998870644));
#46719=CARTESIAN_POINT('Ctrl Pts',(1.81194060728049,2.31780828277232,1.96652627455499));
#46720=CARTESIAN_POINT('Ctrl Pts',(1.88555511165802,2.26026033510215,1.96148422936075));
#46721=CARTESIAN_POINT('Ctrl Pts',(1.95645286468793,2.19918039345385,1.9564421841665));
#46722=CARTESIAN_POINT('Ctrl Pts',(2.02428544472045,2.13486122225613,1.95140013897226));
#46723=CARTESIAN_POINT('Ctrl Pts',(2.0921143951082,2.07054549270463,1.94635836357216));
#46724=CARTESIAN_POINT('Ctrl Pts',(2.15687817772981,2.0029911832811,1.94131658817205));
#46725=CARTESIAN_POINT('Ctrl Pts',(2.21826411704521,1.93252899254568,1.93627481277195));
#46726=CARTESIAN_POINT('Ctrl Pts',(2.2796637991228,1.86205102710451,1.93123190864562));
#46727=CARTESIAN_POINT('Ctrl Pts',(2.33768384541717,1.78866422134694,1.92618900451928));
#46728=CARTESIAN_POINT('Ctrl Pts',(2.3920516066775,1.71273264434108,1.92114610039294));
#46729=CARTESIAN_POINT('Ctrl Pts',(2.44647846095373,1.63671853633187,1.91609771506953));
#46730=CARTESIAN_POINT('Ctrl Pts',(2.4972448496801,1.55815449742095,1.91104932974613));
#46731=CARTESIAN_POINT('Ctrl Pts',(2.54412144579094,1.47743360902162,1.90600094442272));
#46732=CARTESIAN_POINT('Ctrl Pts',(2.59102787443685,1.39666134938516,1.90094934627789));
#46733=CARTESIAN_POINT('Ctrl Pts',(2.63403937864078,1.31372990014908,1.89589774813306));
#46734=CARTESIAN_POINT('Ctrl Pts',(2.67297356051088,1.22905506174856,1.89084614998823));
#46735=CARTESIAN_POINT('Ctrl Pts',(2.71196729562918,1.14425070575131,1.88578682498069));
#46736=CARTESIAN_POINT('Ctrl Pts',(2.74687109648308,1.05769804824939,1.88072749997314));
#46737=CARTESIAN_POINT('Ctrl Pts',(2.7775515549006,0.969830583075863,1.8756681749656));
#46738=CARTESIAN_POINT('Ctrl Pts',(2.78758361797581,0.941099201657635,1.87401384937167));
#46739=CARTESIAN_POINT('Ctrl Pts',(2.79716452718351,0.91222733972703,1.87235952377774));
#46740=CARTESIAN_POINT('Ctrl Pts',(2.80629080157345,0.883230398596102,1.87070519818381));
#46741=CARTESIAN_POINT('Ctrl Pts',(2.83420143639891,0.794549848310172,1.86564581956316));
#46742=CARTESIAN_POINT('Ctrl Pts',(2.85795278857554,0.704391329236729,1.86058644094251));
#46743=CARTESIAN_POINT('Ctrl Pts',(2.87739015045553,0.613180170962414,1.85552706232187));
#46744=CARTESIAN_POINT('Ctrl Pts',(2.89680130479238,0.52209199338784,1.85047450529997));
#46745=CARTESIAN_POINT('Ctrl Pts',(2.91190993682756,0.429954426689562,1.84542194827807));
#46746=CARTESIAN_POINT('Ctrl Pts',(2.92261087498168,0.337208649709403,1.84036939125617));
#46747=CARTESIAN_POINT('Ctrl Pts',(2.93380081896342,0.240224625130997,1.83508594514843));
#46748=CARTESIAN_POINT('Ctrl Pts',(2.9401704609242,0.142575941416614,1.82980249904068));
#46749=CARTESIAN_POINT('Ctrl Pts',(2.94165918157964,0.0447801231376263,
1.82451905293294));
#46750=CARTESIAN_POINT('Ctrl Pts',(2.9430803447815,-0.0485777662194173,
1.81947536716159));
#46751=CARTESIAN_POINT('Ctrl Pts',(2.94005389202632,-0.142069231699168,
1.81443168139025));
#46752=CARTESIAN_POINT('Ctrl Pts',(2.93258015749533,-0.235239494695669,
1.8093879956189));
#46753=CARTESIAN_POINT('Ctrl Pts',(2.92510889587937,-0.328378929443869,
1.80434597870618));
#46754=CARTESIAN_POINT('Ctrl Pts',(2.91319331168689,-0.421196931931897,
1.79930396179347));
#46755=CARTESIAN_POINT('Ctrl Pts',(2.89688578062519,-0.513241438322724,
1.79426194488075));
#46756=CARTESIAN_POINT('Ctrl Pts',(2.88057912173122,-0.605281021942152,
1.78922019762776));
#46757=CARTESIAN_POINT('Ctrl Pts',(2.85988106080887,-0.696546755862382,
1.78417845037477));
#46758=CARTESIAN_POINT('Ctrl Pts',(2.83489532504749,-0.786595509791323,
1.77913670312179));
#46759=CARTESIAN_POINT('Ctrl Pts',(2.80990399473482,-0.876664426519443,
1.77409382697214));
#46760=CARTESIAN_POINT('Ctrl Pts',(2.78062320144801,-0.965515395581965,
1.76905095082249));
#46761=CARTESIAN_POINT('Ctrl Pts',(2.74720657326158,-1.05272030655267,1.76400807467285));
#46762=CARTESIAN_POINT('Ctrl Pts',(2.71375362120272,-1.14002000925535,1.75895971691719));
#46763=CARTESIAN_POINT('Ctrl Pts',(2.67615602077653,-1.22566966905998,1.75391135916153));
#46764=CARTESIAN_POINT('Ctrl Pts',(2.63461547956147,-1.30926134704079,1.74886300140587));
#46765=CARTESIAN_POINT('Ctrl Pts',(2.59304849987271,-1.3929062269375,1.74381143062338));
#46766=CARTESIAN_POINT('Ctrl Pts',(2.54753379891838,-1.47449013126337,1.73875985984088));
#46767=CARTESIAN_POINT('Ctrl Pts',(2.49831789871698,-1.55363177006342,1.73370828905838));
#46768=CARTESIAN_POINT('Ctrl Pts',(2.44902671290464,-1.63289447190616,1.72864899088309));
#46769=CARTESIAN_POINT('Ctrl Pts',(2.39602327933239,-1.70970708867303,1.72358969270781));
#46770=CARTESIAN_POINT('Ctrl Pts',(2.33959587545587,-1.78371946772745,1.71853039453252));
#46771=CARTESIAN_POINT('Ctrl Pts',(2.32114211293664,-1.80792414086007,1.71687582457844));
#46772=CARTESIAN_POINT('Ctrl Pts',(2.30232245356334,-1.83182960538549,1.71522125462436));
#46773=CARTESIAN_POINT('Ctrl Pts',(2.28314783790605,-1.85542446633241,1.71356668467028));
#46774=CARTESIAN_POINT('Ctrl Pts',(2.22451498180353,-1.92757371361778,1.70850727885152));
#46775=CARTESIAN_POINT('Ctrl Pts',(2.16235721498671,-1.99706600845774,1.70344787303276));
#46776=CARTESIAN_POINT('Ctrl Pts',(2.09694427168874,-2.06353791373742,1.698388467214));
#46777=CARTESIAN_POINT('Ctrl Pts',(2.03161952660659,-2.12992019297136,1.69333588314249));
#46778=CARTESIAN_POINT('Ctrl Pts',(1.96304863557668,-2.19328986305016,1.68828329907098));
#46779=CARTESIAN_POINT('Ctrl Pts',(1.89154185024512,-2.25331609606181,1.68323071499948));
#46780=CARTESIAN_POINT('Ctrl Pts',(1.81676788183502,-2.31608495960644,1.6779472756727));
#46781=CARTESIAN_POINT('Ctrl Pts',(1.73878363591286,-2.37519718468404,1.67266383634592));
#46782=CARTESIAN_POINT('Ctrl Pts',(1.65798761618054,-2.43031707079385,1.66738039701914));
#46783=CARTESIAN_POINT('Ctrl Pts',(1.58085757829445,-2.48293598590886,1.66233668475716));
#46784=CARTESIAN_POINT('Ctrl Pts',(1.50116576355505,-2.53191666207956,1.65729297249517));
#46785=CARTESIAN_POINT('Ctrl Pts',(1.41929189825447,-2.57700882954429,1.65224926023319));
#46786=CARTESIAN_POINT('Ctrl Pts',(1.33744512751896,-2.62208607463225,1.64720721708979));
#46787=CARTESIAN_POINT('Ctrl Pts',(1.25341812848943,-2.66327715446222,1.64216517394639));
#46788=CARTESIAN_POINT('Ctrl Pts',(1.16761703258563,-2.70037672653575,1.63712313080299));
#46789=CARTESIAN_POINT('Ctrl Pts',(1.08182053048615,-2.73747431229229,1.63208135761138));
#46790=CARTESIAN_POINT('Ctrl Pts',(0.994250526977929,-2.77048065066324,
1.62703958441977));
#46791=CARTESIAN_POINT('Ctrl Pts',(0.905333988585948,-2.79923817656002,
1.62199781122817));
#46792=CARTESIAN_POINT('Ctrl Pts',(0.816397546733572,-2.82800213966508,
1.61695490946436));
#46793=CARTESIAN_POINT('Ctrl Pts',(0.726114392624978,-2.85251526541975,
1.61191200770056));
#46794=CARTESIAN_POINT('Ctrl Pts',(0.634926449410641,-2.87266990861094,
1.60686910593675));
#46795=CARTESIAN_POINT('Ctrl Pts',(0.543639396670226,-2.89284645729824,
1.60182072318954));
#46796=CARTESIAN_POINT('Ctrl Pts',(0.451446025075634,-2.90865497379437,
1.59677234044232));
#46797=CARTESIAN_POINT('Ctrl Pts',(0.358797911633199,-2.92003905087032,
1.59172395769511));
#46798=CARTESIAN_POINT('Ctrl Pts',(0.266090838691182,-2.93143037255669,
1.58667236225301));
#46799=CARTESIAN_POINT('Ctrl Pts',(0.172928888751452,-2.93839161647353,
1.58162076681091));
#46800=CARTESIAN_POINT('Ctrl Pts',(0.0797660882176299,-2.94091845707603,
1.5765691713688));
#46801=CARTESIAN_POINT('Ctrl Pts',(-0.0135392100561702,-2.94344916262326,
1.57150984922753));
#46802=CARTESIAN_POINT('Ctrl Pts',(-0.106844919901419,-2.94153193742826,
1.56645052708625));
#46803=CARTESIAN_POINT('Ctrl Pts',(-0.199699996586498,-2.93521445747382,
1.56139120494498));
#46804=CARTESIAN_POINT('Ctrl Pts',(-0.230062620282292,-2.933148708638,1.55973686034891));
#46805=CARTESIAN_POINT('Ctrl Pts',(-0.260377129848652,-2.9306128852774,
1.55808251575285));
#46806=CARTESIAN_POINT('Ctrl Pts',(-0.290627994539668,-2.92760983889415,
1.55642817115678));
#46807=CARTESIAN_POINT('Ctrl Pts',(-0.383143673011526,-2.91842567584738,
1.55136871866527));
#46808=CARTESIAN_POINT('Ctrl Pts',(-0.475383880833377,-2.90483591609127,
1.54630926617376));
#46809=CARTESIAN_POINT('Ctrl Pts',(-0.566896699361166,-2.88686545101316,
1.54124981368224));
#46810=CARTESIAN_POINT('Ctrl Pts',(-0.658286137903122,-2.86891921418812,
1.53619718247748));
#46811=CARTESIAN_POINT('Ctrl Pts',(-0.748949705218559,-2.84660409424142,
1.53114455127273));
#46812=CARTESIAN_POINT('Ctrl Pts',(-0.838440375979872,-2.81999676168728,
1.52609192006797));
#46813=CARTESIAN_POINT('Ctrl Pts',(-0.932018842480568,-2.7921740472422,
1.52080849246694));
#46814=CARTESIAN_POINT('Ctrl Pts',(-1.02431421614288,-2.75965768435425,
1.51552506486591));
#46815=CARTESIAN_POINT('Ctrl Pts',(-1.11482680265103,-2.72259530597018,
1.51024163726488));
#46816=CARTESIAN_POINT('Ctrl Pts',(-1.20123354750174,-2.68721415516963,
1.50519787707338));
#46817=CARTESIAN_POINT('Ctrl Pts',(-1.28601525677221,-2.64769060652783,
1.50015411688188));
#46818=CARTESIAN_POINT('Ctrl Pts',(-1.36875386174827,-2.60420369133238,
1.49511035669038));
#46819=CARTESIAN_POINT('Ctrl Pts',(-1.45146508932322,-2.56073116553497,
1.49006826543017));
#46820=CARTESIAN_POINT('Ctrl Pts',(-1.53213416430511,-2.5132980847454,1.48502617416995));
#46821=CARTESIAN_POINT('Ctrl Pts',(-1.61036596567334,-2.46213026799984,
1.47998408290973));
#46822=CARTESIAN_POINT('Ctrl Pts',(-1.68859358046111,-2.41096518950366,
1.47494226147738));
#46823=CARTESIAN_POINT('Ctrl Pts',(-1.76438381076976,-2.3560660152615,1.46990044004504));
#46824=CARTESIAN_POINT('Ctrl Pts',(-1.83736993038489,-2.29770227377644,
1.4648586186127));
#46825=CARTESIAN_POINT('Ctrl Pts',(-1.91037238824883,-2.23932546732321,
1.45981566854749));
#46826=CARTESIAN_POINT('Ctrl Pts',(-1.98056914318539,-2.17748282995883,
1.45477271848228));
#46827=CARTESIAN_POINT('Ctrl Pts',(-2.04762689024727,-2.11248387410089,
1.44972976841708));
#46828=CARTESIAN_POINT('Ctrl Pts',(-2.11475751728926,-2.04741427580687,
1.44468133755187));
#46829=CARTESIAN_POINT('Ctrl Pts',(-2.17874200966107,-1.97918182146721,
1.43963290668666));
#46830=CARTESIAN_POINT('Ctrl Pts',(-2.23928450504664,-1.90813230816367,
1.43458447582145));
#46831=CARTESIAN_POINT('Ctrl Pts',(-2.29986552754096,-1.83703758145578,
1.42953283231289));
#46832=CARTESIAN_POINT('Ctrl Pts',(-2.35699992200141,-1.76312257674857,
1.42448118880433));
#46833=CARTESIAN_POINT('Ctrl Pts',(-2.41043394182378,-1.68676382819405,
1.41942954529578));
#46834=CARTESIAN_POINT('Ctrl Pts',(-2.46394968616524,-1.61028829295524,
1.41437017556453));
#46835=CARTESIAN_POINT('Ctrl Pts',(-2.51375352515499,-1.5313619281524,1.40931080583329));
#46836=CARTESIAN_POINT('Ctrl Pts',(-2.55963675307689,-1.45038742834389,
1.40425143610204));
#46837=CARTESIAN_POINT('Ctrl Pts',(-2.57463614522885,-1.4239165732636,1.40259750994911));
#46838=CARTESIAN_POINT('Ctrl Pts',(-2.58921693702995,-1.39722701076762,
1.40094358379619));
#46839=CARTESIAN_POINT('Ctrl Pts',(-2.60337295665021,-1.3703332618682,1.39928965764326));
#46840=CARTESIAN_POINT('Ctrl Pts',(-2.64903858949363,-1.28357723185635,
1.39395428891139));
#46841=CARTESIAN_POINT('Ctrl Pts',(-2.69042405278558,-1.19442196979203,
1.38861892017953));
#46842=CARTESIAN_POINT('Ctrl Pts',(-2.72728553218514,-1.10330305262589,
1.38328355144766));
#46843=CARTESIAN_POINT('Ctrl Pts',(-2.76404544329879,-1.01243520493341,
1.37796288381477));
#46844=CARTESIAN_POINT('Ctrl Pts',(-2.796306074387,-0.919614827091285,1.37264221618187));
#46845=CARTESIAN_POINT('Ctrl Pts',(-2.82387039829454,-0.825299929501884,
1.36732154854897));
#46846=CARTESIAN_POINT('Ctrl Pts',(-2.85138911804932,-0.731141072416592,
1.36200968376357));
#46847=CARTESIAN_POINT('Ctrl Pts',(-2.87422689292036,-0.635492970896159,
1.35669781897816));
#46848=CARTESIAN_POINT('Ctrl Pts',(-2.89223504922506,-0.538832460078394,
1.35138595419276));
#46849=CARTESIAN_POINT('Ctrl Pts',(-2.91020301497016,-0.442387675954391,
1.34608594441431));
#46850=CARTESIAN_POINT('Ctrl Pts',(-2.92336277411057,-0.344935348068787,
1.34078593463586));
#46851=CARTESIAN_POINT('Ctrl Pts',(-2.93161598538492,-0.246965006095231,
1.3354859248574));
#46852=CARTESIAN_POINT('Ctrl Pts',(-2.93852469309688,-0.164954691002573,
1.3310493222778));
#46853=CARTESIAN_POINT('Ctrl Pts',(-2.94199609487689,-0.0825817753051015,
1.32661271969819));
#46854=CARTESIAN_POINT('Ctrl Pts',(-2.94199999670507,-0.000139238540423715,
1.32217611711858));
#46855=CARTESIAN_POINT('Ctrl Pts',(-2.94199999670509,-0.000139238001722604,
1.32217611708959));
#46856=CARTESIAN_POINT('Ctrl Pts',(-2.94200461971914,0.0975417624295902,
1.3169194644501));
#46857=CARTESIAN_POINT('Ctrl Pts',(-2.93714008660293,0.195140032597408,
1.3116628118106));
#46858=CARTESIAN_POINT('Ctrl Pts',(-2.9274568958829,0.292164547383291,1.30640615917111));
#46859=CARTESIAN_POINT('Ctrl Pts',(-2.91759330638285,0.390996638267333,
1.30105157458433));
#46860=CARTESIAN_POINT('Ctrl Pts',(-2.90272978303102,0.489232965131264,
1.29569698999755));
#46861=CARTESIAN_POINT('Ctrl Pts',(-2.88297400170303,0.586365846127163,
1.29034240541077));
#46862=CARTESIAN_POINT('Ctrl Pts',(-2.86350947736034,0.682066709344435,
1.28506676278727));
#46863=CARTESIAN_POINT('Ctrl Pts',(-2.83929615567487,0.776696093972239,
1.27979112016378));
#46864=CARTESIAN_POINT('Ctrl Pts',(-2.81048718761002,0.86978489770744,1.27451547754029));
#46865=CARTESIAN_POINT('Ctrl Pts',(-2.78103159599759,0.964963099867981,
1.26912142197186));
#46866=CARTESIAN_POINT('Ctrl Pts',(-2.74677175407064,1.05853033508138,1.26372736640344));
#46867=CARTESIAN_POINT('Ctrl Pts',(-2.7079224893435,1.15000860505811,1.25833331083501));
#46868=CARTESIAN_POINT('Ctrl Pts',(-2.66907322461637,1.24148687503483,1.25293925526659));
#46869=CARTESIAN_POINT('Ctrl Pts',(-2.6256347840461,1.33087583051891,1.24754519969817));
#46870=CARTESIAN_POINT('Ctrl Pts',(-2.57787031674964,1.41772657096534,1.24215114412974));
#46871=CARTESIAN_POINT('Ctrl Pts',(-2.53306833937824,1.49919057817427,1.23709164343404));
#46872=CARTESIAN_POINT('Ctrl Pts',(-2.484323403088,1.57866996854652,1.23203214273833));
#46873=CARTESIAN_POINT('Ctrl Pts',(-2.43183598902006,1.655758956644,1.22697264204262));
#46874=CARTESIAN_POINT('Ctrl Pts',(-2.37941935174519,1.73274399389049,1.22191996384408));
#46875=CARTESIAN_POINT('Ctrl Pts',(-2.32327051304004,1.80734467177867,1.21686728564554));
#46876=CARTESIAN_POINT('Ctrl Pts',(-2.26363564474575,1.87918005200047,1.211814607447));
#46877=CARTESIAN_POINT('Ctrl Pts',(-2.20127746812945,1.95429589371013,1.20653119174572));
#46878=CARTESIAN_POINT('Ctrl Pts',(-2.1351075099787,2.02638741982237,1.20124777604444));
#46879=CARTESIAN_POINT('Ctrl Pts',(-2.06545788195732,2.09505315871946,1.19596436034315));
#46880=CARTESIAN_POINT('Ctrl Pts',(-1.99896698228195,2.16060479030521,1.19092055647346));
#46881=CARTESIAN_POINT('Ctrl Pts',(-1.92930549514981,2.22303423457185,1.18587675260376));
#46882=CARTESIAN_POINT('Ctrl Pts',(-1.85680233912528,2.28202740417789,1.18083294873406));
#46883=CARTESIAN_POINT('Ctrl Pts',(-1.78432319216586,2.34100103848468,1.17579081509532));
#46884=CARTESIAN_POINT('Ctrl Pts',(-1.70900458915356,2.39654037991088,1.17074868145657));
#46885=CARTESIAN_POINT('Ctrl Pts',(-1.63120945504026,2.44837082848723,1.16570654781783));
#46886=CARTESIAN_POINT('Ctrl Pts',(-1.55341850486603,2.50019848954427,1.1606646853526));
#46887=CARTESIAN_POINT('Ctrl Pts',(-1.47315165717348,2.54831740936594,1.15562282288737));
#46888=CARTESIAN_POINT('Ctrl Pts',(-1.39080087224642,2.59249627458915,1.15058096042214));
#46889=CARTESIAN_POINT('Ctrl Pts',(-1.30843167565013,2.63668501715176,1.14553797071685));
#46890=CARTESIAN_POINT('Ctrl Pts',(-1.22397800664928,2.67693174654931,1.14049498101155));
#46891=CARTESIAN_POINT('Ctrl Pts',(-1.13785545991309,2.71305159411795,1.13545199130626));
#46892=CARTESIAN_POINT('Ctrl Pts',(-1.05163935271553,2.749210681,1.13040352307692));
#46893=CARTESIAN_POINT('Ctrl Pts',(-0.963751158273544,2.78123376718841,
1.12535505484758));
#46894=CARTESIAN_POINT('Ctrl Pts',(-0.874625123638633,2.80898467299131,
1.12030658661823));
#46895=CARTESIAN_POINT('Ctrl Pts',(-0.785442395262867,2.83675323135408,
1.11525490702029));
#46896=CARTESIAN_POINT('Ctrl Pts',(-0.695020687100776,2.86024408796144,
1.11020322742234));
#46897=CARTESIAN_POINT('Ctrl Pts',(-0.603805961307181,2.87937186919125,
1.10515154782439));
#46898=CARTESIAN_POINT('Ctrl Pts',(-0.512451767661679,2.898528896911,1.10009214417864));
#46899=CARTESIAN_POINT('Ctrl Pts',(-0.420302572603004,2.91330946531776,
1.0950327405329));
#46900=CARTESIAN_POINT('Ctrl Pts',(-0.327810695308905,2.92367989835431,
1.08997333688715));
#46901=CARTESIAN_POINT('Ctrl Pts',(-0.297581504424793,2.92706927490266,
1.08831976813018));
#46902=CARTESIAN_POINT('Ctrl Pts',(-0.267315714603243,2.92998798311205,
1.08666619937321));
#46903=CARTESIAN_POINT('Ctrl Pts',(-0.23702909370367,2.93243605364857,1.08501263061624));
#46904=CARTESIAN_POINT('Ctrl Pts',(-0.144355971888771,2.93992683117027,
1.07995292523173));
#46905=CARTESIAN_POINT('Ctrl Pts',(-0.0511669651402399,2.94303318993482,
1.07489321984723));
#46906=CARTESIAN_POINT('Ctrl Pts',(0.0420887859023279,2.94169891968931,
1.06983351446272));
#46907=CARTESIAN_POINT('Ctrl Pts',(0.13521885028736,2.94036644772397,1.06478062836229));
#46908=CARTESIAN_POINT('Ctrl Pts',(0.228415041169705,2.93460524712247,1.05972774226186));
#46909=CARTESIAN_POINT('Ctrl Pts',(0.321223787193121,2.9244109284677,1.05467485616143));
#46910=CARTESIAN_POINT('Ctrl Pts',(0.418265832018059,2.91375161487665,1.04939149203398));
#46911=CARTESIAN_POINT('Ctrl Pts',(0.514883757398431,2.89824508608974,1.04410812790654));
#46912=CARTESIAN_POINT('Ctrl Pts',(0.610559589537355,2.8779473566457,1.03882476377909));
#46913=CARTESIAN_POINT('Ctrl Pts',(0.701901133702176,2.85856915100056,1.03378074558769));
#46914=CARTESIAN_POINT('Ctrl Pts',(0.792383595393697,2.8348244836784,1.02873672739629));
#46915=CARTESIAN_POINT('Ctrl Pts',(0.881563614700024,2.80681484840683,1.02369270920489));
#46916=CARTESIAN_POINT('Ctrl Pts',(0.970714136927654,2.7788144775694,1.01865035936704));
#46917=CARTESIAN_POINT('Ctrl Pts',(1.05856265076265,2.7465520742627,1.01360800952919));
#46918=CARTESIAN_POINT('Ctrl Pts',(1.1446800186878,2.71017926617722,1.00856565969134));
#46919=CARTESIAN_POINT('Ctrl Pts',(1.23079278236441,2.67380840275694,1.00352357944175));
#46920=CARTESIAN_POINT('Ctrl Pts',(1.31517417658744,2.63332774428076,0.998481499192167));
#46921=CARTESIAN_POINT('Ctrl Pts',(1.39741519490234,2.58893699673361,0.993439418942582));
#46922=CARTESIAN_POINT('Ctrl Pts',(1.47967462066404,2.54453631350788,0.988396210158526));
#46923=CARTESIAN_POINT('Ctrl Pts',(1.55979232969195,2.49622401350885,0.983353001374471));
#46924=CARTESIAN_POINT('Ctrl Pts',(1.63738505705346,2.4442451135142,0.978309792590416));
#46925=CARTESIAN_POINT('Ctrl Pts',(1.71506208503325,2.39220974104389,0.9732611046122));
#46926=CARTESIAN_POINT('Ctrl Pts',(1.79020828831455,2.33650006511776,0.968212416633985));
#46927=CARTESIAN_POINT('Ctrl Pts',(1.86247076061764,2.27740349210331,0.963163728655769));
#46928=CARTESIAN_POINT('Ctrl Pts',(1.93477920673401,2.21826932149876,0.958111828672331));
#46929=CARTESIAN_POINT('Ctrl Pts',(2.00419994088024,2.15574425994461,0.953059928688893));
#46930=CARTESIAN_POINT('Ctrl Pts',(2.0704160035922,2.09015348050551,0.948008028705455));
#46931=CARTESIAN_POINT('Ctrl Pts',(2.13673329482258,2.02446242845653,0.942948405575554));
#46932=CARTESIAN_POINT('Ctrl Pts',(2.19983583847281,1.9556966303443,0.937888782445653));
#46933=CARTESIAN_POINT('Ctrl Pts',(2.25944631754215,1.88421504562117,0.932829159315752));
#46934=CARTESIAN_POINT('Ctrl Pts',(2.27890576689535,1.86088035180019,0.931177478578075));
#46935=CARTESIAN_POINT('Ctrl Pts',(2.29799342574526,1.83725648233511,0.929525797840397));
#46936=CARTESIAN_POINT('Ctrl Pts',(2.31670066257897,1.81335656725481,0.92787411710272));
#46937=CARTESIAN_POINT('Ctrl Pts',(2.37399274853932,1.74016157852416,0.922815741264366));
#46938=CARTESIAN_POINT('Ctrl Pts',(2.42791212019609,1.66412162110509,0.917757365426012));
#46939=CARTESIAN_POINT('Ctrl Pts',(2.47816445280402,1.58558031800932,0.912698989587657));
#46940=CARTESIAN_POINT('Ctrl Pts',(2.52834900067583,1.50714495828431,0.907647436928519));
#46941=CARTESIAN_POINT('Ctrl Pts',(2.57487610284079,1.42621532820593,0.902595884269381));
#46942=CARTESIAN_POINT('Ctrl Pts',(2.61749222992237,1.34316731135626,0.897544331610243));
#46943=CARTESIAN_POINT('Ctrl Pts',(2.66206678314268,1.25630281895836,0.892260634609366));
#46944=CARTESIAN_POINT('Ctrl Pts',(2.70236197047381,1.16712094851813,0.88697693760849));
#46945=CARTESIAN_POINT('Ctrl Pts',(2.73813896039309,1.07608504941639,0.881693240607613));
#46946=CARTESIAN_POINT('Ctrl Pts',(2.77228400676289,0.989201692175915,0.8766505559238));
#46947=CARTESIAN_POINT('Ctrl Pts',(2.80231381262609,0.900630195460668,0.871607871239987));
#46948=CARTESIAN_POINT('Ctrl Pts',(2.82806884408845,0.810796283351271,0.866565186556173));
#46949=CARTESIAN_POINT('Ctrl Pts',(2.85381536898689,0.720992042256478,0.861524167407873));
#46950=CARTESIAN_POINT('Ctrl Pts',(2.87528980285597,0.629926639656187,0.856483148259572));
#46951=CARTESIAN_POINT('Ctrl Pts',(2.89238228544692,0.538041554931251,0.851442129111271));
#46952=CARTESIAN_POINT('Ctrl Pts',(2.90947386925272,0.446161301859626,0.846401375038167));
#46953=CARTESIAN_POINT('Ctrl Pts',(2.92218387947666,0.353461887938309,0.841360620965063));
#46954=CARTESIAN_POINT('Ctrl Pts',(2.93045367039417,0.26039448088107,0.836319866891959));
#46955=CARTESIAN_POINT('Ctrl Pts',(2.93872532296153,0.167306123001053,0.831277978072023));
#46956=CARTESIAN_POINT('Ctrl Pts',(2.94255473209556,0.0738500486034947,
0.826236089252088));
#46957=CARTESIAN_POINT('Ctrl Pts',(2.94193524824454,-0.0195190967095212,
0.821194200432152));
#46958=CARTESIAN_POINT('Ctrl Pts',(2.94131508913938,-0.112990016912663,
0.816146815817231));
#46959=CARTESIAN_POINT('Ctrl Pts',(2.93623636193386,-0.206373375464665,
0.811099431202309));
#46960=CARTESIAN_POINT('Ctrl Pts',(2.92674451882024,-0.299216512839292,
0.806052046587388));
#46961=CARTESIAN_POINT('Ctrl Pts',(2.91724662010408,-0.392118882244111,
0.80100144184391));
#46962=CARTESIAN_POINT('Ctrl Pts',(2.90333006640131,-0.484479906895986,
0.795950837100432));
#46963=CARTESIAN_POINT('Ctrl Pts',(2.88509163073236,-0.575856129843267,
0.790900232356954));
#46964=CARTESIAN_POINT('Ctrl Pts',(2.86682522357148,-0.66737249251143,0.785841881721643));
#46965=CARTESIAN_POINT('Ctrl Pts',(2.84422381317679,-0.757900610476704,
0.780783531086332));
#46966=CARTESIAN_POINT('Ctrl Pts',(2.817434206504,-0.847011506427842,0.775725180451022));
#46967=CARTESIAN_POINT('Ctrl Pts',(2.8086257488842,-0.876311285257559,0.77406198816375));
#46968=CARTESIAN_POINT('Ctrl Pts',(2.79936489210506,-0.905458007307212,
0.77239879587648));
#46969=CARTESIAN_POINT('Ctrl Pts',(2.78965797630214,-0.934436929521649,
0.770735603589208));
#46970=CARTESIAN_POINT('Ctrl Pts',(2.76012371083481,-1.02260820853707,0.765675174145623));
#46971=CARTESIAN_POINT('Ctrl Pts',(2.72635407592158,-1.10953048163224,0.760614744702038));
#46972=CARTESIAN_POINT('Ctrl Pts',(2.68847392916613,-1.19476856846589,0.755554315258454));
#46973=CARTESIAN_POINT('Ctrl Pts',(2.6506448841658,-1.27989166588652,0.750500712526178));
#46974=CARTESIAN_POINT('Ctrl Pts',(2.60871652594505,-1.36333469126638,0.745447109793901));
#46975=CARTESIAN_POINT('Ctrl Pts',(2.5628631043721,-1.44467875607285,0.740393507061625));
#46976=CARTESIAN_POINT('Ctrl Pts',(2.51492659691061,-1.52971821955847,0.735110323020545));
#46977=CARTESIAN_POINT('Ctrl Pts',(2.46270008736353,-1.61246302272199,0.729827138979464));
#46978=CARTESIAN_POINT('Ctrl Pts',(2.40643854657599,-1.6924590162108,0.724543954938384));
#46979=CARTESIAN_POINT('Ctrl Pts',(2.35271654217843,-1.76884414633411,0.719499243536685));
#46980=CARTESIAN_POINT('Ctrl Pts',(2.29531614667676,-1.84272282308006,0.714454532134986));
#46981=CARTESIAN_POINT('Ctrl Pts',(2.23450495372136,-1.91372715186746,0.709409820733287));
#46982=CARTESIAN_POINT('Ctrl Pts',(2.17371399249588,-1.98470785769443,0.704366787694299));
#46983=CARTESIAN_POINT('Ctrl Pts',(2.10951477618156,-2.0528157798459,0.699323754655311));
#46984=CARTESIAN_POINT('Ctrl Pts',(2.04221541263933,-2.11771579971874,0.694280721616323));
#46985=CARTESIAN_POINT('Ctrl Pts',(1.97491979124556,-2.18261221085745,0.689237968992741));
#46986=CARTESIAN_POINT('Ctrl Pts',(1.90452468432683,-2.24430076759546,0.684195216369159));
#46987=CARTESIAN_POINT('Ctrl Pts',(1.83137450342477,-2.30248375199602,0.679152463745576));
#46988=CARTESIAN_POINT('Ctrl Pts',(1.75820812106062,-2.36067962289125,0.674108594242112));
#46989=CARTESIAN_POINT('Ctrl Pts',(1.68228579925905,-2.41536810418269,0.669064724738647));
#46990=CARTESIAN_POINT('Ctrl Pts',(1.60398350556405,-2.46629294972808,0.664020855235182));
#46991=CARTESIAN_POINT('Ctrl Pts',(1.52559647602039,-2.51727290425947,0.658971527442531));
#46992=CARTESIAN_POINT('Ctrl Pts',(1.44482470597328,-2.56448085311737,0.653922199649879));
#46993=CARTESIAN_POINT('Ctrl Pts',(1.36207121844092,-2.60770512057918,0.648872871857228));
#46994=CARTESIAN_POINT('Ctrl Pts',(1.27926527577715,-2.65095678670052,0.643820343436291));
#46995=CARTESIAN_POINT('Ctrl Pts',(1.19447551590553,-2.69021955848492,0.638767815015354));
#46996=CARTESIAN_POINT('Ctrl Pts',(1.10812557491149,-2.72532965166181,0.633715286594418));
#46997=CARTESIAN_POINT('Ctrl Pts',(1.0216440172149,-2.76049326050573,0.62865505698547));
#46998=CARTESIAN_POINT('Ctrl Pts',(0.933597948821291,-2.79149141171207,
0.623594827376522));
#46999=CARTESIAN_POINT('Ctrl Pts',(0.844426506240923,-2.81821004816138,
0.618534597767575));
#47000=CARTESIAN_POINT('Ctrl Pts',(0.815423561206037,-2.82690026469172,
0.616888761870281));
#47001=CARTESIAN_POINT('Ctrl Pts',(0.786301645408335,-2.8351381676959,0.615242925972988));
#47002=CARTESIAN_POINT('Ctrl Pts',(0.757076058362179,-2.84292100520834,
0.613597090075694));
#47003=CARTESIAN_POINT('Ctrl Pts',(0.667207001745775,-2.86685333080839,
0.608536123491804));
#47004=CARTESIAN_POINT('Ctrl Pts',(0.576047154021573,-2.88656138929389,
0.603475156907913));
#47005=CARTESIAN_POINT('Ctrl Pts',(0.484028648964702,-2.90190976203283,
0.598414190324023));
#47006=CARTESIAN_POINT('Ctrl Pts',(0.392133871894972,-2.91723749736558,
0.59336002871059));
#47007=CARTESIAN_POINT('Ctrl Pts',(0.299383164868472,-2.92821712480805,
0.588305867097157));
#47008=CARTESIAN_POINT('Ctrl Pts',(0.206222253901962,-2.93476342862514,
0.583251705483724));
#47009=CARTESIAN_POINT('Ctrl Pts',(0.108842408851515,-2.94160619180498,
0.577968658445326));
#47010=CARTESIAN_POINT('Ctrl Pts',(0.0110147984464832,-2.94360446042169,
0.572685611406928));
#47011=CARTESIAN_POINT('Ctrl Pts',(-0.0867411774537793,-2.94072099460896,
0.567402564368531));
#47012=CARTESIAN_POINT('Ctrl Pts',(-0.180098316403701,-2.93796727939046,
0.562357244612878));
#47013=CARTESIAN_POINT('Ctrl Pts',(-0.273389632933628,-2.93076167051084,
0.557311924857226));
#47014=CARTESIAN_POINT('Ctrl Pts',(-0.366160572951378,-2.91912494333763,
0.552266605101574));
#47015=CARTESIAN_POINT('Ctrl Pts',(-0.458900958962508,-2.90749204870766,
0.54722294701641));
#47016=CARTESIAN_POINT('Ctrl Pts',(-0.551120870401268,-2.89143099057585,
0.542179288931246));
#47017=CARTESIAN_POINT('Ctrl Pts',(-0.642370803818245,-2.87101441138875,
0.537135630846082));
#47018=CARTESIAN_POINT('Ctrl Pts',(-0.733615949180425,-2.85059890349778,
0.532092237411098));
#47019=CARTESIAN_POINT('Ctrl Pts',(-0.823890786108729,-2.8258284261362,
0.527048843976114));
#47020=CARTESIAN_POINT('Ctrl Pts',(-0.912757038905083,-2.79682652088563,
0.52200545054113));
#47021=CARTESIAN_POINT('Ctrl Pts',(-1.00164323318172,-2.7678181076424,0.516960925374724));
#47022=CARTESIAN_POINT('Ctrl Pts',(-1.08911979511789,-2.73457651811266,
0.511916400208317));
#47023=CARTESIAN_POINT('Ctrl Pts',(-1.17476568767022,-2.69727447232808,
0.50687187504191));
#47024=CARTESIAN_POINT('Ctrl Pts',(-1.26050455944576,-2.65993193055311,
0.501821873418695));
#47025=CARTESIAN_POINT('Ctrl Pts',(-1.34440838938401,-2.61852031194909,
0.496771871795479));
#47026=CARTESIAN_POINT('Ctrl Pts',(-1.42607844119853,-2.57325946603695,
0.491721870172263));
#47027=CARTESIAN_POINT('Ctrl Pts',(-1.50780043677,-2.52796983333789,0.486668656648834));
#47028=CARTESIAN_POINT('Ctrl Pts',(-1.58728544990138,-2.47882633170898,
0.481615443125405));
#47029=CARTESIAN_POINT('Ctrl Pts',(-1.66416336507436,-2.42609239196375,
0.476562229601975));
#47030=CARTESIAN_POINT('Ctrl Pts',(-1.74115860868422,-2.3732779714887,0.471501304037415));
#47031=CARTESIAN_POINT('Ctrl Pts',(-1.81553846179002,-2.31686244365307,
0.466440378472854));
#47032=CARTESIAN_POINT('Ctrl Pts',(-1.88696577597676,-2.2571495653351,0.461379452908294));
#47033=CARTESIAN_POINT('Ctrl Pts',(-1.91011601969959,-2.23779607707655,
0.459739160792923));
#47034=CARTESIAN_POINT('Ctrl Pts',(-1.93295640049665,-2.21809649974357,
0.458098868677552));
#47035=CARTESIAN_POINT('Ctrl Pts',(-1.95547630356216,-2.19806197051104,
0.456458576562181));
#47036=CARTESIAN_POINT('Ctrl Pts',(-2.02385521807488,-2.137229587809,0.451478031397016));
#47037=CARTESIAN_POINT('Ctrl Pts',(-2.08952991361327,-2.07308110044888,
0.446497486231852));
#47038=CARTESIAN_POINT('Ctrl Pts',(-2.15215463624812,-2.00588993259244,
0.441516941066687));
#47039=CARTESIAN_POINT('Ctrl Pts',(-2.21467995181695,-1.93880542032789,
0.43654430174703));
#47040=CARTESIAN_POINT('Ctrl Pts',(-2.27416460854903,-1.86868815980554,
0.431571662427372));
#47041=CARTESIAN_POINT('Ctrl Pts',(-2.33029690289864,-1.79585086918179,
0.426599023107715));
#47042=CARTESIAN_POINT('Ctrl Pts',(-2.38637883272966,-1.72307893158024,
0.421630845472519));
#47043=CARTESIAN_POINT('Ctrl Pts',(-2.43911409152223,-1.64759216767629,
0.416662667837323));
#47044=CARTESIAN_POINT('Ctrl Pts',(-2.48822931388568,-1.5697384755175,0.411694490202127));
#47045=CARTESIAN_POINT('Ctrl Pts',(-2.53731512223824,-1.49193140819799,
0.406729287897674));
#47046=CARTESIAN_POINT('Ctrl Pts',(-2.58278495436859,-1.41176061293751,
0.40176408559322));
#47047=CARTESIAN_POINT('Ctrl Pts',(-2.6244078838903,-1.32960417379551,0.396798883288767));
#47048=CARTESIAN_POINT('Ctrl Pts',(-2.66601830188986,-1.24747243022683,
0.391835173484704));
#47049=CARTESIAN_POINT('Ctrl Pts',(-2.70378390784644,-1.1633566367953,0.386871463680641));
#47050=CARTESIAN_POINT('Ctrl Pts',(-2.73751964702703,-1.07765958546333,
0.381907753876579));
#47051=CARTESIAN_POINT('Ctrl Pts',(-2.77135003798828,-0.991722095394787,
0.376930117477664));
#47052=CARTESIAN_POINT('Ctrl Pts',(-2.80112772804158,-0.904194884455238,
0.371952481078748));
#47053=CARTESIAN_POINT('Ctrl Pts',(-2.82671515886674,-0.815503164085203,
0.366974844679833));
#47054=CARTESIAN_POINT('Ctrl Pts',(-2.85224966434525,-0.726994894725836,
0.362007504083325));
#47055=CARTESIAN_POINT('Ctrl Pts',(-2.87361114176866,-0.637327381440443,
0.357040163486818));
#47056=CARTESIAN_POINT('Ctrl Pts',(-2.89071367265674,-0.546935519705347,
0.35207282289031));
#47057=CARTESIAN_POINT('Ctrl Pts',(-2.90786937614552,-0.456262625273901,
0.347090038590191));
#47058=CARTESIAN_POINT('Ctrl Pts',(-2.92073954449786,-0.364861329719361,
0.342107254290072));
#47059=CARTESIAN_POINT('Ctrl Pts',(-2.92928980875558,-0.27317616352954,
0.337124469989953));
#47060=CARTESIAN_POINT('Ctrl Pts',(-2.9378400730133,-0.181490997339719,
0.332141685689834));
#47061=CARTESIAN_POINT('Ctrl Pts',(-2.94207046158018,-0.0895224226019215,
0.327158901389715));
#47062=CARTESIAN_POINT('Ctrl Pts',(-2.94199911155216,0.00228640028720795,
0.322176117089596));
#47063=CARTESIAN_POINT('Origin',(0.,0.,-1.84858989190501));
#47064=CARTESIAN_POINT('',(-2.37174915417064,-0.00200304539514994,10.651410108095));
#47065=CARTESIAN_POINT('Ctrl Pts',(-2.36545136240482,0.172736546790724,
10.6389210243916));
#47066=CARTESIAN_POINT('Ctrl Pts',(-2.36969609595299,0.114609237074736,
10.643124268197));
#47067=CARTESIAN_POINT('Ctrl Pts',(-2.37179806469451,0.0563280682077159,
10.6473616493302));
#47068=CARTESIAN_POINT('Ctrl Pts',(-2.37174916623817,-0.00198870524203496,
10.6516070788671));
#47069=CARTESIAN_POINT('',(-2.34668236863852,0.343918483395543,11.62825));
#47070=CARTESIAN_POINT('Ctrl Pts',(-2.37174915417064,-0.00200304539514992,
10.651410108095));
#47071=CARTESIAN_POINT('Ctrl Pts',(-2.3716576055993,-0.11040310820655,10.6586904087473));
#47072=CARTESIAN_POINT('Ctrl Pts',(-2.36413081146793,-0.21849095763389,
10.6659707093996));
#47073=CARTESIAN_POINT('Ctrl Pts',(-2.34931805963096,-0.325426976742579,
10.6732510100519));
#47074=CARTESIAN_POINT('Ctrl Pts',(-2.34106564337189,-0.385002709360389,
10.6773069796742));
#47075=CARTESIAN_POINT('Ctrl Pts',(-2.33055266045321,-0.444221480602426,
10.6813629492966));
#47076=CARTESIAN_POINT('Ctrl Pts',(-2.31781106222524,-0.502941291132799,
10.6854189189189));
#47077=CARTESIAN_POINT('Ctrl Pts',(-2.30103244669589,-0.580265745037053,
10.6907599721898));
#47078=CARTESIAN_POINT('Ctrl Pts',(-2.28034966391946,-0.656890328392001,
10.6961010254607));
#47079=CARTESIAN_POINT('Ctrl Pts',(-2.25583677761288,-0.732392309673682,
10.7014420787316));
#47080=CARTESIAN_POINT('Ctrl Pts',(-2.23135845642761,-0.807787827150567,
10.7067756006922));
#47081=CARTESIAN_POINT('Ctrl Pts',(-2.20306090137613,-0.88206344593845,
10.7121091226527));
#47082=CARTESIAN_POINT('Ctrl Pts',(-2.17106897787264,-0.954807601466947,
10.7174426446133));
#47083=CARTESIAN_POINT('Ctrl Pts',(-2.13911306659992,-1.02746987134964,
10.7227701628078));
#47084=CARTESIAN_POINT('Ctrl Pts',(-2.10347123892394,-1.09860367880999,
10.7280976810023));
#47085=CARTESIAN_POINT('Ctrl Pts',(-2.06431736356217,-1.16781500461148,
10.7334251991968));
#47086=CARTESIAN_POINT('Ctrl Pts',(-2.02518748579086,-1.23698391047278,
10.7387494521309));
#47087=CARTESIAN_POINT('Ctrl Pts',(-1.9825500628117,-1.3042322684173,10.744073705065));
#47088=CARTESIAN_POINT('Ctrl Pts',(-1.93662550425837,-1.36918943859351,
10.7493979579991));
#47089=CARTESIAN_POINT('Ctrl Pts',(-1.89071493070968,-1.43412682793013,
10.754720589585));
#47090=CARTESIAN_POINT('Ctrl Pts',(-1.84151947905621,-1.49677403427864,
10.7600432211708));
#47091=CARTESIAN_POINT('Ctrl Pts',(-1.78930279570886,-1.55678950657064,
10.7653658527567));
#47092=CARTESIAN_POINT('Ctrl Pts',(-1.73708591124963,-1.61680521001145,
10.7706885048426));
#47093=CARTESIAN_POINT('Ctrl Pts',(-1.68184807965202,-1.67418880810358,
10.7760111569285));
#47094=CARTESIAN_POINT('Ctrl Pts',(-1.62389216613693,-1.72863307131939,
10.7813338090144));
#47095=CARTESIAN_POINT('Ctrl Pts',(-1.56587940826847,-1.78313073458964,
10.786661681667));
#47096=CARTESIAN_POINT('Ctrl Pts',(-1.50514358481335,-1.83468298449049,
10.7919895543197));
#47097=CARTESIAN_POINT('Ctrl Pts',(-1.44202280445052,-1.8830210550986,10.7973174269724));
#47098=CARTESIAN_POINT('Ctrl Pts',(-1.37887101516864,-1.93138287242388,
10.802647917013));
#47099=CARTESIAN_POINT('Ctrl Pts',(-1.31333231975803,-1.9765270996243,10.8079784070537));
#47100=CARTESIAN_POINT('Ctrl Pts',(-1.24577408566008,-2.01822818085513,
10.8133088970943));
#47101=CARTESIAN_POINT('Ctrl Pts',(-1.17809860777621,-2.06000163213389,
10.818648637922));
#47102=CARTESIAN_POINT('Ctrl Pts',(-1.10839699898012,-2.09831977402247,
10.8239883787496));
#47103=CARTESIAN_POINT('Ctrl Pts',(-1.0370612503182,-2.13300305334719,10.8293281195772));
#47104=CARTESIAN_POINT('Ctrl Pts',(-0.978149343837453,-2.16164588876071,
10.833737890529));
#47105=CARTESIAN_POINT('Ctrl Pts',(-0.918123466404,-2.18781053406727,10.8381476614807));
#47106=CARTESIAN_POINT('Ctrl Pts',(-0.857212862138923,-2.21142130121865,
10.8425574324324));
#47107=CARTESIAN_POINT('Ctrl Pts',(-0.783564483559484,-2.23996960965684,
10.8478893854547));
#47108=CARTESIAN_POINT('Ctrl Pts',(-0.708351392720743,-2.2648878699676,
10.853221338477));
#47109=CARTESIAN_POINT('Ctrl Pts',(-0.631965683600276,-2.28600468880789,
10.8585532914993));
#47110=CARTESIAN_POINT('Ctrl Pts',(-0.555688377193635,-2.30709153973276,
10.8638776776851));
#47111=CARTESIAN_POINT('Ctrl Pts',(-0.478242205414549,-2.32438753902868,
10.8692020638708));
#47112=CARTESIAN_POINT('Ctrl Pts',(-0.400038041337422,-2.33776979790203,
10.8745264500565));
#47113=CARTESIAN_POINT('Ctrl Pts',(-0.321922208961844,-2.35113694149719,
10.8798448223414));
#47114=CARTESIAN_POINT('Ctrl Pts',(-0.243050545349262,-2.36059905065694,
10.8851631946262));
#47115=CARTESIAN_POINT('Ctrl Pts',(-0.163846373361652,-2.36608377460229,
10.8904815669111));
#47116=CARTESIAN_POINT('Ctrl Pts',(-0.0846908540129318,-2.37156512945374,
10.8957966722866));
#47117=CARTESIAN_POINT('Ctrl Pts',(-0.00520369810401163,-2.37307391631134,
10.9011117776622));
#47118=CARTESIAN_POINT('Ctrl Pts',(0.0741855701400063,-2.37058949708358,
10.9064268830377));
#47119=CARTESIAN_POINT('Ctrl Pts',(0.153550788114269,-2.36810583048844,
10.9117403782496));
#47120=CARTESIAN_POINT('Ctrl Pts',(0.232817709169052,-2.36163137480067,
10.9170538734614));
#47121=CARTESIAN_POINT('Ctrl Pts',(0.31155721659169,-2.35119760192325,10.9223673686732));
#47122=CARTESIAN_POINT('Ctrl Pts',(0.390297383798681,-2.3407637416178,10.9276809084086));
#47123=CARTESIAN_POINT('Ctrl Pts',(0.468509664188686,-2.32637056139121,
10.932994448144));
#47124=CARTESIAN_POINT('Ctrl Pts',(0.545771953761925,-2.30810117563916,
10.9383079878794));
#47125=CARTESIAN_POINT('Ctrl Pts',(0.623111609465042,-2.28981349594736,
10.9436268482959));
#47126=CARTESIAN_POINT('Ctrl Pts',(0.699498917311407,-2.26764196667449,
10.9489457087124));
#47127=CARTESIAN_POINT('Ctrl Pts',(0.774524443417242,-2.24172031017458,
10.9542645691289));
#47128=CARTESIAN_POINT('Ctrl Pts',(0.849587474036689,-2.21578569569664,
10.9595860883907));
#47129=CARTESIAN_POINT('Ctrl Pts',(0.92328693181771,-2.18609739534769,10.9649076076526));
#47130=CARTESIAN_POINT('Ctrl Pts',(0.995233349937592,-2.15283734677565,
10.9702291269145));
#47131=CARTESIAN_POINT('Ctrl Pts',(1.06730714142768,-2.11951841487639,10.975560067352));
#47132=CARTESIAN_POINT('Ctrl Pts',(1.13762127719207,-2.08261532012154,10.9808910077895));
#47133=CARTESIAN_POINT('Ctrl Pts',(1.20581113914771,-2.04235588456256,10.986221948227));
#47134=CARTESIAN_POINT('Ctrl Pts',(1.26326129296913,-2.00843719490262,10.9907132808));
#47135=CARTESIAN_POINT('Ctrl Pts',(1.31920397143183,-1.97213701067979,10.995204613373));
#47136=CARTESIAN_POINT('Ctrl Pts',(1.37343893525149,-1.93361411704488,10.999695945946));
#47137=CARTESIAN_POINT('Ctrl Pts',(1.43803180442143,-1.8877340416588,11.0050450424854));
#47138=CARTESIAN_POINT('Ctrl Pts',(1.50043956590866,-1.838531201315,11.0103941390249));
#47139=CARTESIAN_POINT('Ctrl Pts',(1.56030198093737,-1.78624068668892,11.0157432355643));
#47140=CARTESIAN_POINT('Ctrl Pts',(1.62007956202568,-1.73402427549485,11.0210847516389));
#47141=CARTESIAN_POINT('Ctrl Pts',(1.67731861367735,-1.67872918518825,11.0264262677134));
#47142=CARTESIAN_POINT('Ctrl Pts',(1.73168916755986,-1.62063280525104,11.031767783788));
#47143=CARTESIAN_POINT('Ctrl Pts',(1.78599747919602,-1.5626029328061,11.0371031850092));
#47144=CARTESIAN_POINT('Ctrl Pts',(1.83744350365328,-1.50177848304249,11.0424385862305));
#47145=CARTESIAN_POINT('Ctrl Pts',(1.88573269170631,-1.43847498342171,11.0477739874517));
#47146=CARTESIAN_POINT('Ctrl Pts',(1.93399167314639,-1.37521108240235,11.0531060511889));
#47147=CARTESIAN_POINT('Ctrl Pts',(1.97909745714498,-1.30947157937917,11.058438114926));
#47148=CARTESIAN_POINT('Ctrl Pts',(2.0207952858779,-1.24160560367358,11.0637701786631));
#47149=CARTESIAN_POINT('Ctrl Pts',(2.06247978565975,-1.17376132171794,11.0691005379753));
#47150=CARTESIAN_POINT('Ctrl Pts',(2.10075825055903,-1.10379231349086,11.0744308972876));
#47151=CARTESIAN_POINT('Ctrl Pts',(2.1354196543779,-1.03207604477412,11.0797612565998));
#47152=CARTESIAN_POINT('Ctrl Pts',(2.17008058021416,-0.960360765028534,
11.0850915424061));
#47153=CARTESIAN_POINT('Ctrl Pts',(2.20112434301785,-0.886898692362133,
11.0904218282124));
#47154=CARTESIAN_POINT('Ctrl Pts',(2.22838687424989,-0.812089897222463,
11.0957521140187));
#47155=CARTESIAN_POINT('Ctrl Pts',(2.25567509291515,-0.737210615380259,
11.1010874221525));
#47156=CARTESIAN_POINT('Ctrl Pts',(2.27917480399258,-0.660982514702551,
11.1064227302863));
#47157=CARTESIAN_POINT('Ctrl Pts',(2.29877114623207,-0.583822986658526,
11.1117580384201));
#47158=CARTESIAN_POINT('Ctrl Pts',(2.3183767394164,-0.506627033524114,11.11709586522));
#47159=CARTESIAN_POINT('Ctrl Pts',(2.33407520004438,-0.428499233640839,
11.1224336920198));
#47160=CARTESIAN_POINT('Ctrl Pts',(2.34580288183145,-0.349866977709081,
11.1277715188196));
#47161=CARTESIAN_POINT('Ctrl Pts',(2.35755035012552,-0.271102056369778,
11.1331183514016));
#47162=CARTESIAN_POINT('Ctrl Pts',(2.36531360899113,-0.191831442605272,
11.1384651839836));
#47163=CARTESIAN_POINT('Ctrl Pts',(2.36908098257407,-0.112487157070807,
11.1438120165656));
#47164=CARTESIAN_POINT('Ctrl Pts',(2.37213951654979,-0.0480716729824705,
11.1481528308635));
#47165=CARTESIAN_POINT('Ctrl Pts',(2.37256537656481,0.016392218425755,11.1524936451615));
#47166=CARTESIAN_POINT('Ctrl Pts',(2.37037751204224,0.0806753550002586,
11.1568344594594));
#47167=CARTESIAN_POINT('Ctrl Pts',(2.36768235674937,0.159863546953882,11.1621817597652));
#47168=CARTESIAN_POINT('Ctrl Pts',(2.36100990357596,0.239056903868901,11.167529060071));
#47169=CARTESIAN_POINT('Ctrl Pts',(2.35035851903795,0.317825257784452,11.1728763603767));
#47170=CARTESIAN_POINT('Ctrl Pts',(2.33972192171891,0.396484258320294,11.1782162370748));
#47171=CARTESIAN_POINT('Ctrl Pts',(2.32511742713896,0.474718970005106,11.1835561137728));
#47172=CARTESIAN_POINT('Ctrl Pts',(2.30659537861471,0.552101278619481,11.1888959904709));
#47173=CARTESIAN_POINT('Ctrl Pts',(2.28809370973354,0.62939844417701,11.1942299917507));
#47174=CARTESIAN_POINT('Ctrl Pts',(2.26568316195647,0.705844620125849,11.1995639930305));
#47175=CARTESIAN_POINT('Ctrl Pts',(2.23946541145361,0.781020315614714,11.2048979943104));
#47176=CARTESIAN_POINT('Ctrl Pts',(2.21326334452963,0.856151040656937,11.2102288047661));
#47177=CARTESIAN_POINT('Ctrl Pts',(2.18325874939859,0.93001235560192,11.2155596152219));
#47178=CARTESIAN_POINT('Ctrl Pts',(2.14960324258805,1.00219956194111,11.2208904256776));
#47179=CARTESIAN_POINT('Ctrl Pts',(2.11595756843179,1.07436567836333,11.2262196787057));
#47180=CARTESIAN_POINT('Ctrl Pts',(2.07866329785775,1.14485823605629,11.2315489317338));
#47181=CARTESIAN_POINT('Ctrl Pts',(2.03791975049785,1.21329351478971,11.236878184762));
#47182=CARTESIAN_POINT('Ctrl Pts',(1.99717563763221,1.28172974338012,11.2422075117582));
#47183=CARTESIAN_POINT('Ctrl Pts',(1.95298239238847,1.34810823714408,11.2475368387544));
#47184=CARTESIAN_POINT('Ctrl Pts',(1.90558401794835,1.41207209909403,11.2528661657506));
#47185=CARTESIAN_POINT('Ctrl Pts',(1.85813890409124,1.47609903564625,11.2582007479827));
#47186=CARTESIAN_POINT('Ctrl Pts',(1.80748262627876,1.53770620995198,11.2635353302148));
#47187=CARTESIAN_POINT('Ctrl Pts',(1.75390070327161,1.59656831534493,11.2688699124469));
#47188=CARTESIAN_POINT('Ctrl Pts',(1.70029220062007,1.65545961964941,11.2742071409315));
#47189=CARTESIAN_POINT('Ctrl Pts',(1.6437554920223,1.71160281372472,11.2795443694161));
#47190=CARTESIAN_POINT('Ctrl Pts',(1.5846125787407,1.76470990188097,11.2848815979007));
#47191=CARTESIAN_POINT('Ctrl Pts',(1.5253674895908,1.81790873835573,11.2902280470327));
#47192=CARTESIAN_POINT('Ctrl Pts',(1.46350756252603,1.86806069585571,11.2955744961648));
#47193=CARTESIAN_POINT('Ctrl Pts',(1.39938722291788,1.91491865697585,11.3009209452969));
#47194=CARTESIAN_POINT('Ctrl Pts',(1.34720926165235,1.9530493483485,11.3052716211889));
#47195=CARTESIAN_POINT('Ctrl Pts',(1.2935351519869,1.98899953936095,11.309622297081));
#47196=CARTESIAN_POINT('Ctrl Pts',(1.23856812126655,2.02265841690639,11.313972972973));
#47197=CARTESIAN_POINT('Ctrl Pts',(1.17182834791455,2.06352629405431,11.3192554690285));
#47198=CARTESIAN_POINT('Ctrl Pts',(1.10292632796187,2.10117133881163,11.324537965084));
#47199=CARTESIAN_POINT('Ctrl Pts',(1.03220941490833,2.13535518972245,11.3298204611394));
#47200=CARTESIAN_POINT('Ctrl Pts',(0.961594100115952,2.16948992904649,11.3350953678872));
#47201=CARTESIAN_POINT('Ctrl Pts',(0.889169494008856,2.20017313813373,11.340370274635));
#47202=CARTESIAN_POINT('Ctrl Pts',(0.8153105507563,2.2272105352493,11.3456451813828));
#47203=CARTESIAN_POINT('Ctrl Pts',(0.741533284605296,2.25421803299002,11.3509142548614));
#47204=CARTESIAN_POINT('Ctrl Pts',(0.666325277816863,2.27758756180128,11.35618332834));
#47205=CARTESIAN_POINT('Ctrl Pts',(0.59008317191016,2.29717215565757,11.3614524018187));
#47206=CARTESIAN_POINT('Ctrl Pts',(0.513886564346098,2.31674506218504,11.3667183309178));
#47207=CARTESIAN_POINT('Ctrl Pts',(0.436657543679518,2.33253739536388,11.371984260017));
#47208=CARTESIAN_POINT('Ctrl Pts',(0.358808370350743,2.34445187962266,11.3772501891162));
#47209=CARTESIAN_POINT('Ctrl Pts',(0.280980323372962,2.35636313058345,11.3825146891718));
#47210=CARTESIAN_POINT('Ctrl Pts',(0.202532930124588,2.36439854875748,11.3877791892273));
#47211=CARTESIAN_POINT('Ctrl Pts',(0.123887518991857,2.36851217964739,11.3930436892829));
#47212=CARTESIAN_POINT('Ctrl Pts',(0.045237860004629,2.3726260327258,11.3983084736885));
#47213=CARTESIAN_POINT('Ctrl Pts',(-0.0336093604692796,2.37281765462148,
11.4035732580942));
#47214=CARTESIAN_POINT('Ctrl Pts',(-0.112230456956044,2.36909315710283,
11.4088380424998));
#47215=CARTESIAN_POINT('Ctrl Pts',(-0.190941448627036,2.36536440100212,
11.414108846648));
#47216=CARTESIAN_POINT('Ctrl Pts',(-0.269425321212711,2.35771060679778,
11.4193796507963));
#47217=CARTESIAN_POINT('Ctrl Pts',(-0.34726182368926,2.34618995145491,11.4246504549445));
#47218=CARTESIAN_POINT('Ctrl Pts',(-0.425141988134603,2.3346628336622,11.4299242157221));
#47219=CARTESIAN_POINT('Ctrl Pts',(-0.502373590799942,2.31926463273651,
11.4351979764997));
#47220=CARTESIAN_POINT('Ctrl Pts',(-0.578547654010976,2.30010449209126,
11.4404717372772));
#47221=CARTESIAN_POINT('Ctrl Pts',(-0.654872977533989,2.28090630478381,
11.4457559702637));
#47222=CARTESIAN_POINT('Ctrl Pts',(-0.73013610921208,2.25793139694226,11.4510402032501));
#47223=CARTESIAN_POINT('Ctrl Pts',(-0.803944534133875,2.23133844329727,
11.4563244362366));
#47224=CARTESIAN_POINT('Ctrl Pts',(-0.872791415727006,2.20653311880011,
11.4612534529866));
#47225=CARTESIAN_POINT('Ctrl Pts',(-0.940372510114562,2.17858045132383,
11.4661824697365));
#47226=CARTESIAN_POINT('Ctrl Pts',(-1.00638901194834,2.14764504030104,11.4711114864865));
#47227=CARTESIAN_POINT('Ctrl Pts',(-1.07985541228931,2.11321859800581,11.4765967380188));
#47228=CARTESIAN_POINT('Ctrl Pts',(-1.15166315267971,2.07496716452492,11.4820819895511));
#47229=CARTESIAN_POINT('Ctrl Pts',(-1.22140116858542,2.03307089101147,11.4875672410834));
#47230=CARTESIAN_POINT('Ctrl Pts',(-1.2910301291608,1.99124013430242,11.4930439148563));
#47231=CARTESIAN_POINT('Ctrl Pts',(-1.35859543081844,1.9457760960418,11.4985205886293));
#47232=CARTESIAN_POINT('Ctrl Pts',(-1.42370896548185,1.89690559704657,11.5039972624022));
#47233=CARTESIAN_POINT('Ctrl Pts',(-1.48872157623438,1.84811084577277,11.5094654475048));
#47234=CARTESIAN_POINT('Ctrl Pts',(-1.5512896385893,1.79592040565499,11.5149336326073));
#47235=CARTESIAN_POINT('Ctrl Pts',(-1.61105366257491,1.74060453831534,11.5204018177098));
#47236=CARTESIAN_POINT('Ctrl Pts',(-1.67076303528782,1.68533925462702,11.5258650024249));
#47237=CARTESIAN_POINT('Ctrl Pts',(-1.72767314955874,1.62695452169227,11.53132818714));
#47238=CARTESIAN_POINT('Ctrl Pts',(-1.78145770591508,1.56576067920221,11.5367913718551));
#47239=CARTESIAN_POINT('Ctrl Pts',(-1.83520615804759,1.50460791460396,11.5422508892712));
#47240=CARTESIAN_POINT('Ctrl Pts',(-1.88583293825317,1.44065011779986,11.5477104066874));
#47241=CARTESIAN_POINT('Ctrl Pts',(-1.93304949521141,1.37423349965096,11.5531699241036));
#47242=CARTESIAN_POINT('Ctrl Pts',(-1.98024582745808,1.30784533035628,11.5586271029934));
#47243=CARTESIAN_POINT('Ctrl Pts',(-2.02403459094754,1.23900079045998,11.5640842818832));
#47244=CARTESIAN_POINT('Ctrl Pts',(-2.06416899572855,1.16807723185283,11.569541460773));
#47245=CARTESIAN_POINT('Ctrl Pts',(-2.10430706105056,1.09714720451654,11.574999137396));
#47246=CARTESIAN_POINT('Ctrl Pts',(-2.14078987938564,1.0241381548064,11.580456814019));
#47247=CARTESIAN_POINT('Ctrl Pts',(-2.17341566996079,0.949453731399744,
11.5859144906421));
#47248=CARTESIAN_POINT('Ctrl Pts',(-2.2060417007892,0.874768758024002,11.5913722074549));
#47249=CARTESIAN_POINT('Ctrl Pts',(-2.2348104786237,0.798408788636254,11.5968299242678));
#47250=CARTESIAN_POINT('Ctrl Pts',(-2.25956822195664,0.72079783075681,11.6022876410806));
#47251=CARTESIAN_POINT('Ctrl Pts',(-2.28434270277559,0.643134403946534,
11.6077490475859));
#47252=CARTESIAN_POINT('Ctrl Pts',(-2.30510060547981,0.564218716888628,
11.6132104540912));
#47253=CARTESIAN_POINT('Ctrl Pts',(-2.32173806871777,0.484489837629956,
11.6186718605965));
#47254=CARTESIAN_POINT('Ctrl Pts',(-2.33146425323691,0.437880701364198,
11.621864573731));
#47255=CARTESIAN_POINT('Ctrl Pts',(-2.33978322345457,0.39099388975932,11.6250572868655));
#47256=CARTESIAN_POINT('Ctrl Pts',(-2.34668236863852,0.343918483395542,
11.62825));
#47257=CARTESIAN_POINT('',(-0.439445221994028,2.33068358199191,11.62825));
#47258=CARTESIAN_POINT('Origin',(0.,0.,11.62825));
#47259=CARTESIAN_POINT('',(-2.37174991248389,0.000644307893693102,10.8485898919608));
#47260=CARTESIAN_POINT('Ctrl Pts',(-2.37174991248389,0.00064430789369313,
10.8485898919608));
#47261=CARTESIAN_POINT('Ctrl Pts',(-2.37177122382654,-0.0778044827509494,
10.8538838529935));
#47262=CARTESIAN_POINT('Ctrl Pts',(-2.36789607083802,-0.156407906642089,
10.8591778140261));
#47263=CARTESIAN_POINT('Ctrl Pts',(-2.36010456354706,-0.234743501772307,
10.8644717750587));
#47264=CARTESIAN_POINT('Ctrl Pts',(-2.35232391937685,-0.312969879392242,
10.8697583551141));
#47265=CARTESIAN_POINT('Ctrl Pts',(-2.34063780741033,-0.390928699789423,
10.8750449351695));
#47266=CARTESIAN_POINT('Ctrl Pts',(-2.32507835604017,-0.46819728830222,
10.8803315152249));
#47267=CARTESIAN_POINT('Ctrl Pts',(-2.30953561317691,-0.545382901990649,
10.8856124182897));
#47268=CARTESIAN_POINT('Ctrl Pts',(-2.29012788664027,-0.621879291708473,
10.8908933213545));
#47269=CARTESIAN_POINT('Ctrl Pts',(-2.26693895282476,-0.697270282362413,
10.8961742244193));
#47270=CARTESIAN_POINT('Ctrl Pts',(-2.24376319966359,-0.772618420568053,
10.9014521258041));
#47271=CARTESIAN_POINT('Ctrl Pts',(-2.21681064342658,-0.846861952431962,
10.906730027189));
#47272=CARTESIAN_POINT('Ctrl Pts',(-2.18621553114936,-0.919597582566052,
10.9120079285738));
#47273=CARTESIAN_POINT('Ctrl Pts',(-2.15562794303006,-0.992315325059684,
10.9172845319813));
#47274=CARTESIAN_POINT('Ctrl Pts',(-2.12139976213312,-1.06352546359016,
10.9225611353887));
#47275=CARTESIAN_POINT('Ctrl Pts',(-2.08371365013264,-1.13284398164571,
10.9278377387962));
#47276=CARTESIAN_POINT('Ctrl Pts',(-2.04602465333876,-1.20216780588948,
10.9331147461166));
#47277=CARTESIAN_POINT('Ctrl Pts',(-2.00487742936107,-1.26959930511781,
10.9383917534371));
#47278=CARTESIAN_POINT('Ctrl Pts',(-1.96050016921421,-1.3347798129321,10.9436687607576));
#47279=CARTESIAN_POINT('Ctrl Pts',(-1.91607700733521,-1.40002774037078,
10.948951226364));
#47280=CARTESIAN_POINT('Ctrl Pts',(-1.86841741009435,-1.46301963567997,
10.9542336919704));
#47281=CARTESIAN_POINT('Ctrl Pts',(-1.81779196223019,-1.52342720356153,
10.9595161575769));
#47282=CARTESIAN_POINT('Ctrl Pts',(-1.76713708810984,-1.58386988359803,
10.9648016936388));
#47283=CARTESIAN_POINT('Ctrl Pts',(-1.71351325705018,-1.641724898701,10.9700872297008));
#47284=CARTESIAN_POINT('Ctrl Pts',(-1.65722850576611,-1.69670025112753,
10.9753727657628));
#47285=CARTESIAN_POINT('Ctrl Pts',(-1.60085049685053,-1.75176669165593,
10.9806670593756));
#47286=CARTESIAN_POINT('Ctrl Pts',(-1.54180312567185,-1.8039436332366,10.9859613529885));
#47287=CARTESIAN_POINT('Ctrl Pts',(-1.48042760659234,-1.85297926705597,
10.9912556466014));
#47288=CARTESIAN_POINT('Ctrl Pts',(-1.45085410415822,-1.87660685437197,
10.9938066768394));
#47289=CARTESIAN_POINT('Ctrl Pts',(-1.42074049814803,-1.89950575430157,
10.9963577070774));
#47290=CARTESIAN_POINT('Ctrl Pts',(-1.39012715941737,-1.92165151449221,
10.9989087373155));
#47291=CARTESIAN_POINT('Ctrl Pts',(-1.3259451246521,-1.96808094719684,11.0042570697161));
#47292=CARTESIAN_POINT('Ctrl Pts',(-1.25931844617298,-2.01137536844812,
11.0096054021168));
#47293=CARTESIAN_POINT('Ctrl Pts',(-1.1905852556703,-2.05126907339834,11.0149537345174));
#47294=CARTESIAN_POINT('Ctrl Pts',(-1.12194971603061,-2.09110610042211,
11.0202944684162));
#47295=CARTESIAN_POINT('Ctrl Pts',(-1.05121400829883,-2.12755177584933,
11.025635202315));
#47296=CARTESIAN_POINT('Ctrl Pts',(-0.978746618937616,-2.16038263240987,
11.0309759362138));
#47297=CARTESIAN_POINT('Ctrl Pts',(-0.906362475006621,-2.19317577519593,
11.0363105350539));
#47298=CARTESIAN_POINT('Ctrl Pts',(-0.832251025353797,-2.22236216150651,
11.0416451338939));
#47299=CARTESIAN_POINT('Ctrl Pts',(-0.756805516214812,-2.24776410531151,
11.0469797327339));
#47300=CARTESIAN_POINT('Ctrl Pts',(-0.681407392065659,-2.2731500949416,
11.0523109810775));
#47301=CARTESIAN_POINT('Ctrl Pts',(-0.604677311999744,-2.29475621279531,
11.0576422294211));
#47302=CARTESIAN_POINT('Ctrl Pts',(-0.527027582336053,-2.31245324059904,
11.0629734777647));
#47303=CARTESIAN_POINT('Ctrl Pts',(-0.449402848386129,-2.33014457166895,
11.0683030099612));
#47304=CARTESIAN_POINT('Ctrl Pts',(-0.370859506435195,-2.34392920874058,
11.0736325421577));
#47305=CARTESIAN_POINT('Ctrl Pts',(-0.291822669626693,-2.3537284448279,
11.0789620743542));
#47306=CARTESIAN_POINT('Ctrl Pts',(-0.212787077779679,-2.36352752656097,
11.0842915226017));
#47307=CARTESIAN_POINT('Ctrl Pts',(-0.133258468712647,-2.369341276333,11.0896209708492));
#47308=CARTESIAN_POINT('Ctrl Pts',(-0.0536682963514557,-2.37114271533089,
11.0949504190967));
#47309=CARTESIAN_POINT('Ctrl Pts',(0.0259969974664904,-2.37294585462314,
11.1002848975622));
#47310=CARTESIAN_POINT('Ctrl Pts',(0.105723504207312,-2.37072910816615,
11.1056193760277));
#47311=CARTESIAN_POINT('Ctrl Pts',(0.185079153489236,-2.36451766105557,
11.1109538544932));
#47312=CARTESIAN_POINT('Ctrl Pts',(0.264472156223381,-2.35830329015828,
11.116290843948));
#47313=CARTESIAN_POINT('Ctrl Pts',(0.343493491352376,-2.34809053137083,
11.1216278334028));
#47314=CARTESIAN_POINT('Ctrl Pts',(0.421718057243618,-2.33395628551493,
11.1269648228575));
#47315=CARTESIAN_POINT('Ctrl Pts',(0.500075292527004,-2.31979806788259,
11.1323108638825));
#47316=CARTESIAN_POINT('Ctrl Pts',(0.577632604273632,-2.30170518061197,
11.1376569049075));
#47317=CARTESIAN_POINT('Ctrl Pts',(0.653977177730247,-2.27980523587169,
11.1430029459324));
#47318=CARTESIAN_POINT('Ctrl Pts',(0.717007412965831,-2.26172459691953,
11.1474166482838));
#47319=CARTESIAN_POINT('Ctrl Pts',(0.77921117835256,-2.24104996791998,11.1518303506352));
#47320=CARTESIAN_POINT('Ctrl Pts',(0.840366763087148,-2.21787776173495,
11.1562440529866));
#47321=CARTESIAN_POINT('Ctrl Pts',(0.914445461652096,-2.18980891267537,
11.1615904383979));
#47322=CARTESIAN_POINT('Ctrl Pts',(0.987248208124766,-2.15797464747206,
11.1669368238092));
#47323=CARTESIAN_POINT('Ctrl Pts',(1.05836734865268,-2.12251186517435,11.1722832092205));
#47324=CARTESIAN_POINT('Ctrl Pts',(1.12938749829716,-2.08709844359898,11.1776221529866));
#47325=CARTESIAN_POINT('Ctrl Pts',(1.19872828307868,-2.04806674295669,11.1829610967526));
#47326=CARTESIAN_POINT('Ctrl Pts',(1.26600072393684,-2.00560221118032,11.1883000405187));
#47327=CARTESIAN_POINT('Ctrl Pts',(1.33319888874628,-1.96318456483862,11.1936330895135));
#47328=CARTESIAN_POINT('Ctrl Pts',(1.39833285649444,-1.91734186791345,11.1989661385083));
#47329=CARTESIAN_POINT('Ctrl Pts',(1.46103833856832,-1.86830539145332,11.2042991875032));
#47330=CARTESIAN_POINT('Ctrl Pts',(1.52370615624454,-1.81929836902636,11.2096290331724));
#47331=CARTESIAN_POINT('Ctrl Pts',(1.58394801820038,-1.76710166180247,11.2149588788416));
#47332=CARTESIAN_POINT('Ctrl Pts',(1.64142971969882,-1.71198905889887,11.2202887245108));
#47333=CARTESIAN_POINT('Ctrl Pts',(1.69889450588698,-1.6568926741439,11.2256170017506));
#47334=CARTESIAN_POINT('Ctrl Pts',(1.75360040901508,-1.59888242016868,11.2309452789903));
#47335=CARTESIAN_POINT('Ctrl Pts',(1.80524844651054,-1.53827049275193,11.2362735562301));
#47336=CARTESIAN_POINT('Ctrl Pts',(1.85689710878867,-1.47765783211697,11.2416018979256));
#47337=CARTESIAN_POINT('Ctrl Pts',(1.90548753113069,-1.41444379101006,11.2469302396212));
#47338=CARTESIAN_POINT('Ctrl Pts',(1.95076051625495,-1.34897422907953,11.2522585813167));
#47339=CARTESIAN_POINT('Ctrl Pts',(1.99607824377803,-1.28343996487143,11.2575921889074));
#47340=CARTESIAN_POINT('Ctrl Pts',(2.03807172035962,-1.21564611154979,11.262925796498));
#47341=CARTESIAN_POINT('Ctrl Pts',(2.07652502630167,-1.14596765994632,11.2682594040886));
#47342=CARTESIAN_POINT('Ctrl Pts',(2.11499736363482,-1.07625472293695,11.2735956513995));
#47343=CARTESIAN_POINT('Ctrl Pts',(2.14992583517356,-1.00465574837578,11.2789318987104));
#47344=CARTESIAN_POINT('Ctrl Pts',(2.18114159737732,-0.931568244784202,
11.2842681460214));
#47345=CARTESIAN_POINT('Ctrl Pts',(2.21241159031212,-0.858353767238774,
11.2896136639242));
#47346=CARTESIAN_POINT('Ctrl Pts',(2.23995582575665,-0.783646031814463,
11.294959181827));
#47347=CARTESIAN_POINT('Ctrl Pts',(2.26365460363261,-0.707860083599078,
11.3003046997298));
#47348=CARTESIAN_POINT('Ctrl Pts',(2.28327187527456,-0.645126319834312,
11.3047295893725));
#47349=CARTESIAN_POINT('Ctrl Pts',(2.30025508348975,-0.581654154374832,
11.3091544790151));
#47350=CARTESIAN_POINT('Ctrl Pts',(2.31456296300781,-0.51768364159252,11.3135793686578));
#47351=CARTESIAN_POINT('Ctrl Pts',(2.33164103473651,-0.441327602639413,
11.3188609746857));
#47352=CARTESIAN_POINT('Ctrl Pts',(2.34497176150638,-0.363967864181439,
11.3241425807135));
#47353=CARTESIAN_POINT('Ctrl Pts',(2.35444182868038,-0.286010031048158,
11.3294241867414));
#47354=CARTESIAN_POINT('Ctrl Pts',(2.36389825649962,-0.208164477429283,
11.3346981858857));
#47355=CARTESIAN_POINT('Ctrl Pts',(2.36950500365836,-0.129723009269663,
11.33997218503));
#47356=CARTESIAN_POINT('Ctrl Pts',(2.37119938729804,-0.0511031131870544,
11.3452461841743));
#47357=CARTESIAN_POINT('Ctrl Pts',(2.37289189060657,0.0274295349804628,
11.3505143305326));
#47358=CARTESIAN_POINT('Ctrl Pts',(2.37068064217068,0.106139742249119,11.3557824768908));
#47359=CARTESIAN_POINT('Ctrl Pts',(2.36455474368832,0.184604784881244,11.3610506232491));
#47360=CARTESIAN_POINT('Ctrl Pts',(2.35843251699248,0.26302279655361,11.3663156119467));
#47361=CARTESIAN_POINT('Ctrl Pts',(2.34840033150624,0.341195459410748,11.3715806006443));
#47362=CARTESIAN_POINT('Ctrl Pts',(2.33449936041767,0.418701323988221,11.3768455893419));
#47363=CARTESIAN_POINT('Ctrl Pts',(2.32060219488859,0.496185970394946,11.3821091366849));
#47364=CARTESIAN_POINT('Ctrl Pts',(2.3028384299805,0.573003710209475,11.387372684028));
#47365=CARTESIAN_POINT('Ctrl Pts',(2.28130073672659,0.648741097134066,11.3926362313711));
#47366=CARTESIAN_POINT('Ctrl Pts',(2.2597619264151,0.724482412196269,11.3979000517093));
#47367=CARTESIAN_POINT('Ctrl Pts',(2.23444893155355,0.799142803430474,11.4031638720475));
#47368=CARTESIAN_POINT('Ctrl Pts',(2.20550445712356,0.872323421735368,11.4084276923857));
#47369=CARTESIAN_POINT('Ctrl Pts',(2.17652683422226,0.945587849667984,11.4136975410799));
#47370=CARTESIAN_POINT('Ctrl Pts',(2.14390960310454,1.01736867458185,11.4189673897742));
#47371=CARTESIAN_POINT('Ctrl Pts',(2.10784363126702,1.0872871233612,11.4242372384684));
#47372=CARTESIAN_POINT('Ctrl Pts',(2.07175748752627,1.15724467792671,11.429510034619));
#47373=CARTESIAN_POINT('Ctrl Pts',(2.03221900575049,1.22533737006819,11.4347828307696));
#47374=CARTESIAN_POINT('Ctrl Pts',(1.98946363971034,1.29121357209816,11.4400556269202));
#47375=CARTESIAN_POINT('Ctrl Pts',(1.946622945094,1.3572212458718,11.4453389461988));
#47376=CARTESIAN_POINT('Ctrl Pts',(1.90055282321152,1.42100320556413,11.4506222654773));
#47377=CARTESIAN_POINT('Ctrl Pts',(1.85153028639175,1.48223940747575,11.4559055847559));
#47378=CARTESIAN_POINT('Ctrl Pts',(1.80510845082124,1.54022695933492,11.4609086179469));
#47379=CARTESIAN_POINT('Ctrl Pts',(1.75603972614395,1.59593174530661,11.4659116511379));
#47380=CARTESIAN_POINT('Ctrl Pts',(1.70458831036001,1.64911393017098,11.4709146843289));
#47381=CARTESIAN_POINT('Ctrl Pts',(1.64818248118368,1.70741718944924,11.4763994748101));
#47382=CARTESIAN_POINT('Ctrl Pts',(1.58869775148269,1.76291086987612,11.4818842652913));
#47383=CARTESIAN_POINT('Ctrl Pts',(1.52643780178982,1.81526463629055,11.4873690557724));
#47384=CARTESIAN_POINT('Ctrl Pts',(1.46427549351293,1.86753629701891,11.4928452445327));
#47385=CARTESIAN_POINT('Ctrl Pts',(1.39934695251003,1.91667755805281,11.498321433293));
#47386=CARTESIAN_POINT('Ctrl Pts',(1.33199256123157,1.96239493459491,11.5037976220533));
#47387=CARTESIAN_POINT('Ctrl Pts',(1.26474295129913,2.00804118989072,11.5092652916597));
#47388=CARTESIAN_POINT('Ctrl Pts',(1.19507536319021,2.05027392108357,11.514732961266));
#47389=CARTESIAN_POINT('Ctrl Pts',(1.12336198797659,2.08884080448206,11.5202006308724));
#47390=CARTESIAN_POINT('Ctrl Pts',(1.05171442543819,2.12737229434674,11.5256632826984));
#47391=CARTESIAN_POINT('Ctrl Pts',(0.978025191487546,2.16224442009277,11.5311259345244));
#47392=CARTESIAN_POINT('Ctrl Pts',(0.90269362279425,2.19324925301859,11.5365885863504));
#47393=CARTESIAN_POINT('Ctrl Pts',(0.827412842259987,2.22423318264434,11.5420475552844));
#47394=CARTESIAN_POINT('Ctrl Pts',(0.750492331645188,2.25135483974438,11.5475065242184));
#47395=CARTESIAN_POINT('Ctrl Pts',(0.67235311416707,2.27445363821069,11.5529654931525));
#47396=CARTESIAN_POINT('Ctrl Pts',(0.594247567815922,2.29754248312741,11.5584221097513));
#47397=CARTESIAN_POINT('Ctrl Pts',(0.514924777329727,2.31661179547297,11.56387872635));
#47398=CARTESIAN_POINT('Ctrl Pts',(0.434821674870552,2.33155059425327,11.5693353429488));
#47399=CARTESIAN_POINT('Ctrl Pts',(0.354711340293603,2.34649074178472,11.5747924521988));
#47400=CARTESIAN_POINT('Ctrl Pts',(0.273820980146343,2.35729954199481,11.5802495614489));
#47401=CARTESIAN_POINT('Ctrl Pts',(0.192597799839124,2.36391711995094,11.5857066706989));
#47402=CARTESIAN_POINT('Ctrl Pts',(0.111374163091576,2.37053473509509,11.5911638106156));
#47403=CARTESIAN_POINT('Ctrl Pts',(0.0298181378171431,2.372961052068,11.5966209505323));
#47404=CARTESIAN_POINT('Ctrl Pts',(-0.0516193872324029,2.37118820454256,
11.602078090449));
#47405=CARTESIAN_POINT('Ctrl Pts',(-0.133112285751584,2.36941415156891,
11.6075389409496));
#47406=CARTESIAN_POINT('Ctrl Pts',(-0.214486086717864,2.3634352459725,11.6129997914503));
#47407=CARTESIAN_POINT('Ctrl Pts',(-0.295291847603898,2.3532957288107,11.6184606419509));
#47408=CARTESIAN_POINT('Ctrl Pts',(-0.343577154422689,2.3472368823648,11.6217237613006));
#47409=CARTESIAN_POINT('Ctrl Pts',(-0.391659720980486,2.33969343226212,
11.6249868806503));
#47410=CARTESIAN_POINT('Ctrl Pts',(-0.439445221994028,2.33068358199191,
11.62825));
#47411=CARTESIAN_POINT('Ctrl Pts',(-2.37174994708504,0.000501001099097663,
10.846534127968));
#47412=CARTESIAN_POINT('Ctrl Pts',(-2.37174721579639,0.0134309801352372,
10.8456327823122));
#47413=CARTESIAN_POINT('Ctrl Pts',(-2.37163874962865,0.0263610865209047,
10.8447359062959));
#47414=CARTESIAN_POINT('Ctrl Pts',(-2.37122058518967,0.0516002056234556,
10.8429947803213));
#47415=CARTESIAN_POINT('Ctrl Pts',(-2.3709207720263,0.0639089482834945,
10.84215009231));
#47416=CARTESIAN_POINT('Ctrl Pts',(-2.37019595250979,0.086453069150876,
10.8406117875281));
#47417=CARTESIAN_POINT('Ctrl Pts',(-2.36980045945753,0.0966891034644412,
10.8399166518587));
#47418=CARTESIAN_POINT('Ctrl Pts',(-2.36880781812163,0.118685419646535,
10.8384304507506));
#47419=CARTESIAN_POINT('Ctrl Pts',(-2.36818938716719,0.13044443017894,10.8376405618378));
#47420=CARTESIAN_POINT('Ctrl Pts',(-2.36687173668857,0.152382158825592,
10.8361747513223));
#47421=CARTESIAN_POINT('Ctrl Pts',(-2.36619437722359,0.162561724707678,
10.835497728382));
#47422=CARTESIAN_POINT('Ctrl Pts',(-2.36545134966486,0.172736721251459,
10.8348238720555));
#47423=CARTESIAN_POINT('Origin',(0.,0.,11.5));
#47424=CARTESIAN_POINT('',(-2.86802679864211,0.000931424361933773,11.1319730730322));
#47425=CARTESIAN_POINT('Ctrl Pts',(-0.439445221994028,2.33068358199191,
11.62825));
#47426=CARTESIAN_POINT('Ctrl Pts',(-0.240507280203547,2.37702795048113,
11.6195679168283));
#47427=CARTESIAN_POINT('Ctrl Pts',(-0.0361575228823814,2.39677384679906,
11.6116630415941));
#47428=CARTESIAN_POINT('Ctrl Pts',(0.38478462472991,2.38385320910818,11.5950312564841));
#47429=CARTESIAN_POINT('Ctrl Pts',(0.600009392259926,2.347949842227,11.5862993207748));
#47430=CARTESIAN_POINT('Ctrl Pts',(1.11765369336044,2.18962607273897,11.5630931646838));
#47431=CARTESIAN_POINT('Ctrl Pts',(1.40746702139056,2.03397333167281,11.547868232976));
#47432=CARTESIAN_POINT('Ctrl Pts',(1.95712023912967,1.57686556379433,11.5171288884504));
#47433=CARTESIAN_POINT('Ctrl Pts',(2.14314882880409,1.29900143794958,11.506029731789));
#47434=CARTESIAN_POINT('Ctrl Pts',(2.39172992067706,0.825805923776539,11.4861578388178));
#47435=CARTESIAN_POINT('Ctrl Pts',(2.48167644349775,0.548774870720514,11.4747308319184));
#47436=CARTESIAN_POINT('Ctrl Pts',(2.56075430605598,0.0142339080762581,
11.4516318992604));
#47437=CARTESIAN_POINT('Ctrl Pts',(2.57530303238998,-0.333395071522134,
11.4358158642582));
#47438=CARTESIAN_POINT('Ctrl Pts',(2.43710470439177,-0.874911153872938,
11.4148550733305));
#47439=CARTESIAN_POINT('Ctrl Pts',(2.38775837133174,-1.01518848497531,11.4096305966607));
#47440=CARTESIAN_POINT('Ctrl Pts',(2.20245412277555,-1.42582454691614,11.3937382959454));
#47441=CARTESIAN_POINT('Ctrl Pts',(2.03065015867802,-1.67833993794217,11.3829065162613));
#47442=CARTESIAN_POINT('Ctrl Pts',(1.57762541566582,-2.14937217153313,11.3569961163812));
#47443=CARTESIAN_POINT('Ctrl Pts',(1.2855517434416,-2.35320921048462,11.3416110035159));
#47444=CARTESIAN_POINT('Ctrl Pts',(0.687481433266787,-2.61091912218133,
11.3167784573464));
#47445=CARTESIAN_POINT('Ctrl Pts',(0.39320028291873,-2.68074961248442,11.3071650484887));
#47446=CARTESIAN_POINT('Ctrl Pts',(-0.26155692159266,-2.7262052030806,11.2845788353831));
#47447=CARTESIAN_POINT('Ctrl Pts',(-0.620457783435796,-2.68111934069518,
11.2712031183861));
#47448=CARTESIAN_POINT('Ctrl Pts',(-1.18549877043465,-2.49567016439237,
11.2473229739679));
#47449=CARTESIAN_POINT('Ctrl Pts',(-1.49718036941518,-2.36307019900528,
11.2332600373849));
#47450=CARTESIAN_POINT('Ctrl Pts',(-2.0933840473706,-1.8819605586974,11.2071778307903));
#47451=CARTESIAN_POINT('Ctrl Pts',(-2.32305937208553,-1.60866780784321,
11.1964123534349));
#47452=CARTESIAN_POINT('Ctrl Pts',(-2.60441312869722,-1.11220399175858,
11.1764267582063));
#47453=CARTESIAN_POINT('Ctrl Pts',(-2.69005811846215,-0.910752895230764,
11.1683028423465));
#47454=CARTESIAN_POINT('Ctrl Pts',(-2.81977109542483,-0.473542869844156,
11.150669348876));
#47455=CARTESIAN_POINT('Ctrl Pts',(-2.85892360397332,-0.237243928705007,
11.1411444695169));
#47456=CARTESIAN_POINT('Ctrl Pts',(-2.86761958932067,0.000821401650878822,
11.1323802930381));
#47457=CARTESIAN_POINT('Ctrl Pts',(0.261350361647427,2.92782130397338,11.0605371920139));
#47458=CARTESIAN_POINT('Ctrl Pts',(0.163402798461412,2.92403748423913,11.0730146348275));
#47459=CARTESIAN_POINT('Ctrl Pts',(0.0658923488504137,2.91546186050777,
11.0854003458105));
#47460=CARTESIAN_POINT('Ctrl Pts',(-0.0307627309535459,2.90211667593812,
11.0977202846083));
#47461=CARTESIAN_POINT('Ctrl Pts',(-0.126342250004264,2.88891999423866,
11.1099031292909));
#47462=CARTESIAN_POINT('Ctrl Pts',(-0.221085044441188,2.87105918456392,
11.1220217004903));
#47463=CARTESIAN_POINT('Ctrl Pts',(-0.314574853355365,2.84854913007817,
11.1341337287248));
#47464=CARTESIAN_POINT('Ctrl Pts',(-0.39017932206751,2.83034542713084,11.1439286301192));
#47465=CARTESIAN_POINT('Ctrl Pts',(-0.464964087502808,2.80910118651745,
11.1537198864481));
#47466=CARTESIAN_POINT('Ctrl Pts',(-0.538705163844275,2.78482060950474,
11.1635534412447));
#47467=CARTESIAN_POINT('Ctrl Pts',(-0.594010971100378,2.7666101767452,11.1709286073421));
#47468=CARTESIAN_POINT('Ctrl Pts',(-0.648729636076866,2.74669177190032,
11.1783278575236));
#47469=CARTESIAN_POINT('Ctrl Pts',(-0.702765788630647,2.7250651160814,11.1857754814952));
#47470=CARTESIAN_POINT('Ctrl Pts',(-0.718629674298013,2.71871598167666,
11.1879619483252));
#47471=CARTESIAN_POINT('Ctrl Pts',(-0.734434730791572,2.71221960024673,
11.1901526111987));
#47472=CARTESIAN_POINT('Ctrl Pts',(-0.750178534250807,2.70557592300405,
11.1923481504307));
#47473=CARTESIAN_POINT('Ctrl Pts',(-0.763358987334736,2.7000139457837,11.1941862197331));
#47474=CARTESIAN_POINT('Ctrl Pts',(-0.776488354911949,2.69435215882939,
11.196026571624));
#47475=CARTESIAN_POINT('Ctrl Pts',(-0.78956312197429,2.688591939758,11.1978692853271));
#47476=CARTESIAN_POINT('Ctrl Pts',(-0.872801830852324,2.65192029612018,
11.2096006690485));
#47477=CARTESIAN_POINT('Ctrl Pts',(-0.95385898559835,2.61124905776464,11.2214310006084));
#47478=CARTESIAN_POINT('Ctrl Pts',(-1.03246252049652,2.5666448806666,11.2334778512215));
#47479=CARTESIAN_POINT('Ctrl Pts',(-1.07746886343747,2.54110568712176,11.2403755650553));
#47480=CARTESIAN_POINT('Ctrl Pts',(-1.1216710063815,2.51427636072537,11.2473445633387));
#47481=CARTESIAN_POINT('Ctrl Pts',(-1.16501856324264,2.48616221908335,11.2544088373727));
#47482=CARTESIAN_POINT('Ctrl Pts',(-1.24266078345783,2.43580541619539,11.2670620515309));
#47483=CARTESIAN_POINT('Ctrl Pts',(-1.31756840157884,2.38132606317727,11.2800208331917));
#47484=CARTESIAN_POINT('Ctrl Pts',(-1.38952099343943,2.32292969176299,11.2931991310621));
#47485=CARTESIAN_POINT('Ctrl Pts',(-1.46277813137534,2.26347455713851,11.3066163598219));
#47486=CARTESIAN_POINT('Ctrl Pts',(-1.53297200293144,2.19995698204504,11.3202605352119));
#47487=CARTESIAN_POINT('Ctrl Pts',(-1.59978151883497,2.13260008847238,11.3340510047343));
#47488=CARTESIAN_POINT('Ctrl Pts',(-1.61331518168127,2.11895554284653,11.3368445523672));
#47489=CARTESIAN_POINT('Ctrl Pts',(-1.6267132492287,2.10514961901921,11.3396449260006));
#47490=CARTESIAN_POINT('Ctrl Pts',(-1.63995148862121,2.09120707263336,11.3424470079295));
#47491=CARTESIAN_POINT('Ctrl Pts',(-1.70171752547037,2.02615493025203,11.3555207627199));
#47492=CARTESIAN_POINT('Ctrl Pts',(-1.76008871104665,1.95805043285538,11.3686460413715));
#47493=CARTESIAN_POINT('Ctrl Pts',(-1.81484660700543,1.88716888932194,11.3817802567806));
#47494=CARTESIAN_POINT('Ctrl Pts',(-1.86940990513711,1.81653924360364,11.394867796003));
#47495=CARTESIAN_POINT('Ctrl Pts',(-1.92038481010494,1.74315138575278,11.4079639534782));
#47496=CARTESIAN_POINT('Ctrl Pts',(-1.96751101622977,1.6672954795621,11.4210518006067));
#47497=CARTESIAN_POINT('Ctrl Pts',(-2.01384320160487,1.59271765553543,11.4339191330144));
#47498=CARTESIAN_POINT('Ctrl Pts',(-2.05645453396309,1.51575388926486,11.4467782845076));
#47499=CARTESIAN_POINT('Ctrl Pts',(-2.09506613628272,1.43670608847597,11.4596404781877));
#47500=CARTESIAN_POINT('Ctrl Pts',(-2.11584570714243,1.39416500550823,11.4665625132479));
#47501=CARTESIAN_POINT('Ctrl Pts',(-2.13546637970218,1.35102082416007,11.4734859152846));
#47502=CARTESIAN_POINT('Ctrl Pts',(-2.15388188633923,1.30732413101464,11.4804159938924));
#47503=CARTESIAN_POINT('Ctrl Pts',(-2.15933961437786,1.29437392160277,11.4824698328159));
#47504=CARTESIAN_POINT('Ctrl Pts',(-2.16469222289073,1.28137334258626,11.484524567937));
#47505=CARTESIAN_POINT('Ctrl Pts',(-2.16993611370384,1.26832965527801,11.4865794518199));
#47506=CARTESIAN_POINT('Ctrl Pts',(-2.20175895320132,1.18917332223087,11.4990496275584));
#47507=CARTESIAN_POINT('Ctrl Pts',(-2.22947962309921,1.1086815952271,11.511483675394));
#47508=CARTESIAN_POINT('Ctrl Pts',(-2.25295126705805,1.02716409885249,11.5239435592641));
#47509=CARTESIAN_POINT('Ctrl Pts',(-2.2760786989779,0.946842057883126,11.5362207187353));
#47510=CARTESIAN_POINT('Ctrl Pts',(-2.29508104728318,0.865524217715744,
11.5485231608414));
#47511=CARTESIAN_POINT('Ctrl Pts',(-2.30979972814699,0.783500714904634,
11.5609329335986));
#47512=CARTESIAN_POINT('Ctrl Pts',(-2.32408698795012,0.703881413048161,
11.5729789619839));
#47513=CARTESIAN_POINT('Ctrl Pts',(-2.33433845898191,0.623597301201896,
11.5851264291944));
#47514=CARTESIAN_POINT('Ctrl Pts',(-2.34038703160473,0.542906490436884,
11.5974682280848));
#47515=CARTESIAN_POINT('Ctrl Pts',(-2.34534204029777,0.476804338124139,
11.6075786664647));
#47516=CARTESIAN_POINT('Ctrl Pts',(-2.3474763612765,0.410429125649973,11.6178199429796));
#47517=CARTESIAN_POINT('Ctrl Pts',(-2.34668236863853,0.343918483395475,
11.62825));
#47518=CARTESIAN_POINT('Ctrl Pts',(-2.86819969387402,0.00077918580006163,
11.1318002002877));
#47519=CARTESIAN_POINT('Ctrl Pts',(-2.86975559680702,0.0427595453757233,
11.1302328928719));
#47520=CARTESIAN_POINT('Ctrl Pts',(-2.87035280117414,0.0847243061035006,
11.1287027854165));
#47521=CARTESIAN_POINT('Ctrl Pts',(-2.8699874816256,0.12665023816086,11.1272193909883));
#47522=CARTESIAN_POINT('Ctrl Pts',(-2.86921038481711,0.21583382585658,11.1240639587632));
#47523=CARTESIAN_POINT('Ctrl Pts',(-2.86408052121998,0.304845801774181,
11.12111909617));
#47524=CARTESIAN_POINT('Ctrl Pts',(-2.85472489574556,0.393465375926996,
11.1182871009688));
#47525=CARTESIAN_POINT('Ctrl Pts',(-2.85411091907604,0.399281165704107,
11.1181012471222));
#47526=CARTESIAN_POINT('Ctrl Pts',(-2.85347873052284,0.405095279363024,
11.1179158793767));
#47527=CARTESIAN_POINT('Ctrl Pts',(-2.8528283606803,0.410907660087458,11.1177309701174));
#47528=CARTESIAN_POINT('Ctrl Pts',(-2.84203922631273,0.50733057598794,11.1146634680387));
#47529=CARTESIAN_POINT('Ctrl Pts',(-2.82624903601188,0.603272528673326,
11.1117216154067));
#47530=CARTESIAN_POINT('Ctrl Pts',(-2.80558094060506,0.698407783990052,
11.1087964708405));
#47531=CARTESIAN_POINT('Ctrl Pts',(-2.79250101933245,0.758614669302825,
11.1069452765295));
#47532=CARTESIAN_POINT('Ctrl Pts',(-2.77746677601657,0.818497584311128,
11.1051011503189));
#47533=CARTESIAN_POINT('Ctrl Pts',(-2.76050507677153,0.877965201122309,
11.1032412642294));
#47534=CARTESIAN_POINT('Ctrl Pts',(-2.74977650746049,0.915579501405769,
11.1020648539811));
#47535=CARTESIAN_POINT('Ctrl Pts',(-2.73827675238308,0.953027514721806,
11.100882217146));
#47536=CARTESIAN_POINT('Ctrl Pts',(-2.72601228780754,0.990284803198791,
11.0996884676428));
#47537=CARTESIAN_POINT('Ctrl Pts',(-2.72123391409771,1.00480066295458,11.099223369374));
#47538=CARTESIAN_POINT('Ctrl Pts',(-2.71633888424499,1.019289212608,11.0987565384275));
#47539=CARTESIAN_POINT('Ctrl Pts',(-2.71132938212565,1.03374376926027,11.0982878849096));
#47540=CARTESIAN_POINT('Ctrl Pts',(-2.67885568285608,1.12744428372618,11.0952498757343));
#47541=CARTESIAN_POINT('Ctrl Pts',(-2.64168416110042,1.21939768587777,11.0921427423104));
#47542=CARTESIAN_POINT('Ctrl Pts',(-2.60005965515925,1.30923023475234,11.0889187544872));
#47543=CARTESIAN_POINT('Ctrl Pts',(-2.55796403279677,1.40007953056444,11.0856582767749));
#47544=CARTESIAN_POINT('Ctrl Pts',(-2.51131407129837,1.48875923668141,11.0822782090206));
#47545=CARTESIAN_POINT('Ctrl Pts',(-2.4603548397369,1.57488396663604,11.0787664513456));
#47546=CARTESIAN_POINT('Ctrl Pts',(-2.40966787183388,1.66054855162101,11.0752734561983));
#47547=CARTESIAN_POINT('Ctrl Pts',(-2.35471797004357,1.74368521769819,11.0716502887964));
#47548=CARTESIAN_POINT('Ctrl Pts',(-2.29573496237524,1.82392072310517,11.0679212456613));
#47549=CARTESIAN_POINT('Ctrl Pts',(-2.24798135631813,1.888880698333,11.0649021514529));
#47550=CARTESIAN_POINT('Ctrl Pts',(-2.19758411414171,1.95193923017891,11.0618143815443));
#47551=CARTESIAN_POINT('Ctrl Pts',(-2.14465592532941,2.01290113297903,11.058687366294));
#47552=CARTESIAN_POINT('',(-2.,-2.4492935982947E-16,12.));
#47553=CARTESIAN_POINT('',(-2.5,3.06161699786838E-16,11.5));
#47554=CARTESIAN_POINT('Origin',(0.,0.,12.));
#47555=CARTESIAN_POINT('Ctrl Pts',(1.70910432722271,-2.39912472810947,-0.331414121240076));
#47556=CARTESIAN_POINT('Ctrl Pts',(2.49908112321251,-1.83639873781273,-0.279009803491007));
#47557=CARTESIAN_POINT('Ctrl Pts',(3.46688794428796,0.119722171111187,-0.174225981237435));
#47558=CARTESIAN_POINT('Ctrl Pts',(1.80646906852251,2.96481187827153,-0.0170626544793579));
#47559=CARTESIAN_POINT('Ctrl Pts',(-1.47762516829172,3.13820676414614,0.140075859034155));
#47560=CARTESIAN_POINT('Ctrl Pts',(-3.43381835120548,0.497172601989588,
0.297214372547669));
#47561=CARTESIAN_POINT('Ctrl Pts',(-2.30628780313538,-2.59256922604425,
0.454352886061182));
#47562=CARTESIAN_POINT('Ctrl Pts',(0.89286661821801,-3.35263685283103,0.611491399574695));
#47563=CARTESIAN_POINT('Ctrl Pts',(3.2899750863192,-1.10208983694566,0.768629913088208));
#47564=CARTESIAN_POINT('Ctrl Pts',(2.73221466175904,2.13861997197995,0.925768426601723));
#47565=CARTESIAN_POINT('Ctrl Pts',(-0.279542673141038,3.45834407847404,
1.08290694011524));
#47566=CARTESIAN_POINT('Ctrl Pts',(-3.04021030694678,1.67200480266538,1.24004545362875));
#47567=CARTESIAN_POINT('Ctrl Pts',(-3.07028929888958,-1.61610736971899,
1.39718396714226));
#47568=CARTESIAN_POINT('Ctrl Pts',(-0.34275152402455,-3.45267261769994,
1.55432248065578));
#47569=CARTESIAN_POINT('Ctrl Pts',(2.6926299045483,-2.18819586596506,1.71146099416929));
#47570=CARTESIAN_POINT('Ctrl Pts',(3.30959871793033,1.04163827573356,1.8685995076828));
#47571=CARTESIAN_POINT('Ctrl Pts',(0.954016139202541,3.33591076751599,2.02573802119631));
#47572=CARTESIAN_POINT('Ctrl Pts',(-2.2584257185156,2.63400176430825,2.18287653470983));
#47573=CARTESIAN_POINT('Ctrl Pts',(-3.44243900729852,-0.433664443236683,
2.34001504822334));
#47574=CARTESIAN_POINT('Ctrl Pts',(-1.53458952609955,-3.11182991073641,
2.49715356173686));
#47575=CARTESIAN_POINT('Ctrl Pts',(1.75156758027233,-2.99507296916488,2.65429207525037));
#47576=CARTESIAN_POINT('Ctrl Pts',(3.46453592574662,-0.1882597119523,2.81143058876388));
#47577=CARTESIAN_POINT('Ctrl Pts',(2.06579499679089,2.78764091132087,2.96856910227739));
#47578=CARTESIAN_POINT('Ctrl Pts',(-1.18836135867558,3.25979266149099,3.12570761579091));
#47579=CARTESIAN_POINT('Ctrl Pts',(-3.3751785051291,0.804127440320037,3.28284612930442));
#47580=CARTESIAN_POINT('Ctrl Pts',(-2.5305436919165,-2.37377326169313,3.43998464281794));
#47581=CARTESIAN_POINT('Ctrl Pts',(0.586925466079213,-3.41964462846938,
3.59712315633145));
#47582=CARTESIAN_POINT('Ctrl Pts',(3.17724136420127,-1.39412631986779,3.75426166984497));
#47583=CARTESIAN_POINT('Ctrl Pts',(2.91388462237087,1.8835411567826,3.91140018335848));
#47584=CARTESIAN_POINT('Ctrl Pts',(0.0333918595374598,3.46948639819222,
4.06853869687199));
#47585=CARTESIAN_POINT('Ctrl Pts',(-2.87709215207102,1.93927605850991,4.22567721038551));
#47586=CARTESIAN_POINT('Ctrl Pts',(-3.20348568541843,-1.3327154032213,4.38281572389901));
#47587=CARTESIAN_POINT('Ctrl Pts',(-0.652634966855167,-3.4077145542025,
4.53995423741253));
#47588=CARTESIAN_POINT('Ctrl Pts',(2.48438668906291,-2.42203915367867,4.69709275092605));
#47589=CARTESIAN_POINT('Ctrl Pts',(3.39003039525862,0.739016104011381,4.85423126443955));
#47590=CARTESIAN_POINT('Ctrl Pts',(1.25088276275288,3.23631630046266,5.01136977795308));
#47591=CARTESIAN_POINT('Ctrl Pts',(-2.01175833668358,2.82688508389631,5.16850829146658));
#47592=CARTESIAN_POINT('Ctrl Pts',(-3.46751759586556,-0.121542606266135,
5.3256468049801));
#47593=CARTESIAN_POINT('Ctrl Pts',(-1.8088895747861,-2.96080553042772,5.48278531849362));
#47594=CARTESIAN_POINT('Ctrl Pts',(1.47441158128589,-3.14078992798711,5.63992383200712));
#47595=CARTESIAN_POINT('Ctrl Pts',(3.43345451870903,-0.499840925423201,
5.79706234552064));
#47596=CARTESIAN_POINT('Ctrl Pts',(2.3087042857198,2.59004544436804,5.95420085903415));
#47597=CARTESIAN_POINT('Ctrl Pts',(-0.889632904673123,3.35365534569197,
6.11133937254767));
#47598=CARTESIAN_POINT('Ctrl Pts',(-3.2889369753028,1.10514454042514,6.26847788606118));
#47599=CARTESIAN_POINT('Ctrl Pts',(-2.73424782219197,-2.13596341956599,
6.4256163995747));
#47600=CARTESIAN_POINT('Ctrl Pts',(0.276234676805524,-3.45863344198172,
6.5827549130882));
#47601=CARTESIAN_POINT('Ctrl Pts',(3.03861410485482,-1.67489558014692,6.73989342660173));
#47602=CARTESIAN_POINT('Ctrl Pts',(3.07183041964025,1.61316730579844,6.89703194011523));
#47603=CARTESIAN_POINT('Ctrl Pts',(0.346050039349144,3.45234706425207,7.05417045362875));
#47604=CARTESIAN_POINT('Ctrl Pts',(-2.69053881099474,2.19076511490178,7.21130896714225));
#47605=CARTESIAN_POINT('Ctrl Pts',(-3.31059202324357,-1.0384754900275,7.36844748065578));
#47606=CARTESIAN_POINT('Ctrl Pts',(-0.957202301260398,-3.33499844514049,
7.52558599416929));
#47607=CARTESIAN_POINT('Ctrl Pts',(2.25590869828579,-2.63615758761869,7.68272450768281));
#47608=CARTESIAN_POINT('Ctrl Pts',(3.4428516585937,0.430375849255442,7.83986302119631));
#47609=CARTESIAN_POINT('Ctrl Pts',(1.53756129382305,3.11036269379847,7.99700153470983));
#47610=CARTESIAN_POINT('Ctrl Pts',(-1.74870583733373,2.99674469957124,8.15414004822333));
#47611=CARTESIAN_POINT('Ctrl Pts',(-3.46435454290838,0.191568995177432,
8.31127856173687));
#47612=CARTESIAN_POINT('Ctrl Pts',(-2.06845679284888,-2.78566633017768,
8.46841707525036));
#47613=CARTESIAN_POINT('Ctrl Pts',(1.18524691039277,-3.2609263913346,8.62555558876389));
#47614=CARTESIAN_POINT('Ctrl Pts',(3.37440905771097,-0.807350934643548,
8.7826941022774));
#47615=CARTESIAN_POINT('Ctrl Pts',(2.5328096038664,2.37135466627205,8.93983261579091));
#47616=CARTESIAN_POINT('Ctrl Pts',(-0.583657951598417,3.42020428728099,
9.09697112930442));
#47617=CARTESIAN_POINT('Ctrl Pts',(-3.17590966926535,1.39715951965449,9.25410964281793));
#47618=CARTESIAN_POINT('Ctrl Pts',(-2.91567971810012,-1.88075479361231,
9.41124815633145));
#47619=CARTESIAN_POINT('Ctrl Pts',(-0.0367112214115904,-3.46945697416158,
9.56838666984496));
#47620=CARTESIAN_POINT('Ctrl Pts',(2.87524850237772,-1.94201565909655,9.72552518335847));
#47621=CARTESIAN_POINT('Ctrl Pts',(3.20473796907475,1.32963995908438,9.88266369687199));
#47622=CARTESIAN_POINT('Ctrl Pts',(0.655926631036102,3.4071179312111,10.0398022103855));
#47623=CARTESIAN_POINT('Ctrl Pts',(-2.48214247180021,2.42435699247973,10.196940723899));
#47624=CARTESIAN_POINT('Ctrl Pts',(-3.39060001386736,-0.735673984079567,
10.3540792374125));
#47625=CARTESIAN_POINT('Ctrl Pts',(-1.25423123682802,-3.2353180102252,10.511217750926));
#47626=CARTESIAN_POINT('Ctrl Pts',(2.00955017432607,-2.82842662307344,10.6683562644396));
#47627=CARTESIAN_POINT('Ctrl Pts',(3.46668582007914,0.117504286576653,10.8254947779531));
#47628=CARTESIAN_POINT('Ctrl Pts',(1.81355903899321,2.96048029568761,10.9826332914666));
#47629=CARTESIAN_POINT('Ctrl Pts',(-1.47574573937,3.13939893589932,11.139796701647));
#47630=CARTESIAN_POINT('Ctrl Pts',(-2.77455595124166,1.38549983595441,11.2445806073229));
#47631=CARTESIAN_POINT('Ctrl Pts',(-2.914713972712,0.425769325633511,11.2969850084943));
#47632=CARTESIAN_POINT('Ctrl Pts',(1.5973239975809,-2.24221508328063,-0.22018540887939));
#47633=CARTESIAN_POINT('Ctrl Pts',(2.33563404318066,-1.71629298827072,-0.167781091130323));
#47634=CARTESIAN_POINT('Ctrl Pts',(3.24014351969597,0.111891997411981,-0.0629972688767504));
#47635=CARTESIAN_POINT('Ctrl Pts',(1.68832080527672,2.77090466979952,0.0941660578813266));
#47636=CARTESIAN_POINT('Ctrl Pts',(-1.38098424019397,2.9329590323412,0.25130457139484));
#47637=CARTESIAN_POINT('Ctrl Pts',(-3.20923677294008,0.464656086494237,
0.408443084908354));
#47638=CARTESIAN_POINT('Ctrl Pts',(-2.15544995972395,-2.42300775569364,
0.565581598421868));
#47639=CARTESIAN_POINT('Ctrl Pts',(0.834470578069453,-3.13336477762204,
0.72272011193538));
#47640=CARTESIAN_POINT('Ctrl Pts',(3.07480127053478,-1.03000999763654,0.879858625448894));
#47641=CARTESIAN_POINT('Ctrl Pts',(2.55351997900672,1.99874808608113,1.03699713896241));
#47642=CARTESIAN_POINT('Ctrl Pts',(-0.261259779782845,3.23215844723473,
1.19413565247591));
#47643=CARTESIAN_POINT('Ctrl Pts',(-2.84137182477921,1.56265088843805,1.35127416598943));
#47644=CARTESIAN_POINT('Ctrl Pts',(-2.86948356429563,-1.51040930808146,
1.50841267950295));
#47645=CARTESIAN_POINT('Ctrl Pts',(-0.320334590353228,-3.22685791627738,
1.66555119301647));
#47646=CARTESIAN_POINT('Ctrl Pts',(2.51652417856085,-2.0450815742729,1.82268970652997));
#47647=CARTESIAN_POINT('Ctrl Pts',(3.09314146030137,0.973512142077214,1.97982822004348));
#47648=CARTESIAN_POINT('Ctrl Pts',(0.891620744828347,3.11773262630528,2.136966733557));
#47649=CARTESIAN_POINT('Ctrl Pts',(-2.11071819284485,2.46173048700712,2.29410524707052));
#47650=CARTESIAN_POINT('Ctrl Pts',(-3.21729361337571,-0.405301543648401,
2.45124376058402));
#47651=CARTESIAN_POINT('Ctrl Pts',(-1.43422296546303,-2.90830730086939,
2.60838227409754));
#47652=CARTESIAN_POINT('Ctrl Pts',(1.63701003197397,-2.79918659847233,2.76552078761105));
#47653=CARTESIAN_POINT('Ctrl Pts',(3.23794532991962,-0.17594698631868,2.92265930112457));
#47654=CARTESIAN_POINT('Ctrl Pts',(1.9306860733415,2.60532119272485,3.07979781463808));
#47655=CARTESIAN_POINT('Ctrl Pts',(-1.11063911416977,3.0465928629406,3.23693632815159));
#47656=CARTESIAN_POINT('Ctrl Pts',(-3.15443214114532,0.75153519716593,3.39407484166512));
#47657=CARTESIAN_POINT('Ctrl Pts',(-2.36503886956599,-2.21852167554908,
3.55121335517862));
#47658=CARTESIAN_POINT('Ctrl Pts',(0.548538855602305,-3.19599005236204,
3.70835186869213));
#47659=CARTESIAN_POINT('Ctrl Pts',(2.9694406574889,-1.30294645617249,3.86549038220565));
#47660=CARTESIAN_POINT('Ctrl Pts',(2.72330820264104,1.76035215769955,4.02262889571916));
#47661=CARTESIAN_POINT('Ctrl Pts',(0.0312079360595172,3.24257202725503,
4.17976740923268));
#47662=CARTESIAN_POINT('Ctrl Pts',(-2.68892206552574,1.81244183684538,4.33690592274618));
#47663=CARTESIAN_POINT('Ctrl Pts',(-2.99396852475403,-1.24555198977838,
4.4940444362597));
#47664=CARTESIAN_POINT('Ctrl Pts',(-0.609950766383085,-3.18484023920209,
4.65118294977321));
#47665=CARTESIAN_POINT('Ctrl Pts',(2.32190066721047,-2.26363083963293,4.80832146328674));
#47666=CARTESIAN_POINT('Ctrl Pts',(3.16831267502232,0.690682329179025,4.96545997680025));
#47667=CARTESIAN_POINT('Ctrl Pts',(1.16907143892864,3.02465192332146,5.12259849031377));
#47668=CARTESIAN_POINT('Ctrl Pts',(-1.88018356593827,2.64199868374835,5.27973700382728));
#47669=CARTESIAN_POINT('Ctrl Pts',(-3.24073199025274,-0.113593370881535,
5.43687551734079));
#47670=CARTESIAN_POINT('Ctrl Pts',(-1.69058300348168,-2.76716034860646,
5.59401403085429));
#47671=CARTESIAN_POINT('Ctrl Pts',(1.37798083100417,-2.93537324985099,5.75115254436782));
#47672=CARTESIAN_POINT('Ctrl Pts',(3.20889673613342,-0.467149893914844,
5.90829105788132));
#47673=CARTESIAN_POINT('Ctrl Pts',(2.1577083974099,2.42064903658454,6.06542957139485));
#47674=CARTESIAN_POINT('Ctrl Pts',(-0.831448358674023,3.13431665812589,
6.22256808490835));
#47675=CARTESIAN_POINT('Ctrl Pts',(-3.07383105495917,1.03286491473878,6.37970659842187));
#47676=CARTESIAN_POINT('Ctrl Pts',(-2.55542016491037,-1.99626527982169,
6.53684511193538));
#47677=CARTESIAN_POINT('Ctrl Pts',(0.258168135904549,-3.23242888553827,
6.6939836254489));
#47678=CARTESIAN_POINT('Ctrl Pts',(2.83988001888659,-1.56535260077321,6.85112213896242));
#47679=CARTESIAN_POINT('Ctrl Pts',(2.87092389132481,1.5076615327819,7.00826065247592));
#47680=CARTESIAN_POINT('Ctrl Pts',(0.323417373305934,3.22655365495962,7.16539916598943));
#47681=CARTESIAN_POINT('Ctrl Pts',(-2.51456984852899,2.04748278695315,7.32253767950295));
#47682=CARTESIAN_POINT('Ctrl Pts',(-3.09406980059545,-0.970556211636323,
7.47967619301647));
#47683=CARTESIAN_POINT('Ctrl Pts',(-0.894598522740514,-3.11687997243229,
7.63681470652998));
#47684=CARTESIAN_POINT('Ctrl Pts',(2.10836579296415,-2.46374531328394,7.7939532200435));
#47685=CARTESIAN_POINT('Ctrl Pts',(3.21767927609153,0.402228033154709,7.951091733557));
#47686=CARTESIAN_POINT('Ctrl Pts',(1.43700037104582,2.90693604413139,8.10823024707053));
#47687=CARTESIAN_POINT('Ctrl Pts',(-1.63433545523929,2.80074899291077,8.26536876058403));
#47688=CARTESIAN_POINT('Ctrl Pts',(-3.23777581003972,0.179039832920316,
8.42250727409755));
#47689=CARTESIAN_POINT('Ctrl Pts',(-1.93317378029559,-2.60347575485722,
8.57964578761106));
#47690=CARTESIAN_POINT('Ctrl Pts',(1.10772835974587,-3.04765244359763,8.73678430112457));
#47691=CARTESIAN_POINT('Ctrl Pts',(3.15371301779734,-0.754547865706401,
8.89392281463809));
#47692=CARTESIAN_POINT('Ctrl Pts',(2.36715658436919,2.21626126321204,9.05106132815159));
#47693=CARTESIAN_POINT('Ctrl Pts',(-0.545485045949209,3.19651310788066,
9.20819984166512));
#47694=CARTESIAN_POINT('Ctrl Pts',(-2.96819605922493,1.3057812759852,9.36533835517862));
#47695=CARTESIAN_POINT('Ctrl Pts',(-2.72498589395606,-1.75774803067992,
9.52247686869215));
#47696=CARTESIAN_POINT('Ctrl Pts',(-0.0343102021375739,-3.24254452764047,
9.67961538220565));
#47697=CARTESIAN_POINT('Ctrl Pts',(2.6871989958153,-1.81500225968858,9.83675389571918));
#47698=CARTESIAN_POINT('Ctrl Pts',(2.99513890546405,1.24267768851727,9.99389240923267));
#47699=CARTESIAN_POINT('Ctrl Pts',(0.613027146276597,3.18428263706717,10.1510309227462));
#47700=CARTESIAN_POINT('Ctrl Pts',(-2.31980322819965,2.26579708512215,10.3081694362597));
#47701=CARTESIAN_POINT('Ctrl Pts',(-3.16884503893873,-0.687558793485591,
10.4653079497732));
#47702=CARTESIAN_POINT('Ctrl Pts',(-1.17220091318618,-3.0237189241315,10.6224464632867));
#47703=CARTESIAN_POINT('Ctrl Pts',(1.87811982373831,-2.64343940183772,10.7795849768002));
#47704=CARTESIAN_POINT('Ctrl Pts',(3.23995461499069,0.109819168893298,10.9367234903137));
#47705=CARTESIAN_POINT('Ctrl Pts',(1.69494707132415,2.76685638515205,11.0938620038273));
#47706=CARTESIAN_POINT('Ctrl Pts',(-1.37922773131934,2.93407323263913,11.2510254140077));
#47707=CARTESIAN_POINT('Ctrl Pts',(-2.59309202660024,1.2948841690727,11.3558093196836));
#47708=CARTESIAN_POINT('Ctrl Pts',(-2.7240833110889,0.397922789402426,11.408213720855));
#47709=CARTESIAN_POINT('Ctrl Pts',(1.48554366793907,-2.08530543845179,-0.108956696518706));
#47710=CARTESIAN_POINT('Ctrl Pts',(2.17218696314881,-1.59618723872872,-0.0565523787696377));
#47711=CARTESIAN_POINT('Ctrl Pts',(3.01339909510398,0.104061823712772,0.0482314434839342));
#47712=CARTESIAN_POINT('Ctrl Pts',(1.57017254203093,2.57699746132752,0.205394770242011));
#47713=CARTESIAN_POINT('Ctrl Pts',(-1.28434331209622,2.72771130053625,0.362533283755524));
#47714=CARTESIAN_POINT('Ctrl Pts',(-2.98465519467468,0.43213957099889,0.519671797269038));
#47715=CARTESIAN_POINT('Ctrl Pts',(-2.00461211631251,-2.25344628534304,
0.676810310782551));
#47716=CARTESIAN_POINT('Ctrl Pts',(0.776074537920896,-2.91409270241304,
0.833948824296065));
#47717=CARTESIAN_POINT('Ctrl Pts',(2.85962745475038,-0.957930158327435,
0.991087337809578));
#47718=CARTESIAN_POINT('Ctrl Pts',(2.37482529625441,1.85887620018229,1.14822585132309));
#47719=CARTESIAN_POINT('Ctrl Pts',(-0.242976886424651,3.00597281599543,
1.30536436483661));
#47720=CARTESIAN_POINT('Ctrl Pts',(-2.64253334261165,1.45329697421072,1.46250287835012));
#47721=CARTESIAN_POINT('Ctrl Pts',(-2.66867782970167,-1.40471124644393,
1.61964139186363));
#47722=CARTESIAN_POINT('Ctrl Pts',(-0.297917656681901,-3.00104321485481,
1.77677990537715));
#47723=CARTESIAN_POINT('Ctrl Pts',(2.34041845257341,-1.90196728258075,1.93391841889066));
#47724=CARTESIAN_POINT('Ctrl Pts',(2.87668420267241,0.905386008420865,2.09105693240418));
#47725=CARTESIAN_POINT('Ctrl Pts',(0.829225350454149,2.89955448509455,2.24819544591769));
#47726=CARTESIAN_POINT('Ctrl Pts',(-1.9630106671741,2.28945920970598,2.4053339594312));
#47727=CARTESIAN_POINT('Ctrl Pts',(-2.99214821945292,-0.376938644060123,
2.56247247294471));
#47728=CARTESIAN_POINT('Ctrl Pts',(-1.33385640482652,-2.70478469100235,
2.71961098645823));
#47729=CARTESIAN_POINT('Ctrl Pts',(1.52245248367561,-2.60330022777978,2.87674949997174));
#47730=CARTESIAN_POINT('Ctrl Pts',(3.0113547340926,-0.163634260685059,3.03388801348526));
#47731=CARTESIAN_POINT('Ctrl Pts',(1.79557714989212,2.42300147412883,3.19102652699877));
#47732=CARTESIAN_POINT('Ctrl Pts',(-1.03291686966396,2.83339306439021,3.34816504051229));
#47733=CARTESIAN_POINT('Ctrl Pts',(-2.93368577716156,0.698942954011819,
3.50530355402579));
#47734=CARTESIAN_POINT('Ctrl Pts',(-2.19953404721547,-2.06327008940503,
3.66244206753931));
#47735=CARTESIAN_POINT('Ctrl Pts',(0.510152245125398,-2.9723354762547,3.81958058105282));
#47736=CARTESIAN_POINT('Ctrl Pts',(2.76163995077652,-1.21176659247721,3.97671909456634));
#47737=CARTESIAN_POINT('Ctrl Pts',(2.53273178291119,1.63716315861649,4.13385760807985));
#47738=CARTESIAN_POINT('Ctrl Pts',(0.0290240125815749,3.01565765631784,
4.29099612159337));
#47739=CARTESIAN_POINT('Ctrl Pts',(-2.50075197898047,1.68560761518086,4.44813463510687));
#47740=CARTESIAN_POINT('Ctrl Pts',(-2.78445136408961,-1.15838857633547,
4.60527314862039));
#47741=CARTESIAN_POINT('Ctrl Pts',(-0.567266565911004,-2.96196592420167,
4.76241166213391));
#47742=CARTESIAN_POINT('Ctrl Pts',(2.15941464535803,-2.10522252558719,4.91955017564741));
#47743=CARTESIAN_POINT('Ctrl Pts',(2.94659495478601,0.642348554346671,5.07668868916094));
#47744=CARTESIAN_POINT('Ctrl Pts',(1.08726011510442,2.81298754618025,5.23382720267444));
#47745=CARTESIAN_POINT('Ctrl Pts',(-1.74860879519294,2.45711228360039,5.39096571618796));
#47746=CARTESIAN_POINT('Ctrl Pts',(-3.01394638463993,-0.105644135496936,
5.54810422970147));
#47747=CARTESIAN_POINT('Ctrl Pts',(-1.57227643217725,-2.5735151667852,5.70524274321499));
#47748=CARTESIAN_POINT('Ctrl Pts',(1.28155008072244,-2.72995657171488,5.8623812567285));
#47749=CARTESIAN_POINT('Ctrl Pts',(2.98433895355781,-0.434458862406489,
6.01951977024201));
#47750=CARTESIAN_POINT('Ctrl Pts',(2.00671250910002,2.25125262880104,6.17665828375553));
#47751=CARTESIAN_POINT('Ctrl Pts',(-0.773263812674921,2.91497797055982,
6.33379679726904));
#47752=CARTESIAN_POINT('Ctrl Pts',(-2.85872513461553,0.960585289052411,
6.49093531078255));
#47753=CARTESIAN_POINT('Ctrl Pts',(-2.37659250762878,-1.85656714007738,
6.64807382429607));
#47754=CARTESIAN_POINT('Ctrl Pts',(0.240101595003575,-3.00622432909485,
6.80521233780957));
#47755=CARTESIAN_POINT('Ctrl Pts',(2.64114593291835,-1.45580962139949,6.9623508513231));
#47756=CARTESIAN_POINT('Ctrl Pts',(2.67001736300939,1.40215575976535,7.11948936483661));
#47757=CARTESIAN_POINT('Ctrl Pts',(0.300784707262725,3.00076024566717,7.27662787835012));
#47758=CARTESIAN_POINT('Ctrl Pts',(-2.33860088606324,1.90420045900452,7.43376639186363));
#47759=CARTESIAN_POINT('Ctrl Pts',(-2.87754757794732,-0.902636933245142,
7.59090490537715));
#47760=CARTESIAN_POINT('Ctrl Pts',(-0.831994744220631,-2.89876149972411,
7.74804341889066));
#47761=CARTESIAN_POINT('Ctrl Pts',(1.96082288764251,-2.29133303894919,7.90518193240418));
#47762=CARTESIAN_POINT('Ctrl Pts',(2.99250689358935,0.374080217053975,8.06232044591769));
#47763=CARTESIAN_POINT('Ctrl Pts',(1.33643944826859,2.70350939446431,8.2194589594312));
#47764=CARTESIAN_POINT('Ctrl Pts',(-1.51996507314484,2.6047532862503,8.37659747294471));
#47765=CARTESIAN_POINT('Ctrl Pts',(-3.01119707717106,0.166510670663201,
8.53373598645823));
#47766=CARTESIAN_POINT('Ctrl Pts',(-1.79789076774231,-2.42128517953676,
8.69087449997174));
#47767=CARTESIAN_POINT('Ctrl Pts',(1.03020980909898,-2.83437849586067,8.84801301348525));
#47768=CARTESIAN_POINT('Ctrl Pts',(2.93301697788372,-0.701744796769256,
9.00515152699877));
#47769=CARTESIAN_POINT('Ctrl Pts',(2.20150356487198,2.06116786015204,9.16229004051228));
#47770=CARTESIAN_POINT('Ctrl Pts',(-0.507312140300006,2.97282192848032,
9.3194285540258));
#47771=CARTESIAN_POINT('Ctrl Pts',(-2.7604824491845,1.21440303231589,9.47656706753931));
#47772=CARTESIAN_POINT('Ctrl Pts',(-2.53429206981202,-1.63474126774752,
9.63370558105282));
#47773=CARTESIAN_POINT('Ctrl Pts',(-0.0319091828635594,-3.01563208111935,
9.79084409456634));
#47774=CARTESIAN_POINT('Ctrl Pts',(2.49914948925288,-1.68798886028062,9.94798260807984));
#47775=CARTESIAN_POINT('Ctrl Pts',(2.78553984185336,1.15571541795015,10.1051211215933));
#47776=CARTESIAN_POINT('Ctrl Pts',(0.570127661517096,2.96144734292322,10.2622596351068));
#47777=CARTESIAN_POINT('Ctrl Pts',(-2.15746398459908,2.10723717776457,10.4193981486204));
#47778=CARTESIAN_POINT('Ctrl Pts',(-2.9470900640101,-0.639443602891618,
10.576536662134));
#47779=CARTESIAN_POINT('Ctrl Pts',(-1.09017058954435,-2.81211983803781,
10.7336751756475));
#47780=CARTESIAN_POINT('Ctrl Pts',(1.74668947315055,-2.45845218060199,10.890813689161));
#47781=CARTESIAN_POINT('Ctrl Pts',(3.01322340990224,0.102134051209937,11.0479522026745));
#47782=CARTESIAN_POINT('Ctrl Pts',(1.57633510365508,2.57323247461651,11.2050907161879));
#47783=CARTESIAN_POINT('Ctrl Pts',(-1.2827097232687,2.72874752937894,11.3622541263684));
#47784=CARTESIAN_POINT('Ctrl Pts',(-2.41162810195881,1.20426850219099,11.4670380320443));
#47785=CARTESIAN_POINT('Ctrl Pts',(-2.53345264946579,0.37007625317134,11.5194424332157));
#47786=CARTESIAN_POINT('Ctrl Pts',(1.37376333829725,-1.92839579362295,0.00227201584197912));
#47787=CARTESIAN_POINT('Ctrl Pts',(2.00873988311696,-1.47608148918673,0.0546763335910469));
#47788=CARTESIAN_POINT('Ctrl Pts',(2.786654670512,0.0962316500135649,0.159460155844619));
#47789=CARTESIAN_POINT('Ctrl Pts',(1.45202427878513,2.3830902528555,0.316623482602697));
#47790=CARTESIAN_POINT('Ctrl Pts',(-1.18770238399847,2.52246356873131,0.47376199611621));
#47791=CARTESIAN_POINT('Ctrl Pts',(-2.76007361640928,0.399623055503541,
0.630900509629723));
#47792=CARTESIAN_POINT('Ctrl Pts',(-1.85377427290108,-2.08388481499243,
0.788039023143237));
#47793=CARTESIAN_POINT('Ctrl Pts',(0.717678497772337,-2.69482062720405,
0.94517753665675));
#47794=CARTESIAN_POINT('Ctrl Pts',(2.64445363896598,-0.885850319018325,
1.10231605017026));
#47795=CARTESIAN_POINT('Ctrl Pts',(2.19613061350208,1.71900431428346,1.25945456368378));
#47796=CARTESIAN_POINT('Ctrl Pts',(-0.224693993066457,2.77978718475613,
1.41659307719729));
#47797=CARTESIAN_POINT('Ctrl Pts',(-2.44369486044408,1.34394305998338,1.57373159071081));
#47798=CARTESIAN_POINT('Ctrl Pts',(-2.46787209510772,-1.2990131848064,1.73087010422431));
#47799=CARTESIAN_POINT('Ctrl Pts',(-0.275500723010577,-2.77522851343225,
1.88800861773783));
#47800=CARTESIAN_POINT('Ctrl Pts',(2.16431272658597,-1.75885299088859,2.04514713125134));
#47801=CARTESIAN_POINT('Ctrl Pts',(2.66022694504343,0.837259874764513,2.20228564476486));
#47802=CARTESIAN_POINT('Ctrl Pts',(0.766829956079953,2.68137634388383,2.35942415827837));
#47803=CARTESIAN_POINT('Ctrl Pts',(-1.81530314150335,2.11718793240485,2.51656267179188));
#47804=CARTESIAN_POINT('Ctrl Pts',(-2.76700282553012,-0.348575744471842,
2.67370118530539));
#47805=CARTESIAN_POINT('Ctrl Pts',(-1.23348984419001,-2.50126208113532,
2.83083969881891));
#47806=CARTESIAN_POINT('Ctrl Pts',(1.40789493537724,-2.40741385708723,2.98797821233242));
#47807=CARTESIAN_POINT('Ctrl Pts',(2.7847641382656,-0.151321535051437,3.14511672584594));
#47808=CARTESIAN_POINT('Ctrl Pts',(1.66046822644274,2.24068175553282,3.30225523935945));
#47809=CARTESIAN_POINT('Ctrl Pts',(-0.955194625158153,2.62019326583982,
3.45939375287296));
#47810=CARTESIAN_POINT('Ctrl Pts',(-2.71293941317779,0.64635071085771,3.61653226638648));
#47811=CARTESIAN_POINT('Ctrl Pts',(-2.03402922486496,-1.90801850326096,
3.77367077989999));
#47812=CARTESIAN_POINT('Ctrl Pts',(0.471765634648494,-2.74868090014737,
3.9308092934135));
#47813=CARTESIAN_POINT('Ctrl Pts',(2.55383924406414,-1.12058672878193,4.08794780692702));
#47814=CARTESIAN_POINT('Ctrl Pts',(2.34215536318135,1.51397415953343,4.24508632044053));
#47815=CARTESIAN_POINT('Ctrl Pts',(0.0268400891036326,2.78874328538067,
4.40222483395405));
#47816=CARTESIAN_POINT('Ctrl Pts',(-2.3125818924352,1.55877339351634,4.55936334746756));
#47817=CARTESIAN_POINT('Ctrl Pts',(-2.57493420342521,-1.07122516289255,
4.71650186098107));
#47818=CARTESIAN_POINT('Ctrl Pts',(-0.524582365438923,-2.73909160920127,
4.87364037449459));
#47819=CARTESIAN_POINT('Ctrl Pts',(1.9969286235056,-1.94681421154145,5.0307788880081));
#47820=CARTESIAN_POINT('Ctrl Pts',(2.72487723454969,0.594014779514313,5.18791740152161));
#47821=CARTESIAN_POINT('Ctrl Pts',(1.00544879128018,2.60132316903906,5.34505591503514));
#47822=CARTESIAN_POINT('Ctrl Pts',(-1.61703402444763,2.27222588345243,5.50219442854863));
#47823=CARTESIAN_POINT('Ctrl Pts',(-2.7871607790271,-0.0976949001123346,
5.65933294206217));
#47824=CARTESIAN_POINT('Ctrl Pts',(-1.45396986087282,-2.37986998496394,
5.81647145557566));
#47825=CARTESIAN_POINT('Ctrl Pts',(1.18511933044069,-2.52453989357877,5.97360996908919));
#47826=CARTESIAN_POINT('Ctrl Pts',(2.7597811709822,-0.401767830898135,6.13074848260269));
#47827=CARTESIAN_POINT('Ctrl Pts',(1.85571662079012,2.08185622101755,6.28788699611621));
#47828=CARTESIAN_POINT('Ctrl Pts',(-0.715079266675815,2.69563928299374,
6.44502550962972));
#47829=CARTESIAN_POINT('Ctrl Pts',(-2.64361921427189,0.888305663366045,
6.60216402314323));
#47830=CARTESIAN_POINT('Ctrl Pts',(-2.19776485034718,-1.71686900033308,
6.75930253665675));
#47831=CARTESIAN_POINT('Ctrl Pts',(0.222035054102601,-2.78001977265141,
6.91644105017026));
#47832=CARTESIAN_POINT('Ctrl Pts',(2.44241184695011,-1.34626664202579,7.07357956368377));
#47833=CARTESIAN_POINT('Ctrl Pts',(2.46911083469396,1.29664998674881,7.23071807719729));
#47834=CARTESIAN_POINT('Ctrl Pts',(0.278152041219513,2.77496683637473,7.3878565907108));
#47835=CARTESIAN_POINT('Ctrl Pts',(-2.16263192359748,1.76091813105588,7.54499510422432));
#47836=CARTESIAN_POINT('Ctrl Pts',(-2.66102535529921,-0.83471765485396,
7.70213361773782));
#47837=CARTESIAN_POINT('Ctrl Pts',(-0.769390965700746,-2.68064302701591,
7.85927213125134));
#47838=CARTESIAN_POINT('Ctrl Pts',(1.81327998232086,-2.11892076461443,8.01641064476486));
#47839=CARTESIAN_POINT('Ctrl Pts',(2.76733451108718,0.345932400953242,8.17354915827837));
#47840=CARTESIAN_POINT('Ctrl Pts',(1.23587852549135,2.50008274479723,8.33068767179189));
#47841=CARTESIAN_POINT('Ctrl Pts',(-1.4055946910504,2.40875757958982,8.4878261853054));
#47842=CARTESIAN_POINT('Ctrl Pts',(-2.78461834430241,0.153981508406087,
8.64496469881891));
#47843=CARTESIAN_POINT('Ctrl Pts',(-1.66260775518902,-2.23909460421632,
8.80210321233243));
#47844=CARTESIAN_POINT('Ctrl Pts',(0.952691258452081,-2.6211045481237,8.95924172584593));
#47845=CARTESIAN_POINT('Ctrl Pts',(2.71232093797009,-0.648941727832109,
9.11638023935945));
#47846=CARTESIAN_POINT('Ctrl Pts',(2.03585054537477,1.90607445709202,9.27351875287297));
#47847=CARTESIAN_POINT('Ctrl Pts',(-0.469139234650799,2.74913074907999,
9.43065726638646));
#47848=CARTESIAN_POINT('Ctrl Pts',(-2.55276883914408,1.12302478864659,9.5877957799));
#47849=CARTESIAN_POINT('Ctrl Pts',(-2.34359824566799,-1.51173450481514,
9.74493429341351));
#47850=CARTESIAN_POINT('Ctrl Pts',(-0.0295081635895418,-2.78871963459825,
9.90207280692703));
#47851=CARTESIAN_POINT('Ctrl Pts',(2.31109998269045,-1.56097546087265,10.0592113204406));
#47852=CARTESIAN_POINT('Ctrl Pts',(2.57594077824267,1.06875314738303,10.2163498339541));
#47853=CARTESIAN_POINT('Ctrl Pts',(0.527228176757592,2.73861204877929,10.3734883474676));
#47854=CARTESIAN_POINT('Ctrl Pts',(-1.99512474099851,1.948677270407,10.5306268609811));
#47855=CARTESIAN_POINT('Ctrl Pts',(-2.72533508908147,-0.591328412297643,
10.6877653744946));
#47856=CARTESIAN_POINT('Ctrl Pts',(-1.00814026590252,-2.60052075194411,
10.8449038880081));
#47857=CARTESIAN_POINT('Ctrl Pts',(1.61525912256279,-2.27346495936627,11.0020424015217));
#47858=CARTESIAN_POINT('Ctrl Pts',(2.78649220481378,0.0944489335265817,
11.1591809150351));
#47859=CARTESIAN_POINT('Ctrl Pts',(1.45772313598602,2.37960856408097,11.3163194285487));
#47860=CARTESIAN_POINT('Ctrl Pts',(-1.18619171521805,2.52342182611875,11.4734828387291));
#47861=CARTESIAN_POINT('Ctrl Pts',(-2.23016417731738,1.11365283530928,11.578266744405));
#47862=CARTESIAN_POINT('Ctrl Pts',(-2.34282198784267,0.342229716940255,
11.6306711455764));
#47863=CARTESIAN_POINT('Ctrl Pts',(1.29197400994444,2.64783394680711,-8.8037216405823E-17));
#47864=CARTESIAN_POINT('Ctrl Pts',(1.37074936016223,2.60046826619745,1.38836964406048E-15));
#47865=CARTESIAN_POINT('Ctrl Pts',(1.44700091320012,2.54930204226795,5.54450672197035E-16));
#47866=CARTESIAN_POINT('Ctrl Pts',(1.5204041597113,2.49432533414619,7.28583859910259E-17));
#47867=CARTESIAN_POINT('Ctrl Pts',(1.59819384922954,2.43606331906114,-3.44654117973336E-16));
#47868=CARTESIAN_POINT('Ctrl Pts',(1.67278528785766,2.37352116391825,2.10927055586783E-15));
#47869=CARTESIAN_POINT('Ctrl Pts',(1.74400344302578,2.30706978985341,3.50414142147315E-15));
#47870=CARTESIAN_POINT('Ctrl Pts',(1.77507572754732,2.27807723876983,4.11271972997575E-15));
#47871=CARTESIAN_POINT('Ctrl Pts',(1.80550534467386,2.2483401837646,3.54603031729656E-15));
#47872=CARTESIAN_POINT('Ctrl Pts',(1.83527511247412,2.21788805045802,3.41393580072236E-15));
#47873=CARTESIAN_POINT('Ctrl Pts',(1.85158854668356,2.20120068908634,3.34154977406537E-15));
#47874=CARTESIAN_POINT('Ctrl Pts',(1.86770501691636,2.18429728937136,3.85069962828599E-15));
#47875=CARTESIAN_POINT('Ctrl Pts',(1.883618179848,2.16718615052119,3.69843045078255E-15));
#47876=CARTESIAN_POINT('Ctrl Pts',(1.89863325668145,2.15104070755384,3.55475484025806E-15));
#47877=CARTESIAN_POINT('Ctrl Pts',(1.91346219376733,2.1347157726636,4.15166473682132E-15));
#47878=CARTESIAN_POINT('Ctrl Pts',(1.92809660170213,2.11822316236597,4.33680868994202E-15));
#47879=CARTESIAN_POINT('Ctrl Pts',(1.99241597015465,2.04573684906905,5.15053085694606E-15));
#47880=CARTESIAN_POINT('Ctrl Pts',(2.05302114486396,1.96997093364048,5.27402816434403E-15));
#47881=CARTESIAN_POINT('Ctrl Pts',(2.1097435081236,1.89129938269064,3.91353616180368E-15));
#47882=CARTESIAN_POINT('Ctrl Pts',(2.16643862125782,1.81266562652767,2.55369775646138E-15));
#47883=CARTESIAN_POINT('Ctrl Pts',(2.21925498259858,1.73112805545147,4.69792942335234E-15));
#47884=CARTESIAN_POINT('Ctrl Pts',(2.26797565137533,1.64704303172464,4.76008121808036E-15));
#47885=CARTESIAN_POINT('Ctrl Pts',(2.27370375376251,1.63715713242915,4.76738842162842E-15));
#47886=CARTESIAN_POINT('Ctrl Pts',(2.27937518380796,1.62723601064538,5.31291259247108E-15));
#47887=CARTESIAN_POINT('Ctrl Pts',(2.28498954152194,1.61728023964544,5.759281940243E-15));
#47888=CARTESIAN_POINT('Ctrl Pts',(2.29543189661598,1.59876312668031,6.68580931231859E-15));
#47889=CARTESIAN_POINT('Ctrl Pts',(2.30567682494647,1.58012614919259,4.74072510815603E-15));
#47890=CARTESIAN_POINT('Ctrl Pts',(2.31572165746038,1.56137299470242,4.413136522885E-15));
#47891=CARTESIAN_POINT('Ctrl Pts',(2.32292320728395,1.54792809393149,4.17340296428537E-15));
#47892=CARTESIAN_POINT('Ctrl Pts',(2.33002152872364,1.53442403232929,7.07982753161834E-15));
#47893=CARTESIAN_POINT('Ctrl Pts',(2.33700969851763,1.52087413145422,6.73072708679001E-15));
#47894=CARTESIAN_POINT('Ctrl Pts',(2.38054570717361,1.43645880967822,4.52005977667776E-15));
#47895=CARTESIAN_POINT('Ctrl Pts',(2.41987517047016,1.35014619738548,5.21195039373243E-15));
#47896=CARTESIAN_POINT('Ctrl Pts',(2.45484083362543,1.26228524501801,4.74620343027254E-15));
#47897=CARTESIAN_POINT('Ctrl Pts',(2.489466389985,1.17527890555589,4.28498673145102E-15));
#47898=CARTESIAN_POINT('Ctrl Pts',(2.5198128252979,1.08675327428347,5.61314304544713E-15));
#47899=CARTESIAN_POINT('Ctrl Pts',(2.54567771304716,0.997038113744462,4.12170297892089E-15));
#47900=CARTESIAN_POINT('Ctrl Pts',(2.57079955722097,0.90990028020974,2.67310883426158E-15));
#47901=CARTESIAN_POINT('Ctrl Pts',(2.59169365537883,0.821639511860095,2.2335485000352E-15));
#47902=CARTESIAN_POINT('Ctrl Pts',(2.60812613872453,0.732561686781793,3.58046925441613E-15));
#47903=CARTESIAN_POINT('Ctrl Pts',(2.6179205585058,0.679467726869315,4.38328809822516E-15));
#47904=CARTESIAN_POINT('Ctrl Pts',(2.62612900003745,0.62608362232302,5.90836632262066E-15));
#47905=CARTESIAN_POINT('Ctrl Pts',(2.6326933508001,0.572476447093943,2.692290834716E-15));
#47906=CARTESIAN_POINT('Ctrl Pts',(2.6352683765624,0.551447732716798,1.47778125432564E-15));
#47907=CARTESIAN_POINT('Ctrl Pts',(2.63759088070415,0.530377846603741,4.89932062977248E-15));
#47908=CARTESIAN_POINT('Ctrl Pts',(2.63965388200594,0.509307581220653,4.55191440096314E-15));
#47909=CARTESIAN_POINT('Ctrl Pts',(2.64834931960692,0.420497565581757,3.58563629104739E-15));
#47910=CARTESIAN_POINT('Ctrl Pts',(2.65245297897981,0.331587017875098,1.12456554759877E-15));
#47911=CARTESIAN_POINT('Ctrl Pts',(2.65178792227643,0.242870082279381,1.77635683940025E-15));
#47912=CARTESIAN_POINT('Ctrl Pts',(2.65141677862464,0.193360428010837,1.70825926277529E-15));
#47913=CARTESIAN_POINT('Ctrl Pts',(2.64955959473766,0.143911103164861,4.17994550737481E-16));
#47914=CARTESIAN_POINT('Ctrl Pts',(2.64617859082989,0.0945743399740334,
4.16333634234434E-16));
#47915=CARTESIAN_POINT('Ctrl Pts',(2.63994540686809,0.00361759178976989,
4.69281982652766E-16));
#47916=CARTESIAN_POINT('Ctrl Pts',(2.62853563407678,-0.0869581494466769,
-2.6842679134847E-16));
#47917=CARTESIAN_POINT('Ctrl Pts',(2.61214758827663,-0.176810898454838,
-8.60422844084496E-16));
#47918=CARTESIAN_POINT('Ctrl Pts',(2.59575954247647,-0.266663647463,-1.45241889682052E-15));
#47919=CARTESIAN_POINT('Ctrl Pts',(2.5743925683296,-0.3557942617185,5.20804214904531E-17));
#47920=CARTESIAN_POINT('Ctrl Pts',(2.54820206281091,-0.443829678011399,
-1.72084568816899E-15));
#47921=CARTESIAN_POINT('Ctrl Pts',(2.5433159398537,-0.460253640057088,-1.94456528016881E-15));
#47922=CARTESIAN_POINT('Ctrl Pts',(2.53826078384047,-0.476642310793063,
1.09767773292823E-15));
#47923=CARTESIAN_POINT('Ctrl Pts',(2.53304532831964,-0.492969520416451,
7.49400541621981E-16));
#47924=CARTESIAN_POINT('Ctrl Pts',(2.50606165438058,-0.577443081556576,
-1.37861067859985E-15));
#47925=CARTESIAN_POINT('Ctrl Pts',(2.47475445780067,-0.660402252413519,
-4.29383913192097E-16));
#47926=CARTESIAN_POINT('Ctrl Pts',(2.43933995245441,-0.741546545884959,
-7.7715611723761E-16));
#47927=CARTESIAN_POINT('Ctrl Pts',(2.40390362452278,-0.822740840853054,
-1.12514262015681E-15));
#47928=CARTESIAN_POINT('Ctrl Pts',(2.36435426939278,-0.902118814440422,
1.6833566618084E-16));
#47929=CARTESIAN_POINT('Ctrl Pts',(2.32086575374546,-0.979349725934495,
-1.47104550762833E-15));
#47930=CARTESIAN_POINT('Ctrl Pts',(2.27822747361116,-1.05507071089561,-3.07837545888844E-15));
#47931=CARTESIAN_POINT('Ctrl Pts',(2.23180185773245,-1.12872835588638,-1.56235785302982E-15));
#47932=CARTESIAN_POINT('Ctrl Pts',(2.18172187678888,-1.1999723751995,-4.44089209850063E-16));
#47933=CARTESIAN_POINT('Ctrl Pts',(2.15328177937689,-1.24043139317656,1.90968323031924E-16));
#47934=CARTESIAN_POINT('Ctrl Pts',(2.1236626297252,-1.28011125530021,-1.24815247604854E-15));
#47935=CARTESIAN_POINT('Ctrl Pts',(2.09288546869145,-1.31894102140197,-2.05391259555654E-15));
#47936=CARTESIAN_POINT('Ctrl Pts',(2.08472665052523,-1.32923453095322,-2.69181282397187E-15));
#47937=CARTESIAN_POINT('Ctrl Pts',(2.07648733901943,-1.33946704131009,-3.53561961405176E-15));
#47938=CARTESIAN_POINT('Ctrl Pts',(2.06817568052717,-1.3496280615777,-3.71924713249427E-15));
#47939=CARTESIAN_POINT('Ctrl Pts',(2.01414238364663,-1.41568388247562,-3.61763159642546E-15));
#47940=CARTESIAN_POINT('Ctrl Pts',(1.95696807639177,-1.47883106713657,-2.1047465562029E-15));
#47941=CARTESIAN_POINT('Ctrl Pts',(1.8968144714638,-1.53877542768777,-2.27595720048157E-15));
#47942=CARTESIAN_POINT('Ctrl Pts',(1.83758356200986,-1.59780030236209,-1.96915150342469E-15));
#47943=CARTESIAN_POINT('Ctrl Pts',(1.77546340768274,-1.65372037610682,1.00684964781356E-15));
#47944=CARTESIAN_POINT('Ctrl Pts',(1.71058212136984,-1.70621256949937,0.));
#47945=CARTESIAN_POINT('Ctrl Pts',(1.64772546514904,-1.75706673626848,-1.47459711886327E-15));
#47946=CARTESIAN_POINT('Ctrl Pts',(1.58227673613707,-1.8047039083925,6.77258530541363E-16));
#47947=CARTESIAN_POINT('Ctrl Pts',(1.51433650217974,-1.84878472649022,1.66533453693773E-16));
#47948=CARTESIAN_POINT('Ctrl Pts',(1.46963595840449,-1.87778722507249,-6.32259699606435E-17));
#47949=CARTESIAN_POINT('Ctrl Pts',(1.4238565767745,-1.90524929950466,4.02804854125218E-16));
#47950=CARTESIAN_POINT('Ctrl Pts',(1.37702479013104,-1.93106208855763,-3.88578058618805E-16));
#47951=CARTESIAN_POINT('Ctrl Pts',(-1.03730518518318,2.12835542941762,-0.331584989410291));
#47952=CARTESIAN_POINT('Ctrl Pts',(-1.73864579252332,1.78654022387532,-0.279139884186583));
#47953=CARTESIAN_POINT('Ctrl Pts',(-2.7656846889405,0.361807027866601,-0.174249673739168));
#47954=CARTESIAN_POINT('Ctrl Pts',(-1.82129522076317,-2.11585284458798,
-0.0169143580680439));
#47955=CARTESIAN_POINT('Ctrl Pts',(0.764938575946876,-2.68229399094113,
0.140420957603079));
#47956=CARTESIAN_POINT('Ctrl Pts',(2.66139142426043,-0.837298121388289,
0.297756273274203));
#47957=CARTESIAN_POINT('Ctrl Pts',(2.16259871848842,1.76312751480994,0.455091588945326));
#47958=CARTESIAN_POINT('Ctrl Pts',(-0.283336766153592,2.77546827896293,
0.61242690461645));
#47959=CARTESIAN_POINT('Ctrl Pts',(-2.47403969246375,1.28971871163609,0.769762220287572));
#47960=CARTESIAN_POINT('Ctrl Pts',(-2.4376362160542,-1.35730685306026,0.927097535958697));
#47961=CARTESIAN_POINT('Ctrl Pts',(-0.206765733213128,-2.78232569956815,
1.08443285162982));
#47962=CARTESIAN_POINT('Ctrl Pts',(2.21021679152004,-1.70268993439413,1.24176816730094));
#47963=CARTESIAN_POINT('Ctrl Pts',(2.63751871827682,0.909784458804265,1.39910348297206));
#47964=CARTESIAN_POINT('Ctrl Pts',(0.690453185041018,2.70323004638949,1.55643879864319));
#47965=CARTESIAN_POINT('Ctrl Pts',(-1.87817235801244,2.06316899439893,1.71377411431431));
#47966=CARTESIAN_POINT('Ctrl Pts',(-2.75602147084388,-0.434213789166044,
1.87110942998544));
#47967=CARTESIAN_POINT('Ctrl Pts',(-1.15282950609521,-2.54070379675866,
2.02844474565656));
#47968=CARTESIAN_POINT('Ctrl Pts',(1.48816821785387,-2.35998939911264,2.18578006132768));
#47969=CARTESIAN_POINT('Ctrl Pts',(2.78947957168654,-0.0547522279601586,
2.34311537699881));
#47970=CARTESIAN_POINT('Ctrl Pts',(1.57963081483742,2.2997739166102,2.50045069266992));
#47971=CARTESIAN_POINT('Ctrl Pts',(-1.05224143668056,2.58398567580241,2.65778600834106));
#47972=CARTESIAN_POINT('Ctrl Pts',(-2.73685940153096,0.542028153256274,
2.81512132401217));
#47973=CARTESIAN_POINT('Ctrl Pts',(-1.9576873758141,-1.98787675326332,2.9724566396833));
#47974=CARTESIAN_POINT('Ctrl Pts',(0.583844270639632,-2.72824481623496,
3.12979195535442));
#47975=CARTESIAN_POINT('Ctrl Pts',(2.59978456082284,-1.01257796062119,3.28712727102555));
#47976=CARTESIAN_POINT('Ctrl Pts',(2.27533311107693,1.61463714733595,3.44446258669667));
#47977=CARTESIAN_POINT('Ctrl Pts',(-0.0974306831352009,2.78831511032893,
3.60179790236779));
#47978=CARTESIAN_POINT('Ctrl Pts',(-2.38248491584478,1.45188137075193,3.75913321803891));
#47979=CARTESIAN_POINT('Ctrl Pts',(-2.52276604076759,-1.19157265502464,
3.91646853371004));
#47980=CARTESIAN_POINT('Ctrl Pts',(-0.391989446068178,-2.76234287588842,
4.07380384938116));
#47981=CARTESIAN_POINT('Ctrl Pts',(2.09166595049596,-1.84638225748661,4.23113916505228));
#47982=CARTESIAN_POINT('Ctrl Pts',(2.69235081885991,0.731738312121609,4.38847448072341));
#47983=CARTESIAN_POINT('Ctrl Pts',(0.869313466150996,2.65112956811967,4.54580979639453));
#47984=CARTESIAN_POINT('Ctrl Pts',(-1.73630182933374,2.18390701421848,4.70314511206566));
#47985=CARTESIAN_POINT('Ctrl Pts',(-2.77885435571787,-0.24932380355531,
4.86048042773678));
#47986=CARTESIAN_POINT('Ctrl Pts',(-1.31981199187883,-2.45810703498086,
5.0178157434079));
#47987=CARTESIAN_POINT('Ctrl Pts',(1.32735846804311,-2.45404021699529,5.17515105907903));
#47988=CARTESIAN_POINT('Ctrl Pts',(2.77960730340162,-0.240784401894037,
5.33248637475015));
#47989=CARTESIAN_POINT('Ctrl Pts',(1.7295834260075,2.18923161447142,5.48982169042127));
#47990=CARTESIAN_POINT('Ctrl Pts',(-0.877455144085315,2.64844602728405,
5.6471570060924));
#47991=CARTESIAN_POINT('Ctrl Pts',(-2.6945864272668,0.723462421491616,5.80449232176352));
#47992=CARTESIAN_POINT('Ctrl Pts',(-2.08598293818204,-1.85280033218167,
5.96182763743465));
#47993=CARTESIAN_POINT('Ctrl Pts',(0.400475087797133,-2.76112542152107,
6.11916295310577));
#47994=CARTESIAN_POINT('Ctrl Pts',(2.52641532297249,-1.18381565506602,6.27649826877689));
#47995=CARTESIAN_POINT('Ctrl Pts',(2.37801266228852,1.45919486954518,6.43383358444801));
#47996=CARTESIAN_POINT('Ctrl Pts',(0.0888629298452703,2.78860131051387,
6.59116890011914));
#47997=CARTESIAN_POINT('Ctrl Pts',(-2.28028345691278,1.60763840633388,6.74850421579025));
#47998=CARTESIAN_POINT('Ctrl Pts',(-2.59666107137131,-1.02056120329308,
6.90583953146139));
#47999=CARTESIAN_POINT('Ctrl Pts',(-0.575458792795455,-2.73002583632828,
7.0631748471325));
#48000=CARTESIAN_POINT('Ctrl Pts',(1.96378602838758,-1.98185224588264,7.22051016280364));
#48001=CARTESIAN_POINT('Ctrl Pts',(2.73518105754109,0.550434801880421,7.37784547847475));
#48002=CARTESIAN_POINT('Ctrl Pts',(1.04429700325446,2.58720653562064,7.53518079414588));
#48003=CARTESIAN_POINT('Ctrl Pts',(-1.58668959526433,2.29490958880404,7.692516109817));
#48004=CARTESIAN_POINT('Ctrl Pts',(-2.78929813547626,-0.0633229448848314,
7.84985142548812));
#48005=CARTESIAN_POINT('Ctrl Pts',(-1.48091003456564,-2.36455056163985,
8.00718674115925));
#48006=CARTESIAN_POINT('Ctrl Pts',(1.1606306967401,-2.53715003408474,8.16452205683039));
#48007=CARTESIAN_POINT('Ctrl Pts',(2.7573423423768,-0.425742944184182,8.32185737250149));
#48008=CARTESIAN_POINT('Ctrl Pts',(1.87182477991027,2.06892868315578,8.47919268817262));
#48009=CARTESIAN_POINT('Ctrl Pts',(-0.698756781752635,2.70109847539371,
8.63652800384375));
#48010=CARTESIAN_POINT('Ctrl Pts',(-2.64029974777462,0.901671126634157,
8.79386331951485));
#48011=CARTESIAN_POINT('Ctrl Pts',(-2.2049783515218,-1.70946323641174,8.951198635186));
#48012=CARTESIAN_POINT('Ctrl Pts',(0.215320583295009,-2.78169582358745,
9.1085339508571));
#48013=CARTESIAN_POINT('Ctrl Pts',(2.44178186910215,-1.34977515042753,9.26586926652825));
#48014=CARTESIAN_POINT('Ctrl Pts',(2.4700906186972,1.29724642912539,9.42320458219936));
#48015=CARTESIAN_POINT('Ctrl Pts',(0.274759125503672,2.77645549735693,9.58053989787048));
#48016=CARTESIAN_POINT('Ctrl Pts',(-2.16791313571898,1.75622632949552,9.73787521354162));
#48017=CARTESIAN_POINT('Ctrl Pts',(-2.65898352045171,-0.844996679702688,
9.89521052921272));
#48018=CARTESIAN_POINT('Ctrl Pts',(-0.756353910490317,-2.68554278318001,
10.0525458448839));
#48019=CARTESIAN_POINT('Ctrl Pts',(1.82713427411632,-2.1084754471556,10.209881160555));
#48020=CARTESIAN_POINT('Ctrl Pts',(2.76584800687315,0.366656539637837,10.3672164762261));
#48021=CARTESIAN_POINT('Ctrl Pts',(1.21456463397637,2.5117881090817,10.5245517918972));
#48022=CARTESIAN_POINT('Ctrl Pts',(-1.42988853112819,2.3956048670705,10.6818871075684));
#48023=CARTESIAN_POINT('Ctrl Pts',(-2.78752525882336,0.123104760709679,
10.8392224232395));
#48024=CARTESIAN_POINT('Ctrl Pts',(-1.63498599745775,-2.26072847669162,
10.9965577389106));
#48025=CARTESIAN_POINT('Ctrl Pts',(0.987923826072495,-2.60841687478992,
11.1538930545817));
#48026=CARTESIAN_POINT('Ctrl Pts',(2.72434297818965,-0.609840043220031,
11.3112283702529));
#48027=CARTESIAN_POINT('Ctrl Pts',(2.00243986412736,1.94197408587787,11.4685886307918));
#48028=CARTESIAN_POINT('Ctrl Pts',(0.327206363769202,2.47149229332866,11.573503786107));
#48029=CARTESIAN_POINT('Ctrl Pts',(-0.439784697349138,2.32647548997369,
11.6259738361986));
#48030=CARTESIAN_POINT('Ctrl Pts',(-1.12171304089722,2.30154449716799,-0.22035079308787));
#48031=CARTESIAN_POINT('Ctrl Pts',(-1.88012331070157,1.93191501964248,-0.167905687864162));
#48032=CARTESIAN_POINT('Ctrl Pts',(-2.99073467182806,0.391248079391971,
-0.0630154774167469));
#48033=CARTESIAN_POINT('Ctrl Pts',(-1.96949810878762,-2.28802454889368,
0.094319838254377));
#48034=CARTESIAN_POINT('Ctrl Pts',(0.827183348142068,-2.90055828519513,
0.2516551539255));
#48035=CARTESIAN_POINT('Ctrl Pts',(2.87795482965583,-0.905430952525466,
0.408990469596625));
#48036=CARTESIAN_POINT('Ctrl Pts',(2.33857423968022,1.90659716578758,0.566325785267747));
#48037=CARTESIAN_POINT('Ctrl Pts',(-0.306392516011564,3.00131437457293,
0.723661100938869));
#48038=CARTESIAN_POINT('Ctrl Pts',(-2.67535786610753,1.39466602365043,0.880996416609994));
#48039=CARTESIAN_POINT('Ctrl Pts',(-2.63599215695478,-1.46775396414121,
1.03833173228112));
#48040=CARTESIAN_POINT('Ctrl Pts',(-0.223590725920167,-3.00872979891445,
1.19566704795224));
#48041=CARTESIAN_POINT('Ctrl Pts',(2.39006710240269,-1.84124164353529,1.35300236362336));
#48042=CARTESIAN_POINT('Ctrl Pts',(2.852139547899,0.983815666231478,1.51033767929448));
#48043=CARTESIAN_POINT('Ctrl Pts',(0.746636913468031,2.92319795455841,1.66767299496561));
#48044=CARTESIAN_POINT('Ctrl Pts',(-2.03100346660582,2.23105369533406,1.82500831063673));
#48045=CARTESIAN_POINT('Ctrl Pts',(-2.98028513594331,-0.469546741693888,
1.98234362630786));
#48046=CARTESIAN_POINT('Ctrl Pts',(-1.24663783560453,-2.74744657848983,
2.13967894197898));
#48047=CARTESIAN_POINT('Ctrl Pts',(1.60926381248222,-2.55202704389875,2.2970142576501));
#48048=CARTESIAN_POINT('Ctrl Pts',(3.01646579769545,-0.0592075398815808,
2.45434957332123));
#48049=CARTESIAN_POINT('Ctrl Pts',(1.70816892667258,2.48691169216645,2.61168488899235));
#48050=CARTESIAN_POINT('Ctrl Pts',(-1.13786468876907,2.794250401368,2.76902020466348));
#48051=CARTESIAN_POINT('Ctrl Pts',(-2.95956380595681,0.586134203053899,
2.92635552033459));
#48052=CARTESIAN_POINT('Ctrl Pts',(-2.11698880022736,-2.14963475521249,
3.08369083600572));
#48053=CARTESIAN_POINT('Ctrl Pts',(0.631352991948975,-2.95024823248193,
3.24102615167684));
#48054=CARTESIAN_POINT('Ctrl Pts',(2.81133487719265,-1.09497370646359,3.39836146734797));
#48055=CARTESIAN_POINT('Ctrl Pts',(2.46048208332205,1.74602380317224,3.55569678301909));
#48056=CARTESIAN_POINT('Ctrl Pts',(-0.105358836933763,3.01520658149842,
3.71303209869021));
#48057=CARTESIAN_POINT('Ctrl Pts',(-2.57635307141754,1.57002422302613,3.87036741436133));
#48058=CARTESIAN_POINT('Ctrl Pts',(-2.72804918695356,-1.28853360169179,
4.02770273003246));
#48059=CARTESIAN_POINT('Ctrl Pts',(-0.423886508839853,-2.98712092793252,
4.18503804570358));
#48060=CARTESIAN_POINT('Ctrl Pts',(2.26186951283549,-1.99662653410748,4.34237336137471));
#48061=CARTESIAN_POINT('Ctrl Pts',(2.91143345981847,0.79128150418526,4.49970867704583));
#48062=CARTESIAN_POINT('Ctrl Pts',(0.940051457890825,2.86685794320302,4.65704399271695));
#48063=CARTESIAN_POINT('Ctrl Pts',(-1.8775886139559,2.36161643935406,4.81437930838807));
#48064=CARTESIAN_POINT('Ctrl Pts',(-3.00497598400837,-0.269611842154904,
4.97171462405921));
#48065=CARTESIAN_POINT('Ctrl Pts',(-1.4272080617833,-2.6581287324543,5.12904993973032));
#48066=CARTESIAN_POINT('Ctrl Pts',(1.4353686116843,-2.65373098834339,5.28638525540146));
#48067=CARTESIAN_POINT('Ctrl Pts',(3.00579020073843,-0.260377570176227,
5.44372057107256));
#48068=CARTESIAN_POINT('Ctrl Pts',(1.87032351904202,2.36737431430406,5.6010558867437));
#48069=CARTESIAN_POINT('Ctrl Pts',(-0.94885564246845,2.86395603661459,5.75839120241481));
#48070=CARTESIAN_POINT('Ctrl Pts',(-2.91385098470907,0.782332185723086,
5.91572651808595));
#48071=CARTESIAN_POINT('Ctrl Pts',(-2.25572406102908,-2.00356686197406,
6.07306183375706));
#48072=CARTESIAN_POINT('Ctrl Pts',(0.43306264631962,-2.98580440656537,6.23039714942819));
#48073=CARTESIAN_POINT('Ctrl Pts',(2.73199541945832,-1.28014539720187,6.38773246509931));
#48074=CARTESIAN_POINT('Ctrl Pts',(2.57151690053176,1.57793283766349,6.54506778077043));
#48075=CARTESIAN_POINT('Ctrl Pts',(0.0960939062906457,3.01551607043604,
6.70240309644156));
#48076=CARTESIAN_POINT('Ctrl Pts',(-2.46583524993137,1.73845555887539,6.85973841211269));
#48077=CARTESIAN_POINT('Ctrl Pts',(-2.80795722238004,-1.10360656354518,
7.0170737277838));
#48078=CARTESIAN_POINT('Ctrl Pts',(-0.622285168914556,-2.95217417818558,
7.17440904345494));
#48079=CARTESIAN_POINT('Ctrl Pts',(2.123583713876,-2.14312002011776,7.33174435912604));
#48080=CARTESIAN_POINT('Ctrl Pts',(2.95774889134204,0.595224919582278,7.48907967479718));
#48081=CARTESIAN_POINT('Ctrl Pts',(1.12927379892889,2.79773334979303,7.64641499046829));
#48082=CARTESIAN_POINT('Ctrl Pts',(-1.7158020959373,2.48165154306736,7.80375030613943));
#48083=CARTESIAN_POINT('Ctrl Pts',(-3.01626959761271,-0.0684756753170684,
7.96108562181053));
#48084=CARTESIAN_POINT('Ctrl Pts',(-1.60141501449694,-2.55695935847839,
8.11842093748168));
#48085=CARTESIAN_POINT('Ctrl Pts',(1.25507382667628,-2.74360363815508,8.27575625315278));
#48086=CARTESIAN_POINT('Ctrl Pts',(2.98171348976335,-0.4603866050058,8.43309156882392));
#48087=CARTESIAN_POINT('Ctrl Pts',(2.02413937179845,2.23728206291798,8.59042688449505));
#48088=CARTESIAN_POINT('Ctrl Pts',(-0.755616192517999,2.92089293283704,
8.74776220016616));
#48089=CARTESIAN_POINT('Ctrl Pts',(-2.8551468760213,0.975042133976645,8.90509751583729));
#48090=CARTESIAN_POINT('Ctrl Pts',(-2.38440239876109,-1.84856610437053,
9.0624328315084));
#48091=CARTESIAN_POINT('Ctrl Pts',(0.232841703392179,-3.00804866850868,
9.21976814717955));
#48092=CARTESIAN_POINT('Ctrl Pts',(2.64047515111439,-1.45960938992725,9.37710346285064));
#48093=CARTESIAN_POINT('Ctrl Pts',(2.67108744732754,1.40280628844088,9.5344387785218));
#48094=CARTESIAN_POINT('Ctrl Pts',(0.297116893451739,3.00238192514779,9.69177409419289));
#48095=CARTESIAN_POINT('Ctrl Pts',(-2.34432110299241,1.89913441550408,9.84910940986404));
#48096=CARTESIAN_POINT('Ctrl Pts',(-2.87535098929907,-0.913755959843164,
10.0064447255352));
#48097=CARTESIAN_POINT('Ctrl Pts',(-0.817900129151285,-2.90407143896469,
10.1637800412063));
#48098=CARTESIAN_POINT('Ctrl Pts',(1.97581229904352,-2.28004683604122,10.3211153568773));
#48099=CARTESIAN_POINT('Ctrl Pts',(2.99091127930818,0.396492206842064,10.4784506725486));
#48100=CARTESIAN_POINT('Ctrl Pts',(1.31339648967752,2.71617795627811,10.6357859882197));
#48101=CARTESIAN_POINT('Ctrl Pts',(-1.54624177658248,2.59054062257996,10.7931213038908));
#48102=CARTESIAN_POINT('Ctrl Pts',(-3.01435245799954,0.133122071938945,
10.9504566195618));
#48103=CARTESIAN_POINT('Ctrl Pts',(-1.76802848499101,-2.44468903699242,
11.1077919352331));
#48104=CARTESIAN_POINT('Ctrl Pts',(1.06831340954195,-2.82066962196045,11.2651272509042));
#48105=CARTESIAN_POINT('Ctrl Pts',(2.94602889310002,-0.659464099006171,
11.4224625665753));
#48106=CARTESIAN_POINT('Ctrl Pts',(2.16538289915855,2.09999688455137,11.5798228271142));
#48107=CARTESIAN_POINT('Ctrl Pts',(0.353831881443529,2.67260317937598,11.6847379824294));
#48108=CARTESIAN_POINT('Ctrl Pts',(-0.475570967204255,2.51578603260372,
11.737208032521));
#48109=CARTESIAN_POINT('Ctrl Pts',(-1.20612089661124,2.47473356491836,-0.109116596765449));
#48110=CARTESIAN_POINT('Ctrl Pts',(-2.02160082887981,2.07728981540964,-0.0566714915417416));
#48111=CARTESIAN_POINT('Ctrl Pts',(-3.21578465471561,0.420689130917341,
0.0482187189056736));
#48112=CARTESIAN_POINT('Ctrl Pts',(-2.11770099681207,-2.46019625319938,
0.205554034576798));
#48113=CARTESIAN_POINT('Ctrl Pts',(0.88942812033726,-3.11882257944914,0.36288935024792));
#48114=CARTESIAN_POINT('Ctrl Pts',(3.09451823505123,-0.973563783662645,
0.520224665919045));
#48115=CARTESIAN_POINT('Ctrl Pts',(2.51454976087203,2.05006681676523,0.677559981590167));
#48116=CARTESIAN_POINT('Ctrl Pts',(-0.329448265869537,3.22716047018292,
0.834895297261292));
#48117=CARTESIAN_POINT('Ctrl Pts',(-2.87667603975131,1.49961333566476,0.992230612932414));
#48118=CARTESIAN_POINT('Ctrl Pts',(-2.83434809785535,-1.57820107522217,
1.14956592860354));
#48119=CARTESIAN_POINT('Ctrl Pts',(-0.240415718627206,-3.23513389826074,
1.30690124427466));
#48120=CARTESIAN_POINT('Ctrl Pts',(2.56991741328534,-1.97979335267645,1.46423655994578));
#48121=CARTESIAN_POINT('Ctrl Pts',(3.0667603775212,1.05784687365869,1.62157187561691));
#48122=CARTESIAN_POINT('Ctrl Pts',(0.802820641895047,3.14316586272734,1.77890719128803));
#48123=CARTESIAN_POINT('Ctrl Pts',(-2.18383457519921,2.3989383962692,1.93624250695915));
#48124=CARTESIAN_POINT('Ctrl Pts',(-3.20454880104273,-0.504879694221727,
2.09357782263028));
#48125=CARTESIAN_POINT('Ctrl Pts',(-1.34044616511386,-2.954189360221,2.2509131383014));
#48126=CARTESIAN_POINT('Ctrl Pts',(1.73035940711057,-2.74406468868485,2.40824845397252));
#48127=CARTESIAN_POINT('Ctrl Pts',(3.24345202370436,-0.0636628518030065,
2.56558376964365));
#48128=CARTESIAN_POINT('Ctrl Pts',(1.83670703850775,2.67404946772271,2.72291908531477));
#48129=CARTESIAN_POINT('Ctrl Pts',(-1.22348794085758,3.00451512693359,2.8802544009859));
#48130=CARTESIAN_POINT('Ctrl Pts',(-3.18226821038265,0.630240252851527,
3.03758971665701));
#48131=CARTESIAN_POINT('Ctrl Pts',(-2.27629022464062,-2.31139275716167,
3.19492503232815));
#48132=CARTESIAN_POINT('Ctrl Pts',(0.678861713258322,-3.1722516487289,3.35226034799926));
#48133=CARTESIAN_POINT('Ctrl Pts',(3.02288519356245,-1.17736945230598,3.50959566367039));
#48134=CARTESIAN_POINT('Ctrl Pts',(2.64563105556716,1.87741045900853,3.66693097934151));
#48135=CARTESIAN_POINT('Ctrl Pts',(-0.113286990732327,3.2420980526679,3.82426629501263));
#48136=CARTESIAN_POINT('Ctrl Pts',(-2.77022122699029,1.68816707530034,3.98160161068376));
#48137=CARTESIAN_POINT('Ctrl Pts',(-2.93333233313953,-1.38549454835895,
4.13893692635488));
#48138=CARTESIAN_POINT('Ctrl Pts',(-0.455783571611524,-3.21189897997662,
4.29627224202601));
#48139=CARTESIAN_POINT('Ctrl Pts',(2.43207307517502,-2.14687081072835,4.45360755769713));
#48140=CARTESIAN_POINT('Ctrl Pts',(3.13051610077702,0.850824696248917,4.61094287336825));
#48141=CARTESIAN_POINT('Ctrl Pts',(1.01078944963065,3.08258631828635,4.76827818903937));
#48142=CARTESIAN_POINT('Ctrl Pts',(-2.01887539857807,2.53932586448964,4.9256135047105));
#48143=CARTESIAN_POINT('Ctrl Pts',(-3.23109761229886,-0.289899880754502,
5.08294882038162));
#48144=CARTESIAN_POINT('Ctrl Pts',(-1.53460413168777,-2.85815042992774,
5.24028413605275));
#48145=CARTESIAN_POINT('Ctrl Pts',(1.54337875532549,-2.8534217596915,5.39761945172386));
#48146=CARTESIAN_POINT('Ctrl Pts',(3.23197309807526,-0.279970738458419,
5.554954767395));
#48147=CARTESIAN_POINT('Ctrl Pts',(2.01106361207652,2.5455170141367,5.71229008306611));
#48148=CARTESIAN_POINT('Ctrl Pts',(-1.02025614085158,3.07946604594513,5.86962539873724));
#48149=CARTESIAN_POINT('Ctrl Pts',(-3.13311554215134,0.841201949954562,
6.02696071440836));
#48150=CARTESIAN_POINT('Ctrl Pts',(-2.42546518387612,-2.15433339176646,
6.18429603007949));
#48151=CARTESIAN_POINT('Ctrl Pts',(0.465650204842104,-3.21048339160967,
6.34163134575061));
#48152=CARTESIAN_POINT('Ctrl Pts',(2.93757551594416,-1.3764751393377,6.49896666142173));
#48153=CARTESIAN_POINT('Ctrl Pts',(2.76502113877501,1.6966708057818,6.65630197709286));
#48154=CARTESIAN_POINT('Ctrl Pts',(0.103324882736022,3.24243083035821,6.81363729276398));
#48155=CARTESIAN_POINT('Ctrl Pts',(-2.65138704294996,1.86927271141691,6.9709726084351));
#48156=CARTESIAN_POINT('Ctrl Pts',(-3.01925337338877,-1.18665192379726,
7.12830792410623));
#48157=CARTESIAN_POINT('Ctrl Pts',(-0.66911154503365,-3.17432252004288,
7.28564323977735));
#48158=CARTESIAN_POINT('Ctrl Pts',(2.28338139936439,-2.30438779435288,7.44297855544847));
#48159=CARTESIAN_POINT('Ctrl Pts',(3.18031672514302,0.640015037284128,7.6003138711196));
#48160=CARTESIAN_POINT('Ctrl Pts',(1.21425059460331,3.0082601639654,7.75764918679072));
#48161=CARTESIAN_POINT('Ctrl Pts',(-1.84491459661027,2.66839349733066,7.91498450246185));
#48162=CARTESIAN_POINT('Ctrl Pts',(-3.24324105974916,-0.0736284057493019,
8.07231981813296));
#48163=CARTESIAN_POINT('Ctrl Pts',(-1.72191999442822,-2.74936815531691,
8.2296551338041));
#48164=CARTESIAN_POINT('Ctrl Pts',(1.34951695661245,-2.95005724222544,8.3869904494752));
#48165=CARTESIAN_POINT('Ctrl Pts',(3.20608463714991,-0.495030265827418,
8.54432576514635));
#48166=CARTESIAN_POINT('Ctrl Pts',(2.17645396368663,2.40563544268021,8.70166108081746));
#48167=CARTESIAN_POINT('Ctrl Pts',(-0.812475603283364,3.14068739028035,
8.85899639648857));
#48168=CARTESIAN_POINT('Ctrl Pts',(-3.06999400426798,1.04841314131914,9.01633171215972));
#48169=CARTESIAN_POINT('Ctrl Pts',(-2.56382644600038,-1.9876689723293,9.17366702783083));
#48170=CARTESIAN_POINT('Ctrl Pts',(0.250362823489351,-3.2344015134299,9.33100234350195));
#48171=CARTESIAN_POINT('Ctrl Pts',(2.83916843312661,-1.56944362942696,9.48833765917307));
#48172=CARTESIAN_POINT('Ctrl Pts',(2.87208427595788,1.50836614775637,9.64567297484422));
#48173=CARTESIAN_POINT('Ctrl Pts',(0.319474661399804,3.22830835293867,9.80300829051531));
#48174=CARTESIAN_POINT('Ctrl Pts',(-2.52072907026583,2.04204250151264,9.96034360618647));
#48175=CARTESIAN_POINT('Ctrl Pts',(-3.09171845814643,-0.982515239983637,
10.1176789218575));
#48176=CARTESIAN_POINT('Ctrl Pts',(-0.879446347812255,-3.12260009474938,
10.2750142375287));
#48177=CARTESIAN_POINT('Ctrl Pts',(2.12449032397074,-2.45161822492683,10.4323495531998));
#48178=CARTESIAN_POINT('Ctrl Pts',(3.2159745517432,0.42632787404629,10.5896848688709));
#48179=CARTESIAN_POINT('Ctrl Pts',(1.41222834537867,2.92056780347451,10.7470201845421));
#48180=CARTESIAN_POINT('Ctrl Pts',(-1.66259502203677,2.78547637808942,10.9043555002132));
#48181=CARTESIAN_POINT('Ctrl Pts',(-3.24117965717572,0.143139383168213,
11.0616908158843));
#48182=CARTESIAN_POINT('Ctrl Pts',(-1.90107097252427,-2.62864959729321,
11.2190261315554));
#48183=CARTESIAN_POINT('Ctrl Pts',(1.1487029930114,-3.03292236913098,11.3763614472266));
#48184=CARTESIAN_POINT('Ctrl Pts',(3.1677148080104,-0.709088154792314,11.5336967628977));
#48185=CARTESIAN_POINT('Ctrl Pts',(2.32832593418973,2.25801968322488,11.6910570234366));
#48186=CARTESIAN_POINT('Ctrl Pts',(0.380457399117856,2.8737140654233,11.7959721787519));
#48187=CARTESIAN_POINT('Ctrl Pts',(-0.511357237059373,2.70509657523375,
11.8484422288434));
#48188=CARTESIAN_POINT('Ctrl Pts',(-1.29052875232528,2.64792263266873,0.00211759955697117));
#48189=CARTESIAN_POINT('Ctrl Pts',(-2.16307834705805,2.22266461117681,0.054562704780679));
#48190=CARTESIAN_POINT('Ctrl Pts',(-3.44083463760316,0.45013018244271,0.159452915228094));
#48191=CARTESIAN_POINT('Ctrl Pts',(-2.26590388483652,-2.63236795750508,
0.316788230899218));
#48192=CARTESIAN_POINT('Ctrl Pts',(0.951672892532446,-3.33708687370315,
0.474123546570341));
#48193=CARTESIAN_POINT('Ctrl Pts',(3.31108164044663,-1.04169661479983,0.631458862241466));
#48194=CARTESIAN_POINT('Ctrl Pts',(2.69052528206383,2.19353646774287,0.788794177912587));
#48195=CARTESIAN_POINT('Ctrl Pts',(-0.352504015727509,3.45300656579291,
0.946129493583712));
#48196=CARTESIAN_POINT('Ctrl Pts',(-3.07799421339509,1.6045606476791,1.10346480925483));
#48197=CARTESIAN_POINT('Ctrl Pts',(-3.03270403875592,-1.68864818630313,
1.26080012492596));
#48198=CARTESIAN_POINT('Ctrl Pts',(-0.257240711334243,-3.46153799760704,
1.41813544059708));
#48199=CARTESIAN_POINT('Ctrl Pts',(2.74976772416799,-2.11834506181761,1.57547075626821));
#48200=CARTESIAN_POINT('Ctrl Pts',(3.2813812071434,1.13187808108589,1.73280607193933));
#48201=CARTESIAN_POINT('Ctrl Pts',(0.859004370322057,3.36313377089626,1.89014138761045));
#48202=CARTESIAN_POINT('Ctrl Pts',(-2.3366656837926,2.56682309720432,2.04747670328157));
#48203=CARTESIAN_POINT('Ctrl Pts',(-3.42881246614216,-0.540212646749566,
2.2048120189527));
#48204=CARTESIAN_POINT('Ctrl Pts',(-1.43425449462318,-3.16093214195217,
2.36214733462382));
#48205=CARTESIAN_POINT('Ctrl Pts',(1.85145500173891,-2.93610233347096,2.51948265029494));
#48206=CARTESIAN_POINT('Ctrl Pts',(3.47043824971327,-0.0681181637244305,
2.67681796596607));
#48207=CARTESIAN_POINT('Ctrl Pts',(1.96524515034292,2.86118724327898,2.83415328163719));
#48208=CARTESIAN_POINT('Ctrl Pts',(-1.30911119294609,3.21477985249918,2.99148859730832));
#48209=CARTESIAN_POINT('Ctrl Pts',(-3.40497261480849,0.674346302649153,
3.14882391297943));
#48210=CARTESIAN_POINT('Ctrl Pts',(-2.43559164905389,-2.47315075911084,
3.30615922865057));
#48211=CARTESIAN_POINT('Ctrl Pts',(0.726370434567669,-3.39425506497587,
3.46349454432168));
#48212=CARTESIAN_POINT('Ctrl Pts',(3.23443550993226,-1.25976519814839,3.62082985999281));
#48213=CARTESIAN_POINT('Ctrl Pts',(2.83078002781227,2.00879711484483,3.77816517566393));
#48214=CARTESIAN_POINT('Ctrl Pts',(-0.12121514453089,3.46898952383738,3.93550049133506));
#48215=CARTESIAN_POINT('Ctrl Pts',(-2.96408938256305,1.80630992757453,4.09283580700618));
#48216=CARTESIAN_POINT('Ctrl Pts',(-3.1386154793255,-1.48245549502611,4.2501711226773));
#48217=CARTESIAN_POINT('Ctrl Pts',(-0.4876806343832,-3.43667703202072,4.40750643834843));
#48218=CARTESIAN_POINT('Ctrl Pts',(2.60227663751455,-2.29711508734921,4.56484175401955));
#48219=CARTESIAN_POINT('Ctrl Pts',(3.34959874173558,0.91036788831257,4.72217706969067));
#48220=CARTESIAN_POINT('Ctrl Pts',(1.08152744137048,3.29831469336969,4.87951238536179));
#48221=CARTESIAN_POINT('Ctrl Pts',(-2.16016218320023,2.71703528962523,5.03684770103292));
#48222=CARTESIAN_POINT('Ctrl Pts',(-3.45721924058936,-0.310187919354095,
5.19418301670405));
#48223=CARTESIAN_POINT('Ctrl Pts',(-1.64200020159223,-3.05817212740119,
5.35151833237516));
#48224=CARTESIAN_POINT('Ctrl Pts',(1.65138889896668,-3.05311253103961,5.5088536480463));
#48225=CARTESIAN_POINT('Ctrl Pts',(3.45815599541208,-0.299563906740608,
5.66618896371741));
#48226=CARTESIAN_POINT('Ctrl Pts',(2.15180370511103,2.72365971396933,5.82352427938854));
#48227=CARTESIAN_POINT('Ctrl Pts',(-1.09165663923471,3.29497605527567,5.98085959505965));
#48228=CARTESIAN_POINT('Ctrl Pts',(-3.35238009959362,0.900071714186031,
6.13819491073079));
#48229=CARTESIAN_POINT('Ctrl Pts',(-2.59520630672316,-2.30509992155884,
6.2955302264019));
#48230=CARTESIAN_POINT('Ctrl Pts',(0.498237763364587,-3.43516237665397,
6.45286554207304));
#48231=CARTESIAN_POINT('Ctrl Pts',(3.14315561242999,-1.47280488147353,6.61020085774415));
#48232=CARTESIAN_POINT('Ctrl Pts',(2.95852537701825,1.8154087739001,6.76753617341528));
#48233=CARTESIAN_POINT('Ctrl Pts',(0.110555859181397,3.46934559028038,6.9248714890864));
#48234=CARTESIAN_POINT('Ctrl Pts',(-2.83693883596855,2.00008986395841,7.08220680475753));
#48235=CARTESIAN_POINT('Ctrl Pts',(-3.2305495243975,-1.26969728404936,7.23954212042865));
#48236=CARTESIAN_POINT('Ctrl Pts',(-0.715937921152747,-3.39647086190017,
7.39687743609977));
#48237=CARTESIAN_POINT('Ctrl Pts',(2.4431790848528,-2.465655568588,7.5542127517709));
#48238=CARTESIAN_POINT('Ctrl Pts',(3.40288455894398,0.684805154985982,7.71154806744202));
#48239=CARTESIAN_POINT('Ctrl Pts',(1.29922739027773,3.21878697813778,7.86888338311314));
#48240=CARTESIAN_POINT('Ctrl Pts',(-1.97402709728324,2.85513545159397,8.02621869878427));
#48241=CARTESIAN_POINT('Ctrl Pts',(-3.47021252188561,-0.0787811361815389,
8.18355401445539));
#48242=CARTESIAN_POINT('Ctrl Pts',(-1.84242497435951,-2.94177695215544,
8.34088933012651));
#48243=CARTESIAN_POINT('Ctrl Pts',(1.44396008654862,-3.15651084629578,8.49822464579763));
#48244=CARTESIAN_POINT('Ctrl Pts',(3.43045578453647,-0.529673926649034,
8.65555996146877));
#48245=CARTESIAN_POINT('Ctrl Pts',(2.32876855557479,2.57398882244243,8.81289527713988));
#48246=CARTESIAN_POINT('Ctrl Pts',(-0.869335014048728,3.36048184772367,
8.97023059281101));
#48247=CARTESIAN_POINT('Ctrl Pts',(-3.28484113251466,1.12178414866162,9.12756590848212));
#48248=CARTESIAN_POINT('Ctrl Pts',(-2.74325049323966,-2.12677184028809,
9.28490122415326));
#48249=CARTESIAN_POINT('Ctrl Pts',(0.26788394358652,-3.46075435835112,9.44223653982438));
#48250=CARTESIAN_POINT('Ctrl Pts',(3.03786171513884,-1.67927786892668,9.5995718554955));
#48251=CARTESIAN_POINT('Ctrl Pts',(3.07308110458822,1.61392600707186,9.75690717116663));
#48252=CARTESIAN_POINT('Ctrl Pts',(0.34183242934787,3.45423478072953,9.91424248683774));
#48253=CARTESIAN_POINT('Ctrl Pts',(-2.69713703753925,2.1849505875212,10.0715778025089));
#48254=CARTESIAN_POINT('Ctrl Pts',(-3.30808592699379,-1.05127452012411,
10.22891311818));
#48255=CARTESIAN_POINT('Ctrl Pts',(-0.940992566473223,-3.34112875053406,
10.3862484338511));
#48256=CARTESIAN_POINT('Ctrl Pts',(2.27316834889794,-2.62318961381246,10.5435837495223));
#48257=CARTESIAN_POINT('Ctrl Pts',(3.44103782417822,0.456163541250519,10.7009190651934));
#48258=CARTESIAN_POINT('Ctrl Pts',(1.51106020107982,3.12495765067091,10.8582543808645));
#48259=CARTESIAN_POINT('Ctrl Pts',(-1.77894826749106,2.9804121335989,11.0155896965356));
#48260=CARTESIAN_POINT('Ctrl Pts',(-3.4680068563519,0.15315669439748,11.1729250122068));
#48261=CARTESIAN_POINT('Ctrl Pts',(-2.03411346005753,-2.812610157594,11.3302603278779));
#48262=CARTESIAN_POINT('Ctrl Pts',(1.22909257648086,-3.24517511630151,11.487595643549));
#48263=CARTESIAN_POINT('Ctrl Pts',(3.38940072292078,-0.758712210578455,
11.6449309592201));
#48264=CARTESIAN_POINT('Ctrl Pts',(2.49126896922092,2.41604248189839,11.8022912197591));
#48265=CARTESIAN_POINT('Ctrl Pts',(0.407082916792181,3.07482495147061,11.9072063750743));
#48266=CARTESIAN_POINT('Ctrl Pts',(-0.54714350691449,2.89440711786378,11.9596764251658));
#48267=CARTESIAN_POINT('Ctrl Pts',(-1.37989654081095,-1.933266887693,-5.06105574116233E-16));
#48268=CARTESIAN_POINT('Ctrl Pts',(-1.44414345926609,-1.89839188587405,
-3.26328455905852E-15));
#48269=CARTESIAN_POINT('Ctrl Pts',(-1.5065284577229,-1.86047032724736,-1.75540264544042E-15));
#48270=CARTESIAN_POINT('Ctrl Pts',(-1.56680444439783,-1.81955553349441,
-1.38777878078145E-15));
#48271=CARTESIAN_POINT('Ctrl Pts',(-1.63482660542644,-1.77338270675787,
-7.7622414528857E-16));
#48272=CARTESIAN_POINT('Ctrl Pts',(-1.70016423572007,-1.72339917541855,
-2.57234059054026E-16));
#48273=CARTESIAN_POINT('Ctrl Pts',(-1.76273246655484,-1.66996621356204,
-6.59194920871187E-16));
#48274=CARTESIAN_POINT('Ctrl Pts',(-1.80339137476382,-1.63524370562994,
-9.20402398950369E-16));
#48275=CARTESIAN_POINT('Ctrl Pts',(-1.84288047050014,-1.59906346566465,
3.12793119993545E-15));
#48276=CARTESIAN_POINT('Ctrl Pts',(-1.88117141744704,-1.56151405921778,
3.25434124093249E-15));
#48277=CARTESIAN_POINT('Ctrl Pts',(-1.89157558896771,-1.55131137434519,
3.31815239224361E-15));
#48278=CARTESIAN_POINT('Ctrl Pts',(-1.90188938652621,-1.54100934347453,
8.33738107600677E-16));
#48279=CARTESIAN_POINT('Ctrl Pts',(-1.91210630257196,-1.53061605927471,
1.19348975147204E-15));
#48280=CARTESIAN_POINT('Ctrl Pts',(-1.97123493955355,-1.47046672206319,
2.12803477396886E-15));
#48281=CARTESIAN_POINT('Ctrl Pts',(-2.02717988586207,-1.40720695656129,
2.65582936227977E-16));
#48282=CARTESIAN_POINT('Ctrl Pts',(-2.0798563871476,-1.34121621912243,1.70696790036118E-15));
#48283=CARTESIAN_POINT('Ctrl Pts',(-2.13394121087249,-1.27346119905171,
3.18688873417464E-15));
#48284=CARTESIAN_POINT('Ctrl Pts',(-2.18458111819303,-1.20282670578501,
2.66863689364878E-15));
#48285=CARTESIAN_POINT('Ctrl Pts',(-2.23165714456555,-1.12967611923023,
1.9151347174784E-15));
#48286=CARTESIAN_POINT('Ctrl Pts',(-2.24684650541785,-1.10607364592577,
1.67201274354048E-15));
#48287=CARTESIAN_POINT('Ctrl Pts',(-2.26166459424814,-1.08220890431245,
1.49719989934545E-15));
#48288=CARTESIAN_POINT('Ctrl Pts',(-2.27610666055719,-1.05809323638609,
1.13797860024079E-15));
#48289=CARTESIAN_POINT('Ctrl Pts',(-2.28578146762193,-1.0419380388242,8.35160740259033E-16));
#48290=CARTESIAN_POINT('Ctrl Pts',(-2.29528887628369,-1.02566760843717,
3.28760802647304E-15));
#48291=CARTESIAN_POINT('Ctrl Pts',(-2.30461525834334,-1.0093071858719,3.5527136788005E-15));
#48292=CARTESIAN_POINT('Ctrl Pts',(-2.34873078931698,-0.931919328093436,
3.71885869706561E-15));
#48293=CARTESIAN_POINT('Ctrl Pts',(-2.38885771815723,-0.852425177482761,
5.32218017872543E-15));
#48294=CARTESIAN_POINT('Ctrl Pts',(-2.42490246723541,-0.771229500912766,
5.34294830600857E-15));
#48295=CARTESIAN_POINT('Ctrl Pts',(-2.46140438292463,-0.689003994666118,
5.36397984182167E-15));
#48296=CARTESIAN_POINT('Ctrl Pts',(-2.4937205277099,-0.605032771340319,
6.32528744906619E-15));
#48297=CARTESIAN_POINT('Ctrl Pts',(-2.52171972824353,-0.519694226037686,
4.57966997657877E-15));
#48298=CARTESIAN_POINT('Ctrl Pts',(-2.54960930028344,-0.43468981656746,
2.84088732117391E-15));
#48299=CARTESIAN_POINT('Ctrl Pts',(-2.57321620377506,-0.348327885492083,
5.7661356876764E-15));
#48300=CARTESIAN_POINT('Ctrl Pts',(-2.59236876994043,-0.260953527499912,
4.9960036108132E-15));
#48301=CARTESIAN_POINT('Ctrl Pts',(-2.60380936393625,-0.208761327937561,
4.53597291108992E-15));
#48302=CARTESIAN_POINT('Ctrl Pts',(-2.61365974280453,-0.156207387307918,
3.44984801162762E-15));
#48303=CARTESIAN_POINT('Ctrl Pts',(-2.62187489230509,-0.103362317982872,
3.33066907387547E-15));
#48304=CARTESIAN_POINT('Ctrl Pts',(-2.62397146608191,-0.0898758212887859,
3.70099194019195E-15));
#48305=CARTESIAN_POINT('Ctrl Pts',(-2.62596008221826,-0.0763794055641211,
1.98967329662049E-15));
#48306=CARTESIAN_POINT('Ctrl Pts',(-2.6278400946394,-0.0628763941457671,
2.3037127760972E-15));
#48307=CARTESIAN_POINT('Ctrl Pts',(-2.64060982150931,0.028840961438971,
3.74500870588478E-15));
#48308=CARTESIAN_POINT('Ctrl Pts',(-2.64837710874139,0.12089024961922,5.0717148189266E-15));
#48309=CARTESIAN_POINT('Ctrl Pts',(-2.65101366112899,0.212875307175297,
4.08006961549745E-15));
#48310=CARTESIAN_POINT('Ctrl Pts',(-2.65226659852155,0.25658827063111,2.79591952247038E-15));
#48311=CARTESIAN_POINT('Ctrl Pts',(-2.65236023741466,0.300287183231581,
5.31362288609455E-15));
#48312=CARTESIAN_POINT('Ctrl Pts',(-2.6512772014093,0.343931535522,4.69069227904129E-15));
#48313=CARTESIAN_POINT('Ctrl Pts',(-2.64905271560999,0.433574207982051,
3.47166984399289E-15));
#48314=CARTESIAN_POINT('Ctrl Pts',(-2.64186793473848,0.522986312811907,
3.91533376087034E-15));
#48315=CARTESIAN_POINT('Ctrl Pts',(-2.62997259694039,0.611899469403195,
3.21964677141295E-15));
#48316=CARTESIAN_POINT('Ctrl Pts',(-2.61807725914231,0.700812625994483,
2.52395978195556E-15));
#48317=CARTESIAN_POINT('Ctrl Pts',(-2.60147108990245,0.789227566327091,
1.47008262914315E-15));
#48318=CARTESIAN_POINT('Ctrl Pts',(-2.58035146554208,0.876878238745712,
1.99840144432528E-15));
#48319=CARTESIAN_POINT('Ctrl Pts',(-2.576583244582,0.892517110694274,2.02142778531884E-15));
#48320=CARTESIAN_POINT('Ctrl Pts',(-2.57267071394585,0.908133543901725,
1.70495023809932E-15));
#48321=CARTESIAN_POINT('Ctrl Pts',(-2.5686164135305,0.923719945234905,1.11022302462516E-15));
#48322=CARTESIAN_POINT('Ctrl Pts',(-2.56541851969971,0.936013966782737,
6.41122491330844E-16));
#48323=CARTESIAN_POINT('Ctrl Pts',(-2.5621335320974,0.948285079155145,1.04705546521683E-15));
#48324=CARTESIAN_POINT('Ctrl Pts',(-2.55876298044222,0.960529869852389,
1.19348975147204E-15));
#48325=CARTESIAN_POINT('Ctrl Pts',(-2.53423311716393,1.04964378128372,2.52665339019896E-15));
#48326=CARTESIAN_POINT('Ctrl Pts',(-2.50516230366703,1.13741448707249,-6.39640594898038E-16));
#48327=CARTESIAN_POINT('Ctrl Pts',(-2.47183958755925,1.22356204886004,-3.60822483003176E-16));
#48328=CARTESIAN_POINT('Ctrl Pts',(-2.43793696028359,1.31120882616785,-7.71521334824393E-17));
#48329=CARTESIAN_POINT('Ctrl Pts',(-2.39963296981527,1.39717624648555,1.01309199915213E-15));
#48330=CARTESIAN_POINT('Ctrl Pts',(-2.35717721896034,1.48117223771656,4.16333634234434E-16));
#48331=CARTESIAN_POINT('Ctrl Pts',(-2.31422125531256,1.56615786800741,-1.87455725598068E-16));
#48332=CARTESIAN_POINT('Ctrl Pts',(-2.2670148596246,1.64912621348914,-1.4666715423013E-16));
#48333=CARTESIAN_POINT('Ctrl Pts',(-2.2157644123274,1.72976499945915,-9.99200722162641E-16));
#48334=CARTESIAN_POINT('Ctrl Pts',(-2.18483496065362,1.77843020269588,-1.5137015154285E-15));
#48335=CARTESIAN_POINT('Ctrl Pts',(-2.15243164629588,1.82624671746825,-1.21876760202498E-15));
#48336=CARTESIAN_POINT('Ctrl Pts',(-2.11859145320912,1.87314213253736,-2.38697950294409E-15));
#48337=CARTESIAN_POINT('Ctrl Pts',(-2.10923966749503,1.88610174750099,-2.64989400742177E-15));
#48338=CARTESIAN_POINT('Ctrl Pts',(-2.09977706809611,1.89899226435558,1.01111077252232E-15));
#48339=CARTESIAN_POINT('Ctrl Pts',(-2.0902160744712,1.91179680016256,6.10622663543836E-16));
#48340=CARTESIAN_POINT('Ctrl Pts',(-2.0314089911467,1.99055403331987,-9.7705151409358E-16));
#48341=CARTESIAN_POINT('Ctrl Pts',(-1.96879105165622,2.06618994281066,-2.55502889276557E-15));
#48342=CARTESIAN_POINT('Ctrl Pts',(-1.90263522084903,2.13839704217646,-1.72084568816899E-15));
#48343=CARTESIAN_POINT('Ctrl Pts',(-1.83630675568986,2.21079256674463,-1.02855259101591E-15));
#48344=CARTESIAN_POINT('Ctrl Pts',(-1.76642150904308,2.27974226115181,4.77271459200463E-16));
#48345=CARTESIAN_POINT('Ctrl Pts',(-1.69320457635212,2.34492041918575,1.11022302462516E-16));
#48346=CARTESIAN_POINT('Ctrl Pts',(-1.62138195171819,2.40885735572148,9.39521111622811E-16));
#48347=CARTESIAN_POINT('Ctrl Pts',(-1.54635279516223,2.46916580376612,5.81652154789426E-16));
#48348=CARTESIAN_POINT('Ctrl Pts',(-1.46828869933216,2.52551090352265,-7.7715611723761E-16));
#48349=CARTESIAN_POINT('Ctrl Pts',(-1.4101637796635,2.56746430556038,-8.9644473153275E-16));
#48350=CARTESIAN_POINT('Ctrl Pts',(-1.35035542783317,2.60721994909749,-2.27967887895237E-16));
#48351=CARTESIAN_POINT('Ctrl Pts',(-1.28892185405326,2.64462557919715,5.55111512312578E-17));
#48352=CARTESIAN_POINT('Origin',(-1.44337567297407,-2.5,-6.));
#48353=CARTESIAN_POINT('',(-1.44337567297407,-2.5,-6.));
#48354=CARTESIAN_POINT('',(1.44337567297406,-2.5,-6.));
#48355=CARTESIAN_POINT('',(-0.721687836487033,-2.5,-6.));
#48356=CARTESIAN_POINT('',(-1.44337567297407,-2.5,-3.));
#48357=CARTESIAN_POINT('',(-1.44337567297407,-2.5,-6.));
#48358=CARTESIAN_POINT('',(1.44337567297406,-2.5,-3.));
#48359=CARTESIAN_POINT('',(-1.44337567297407,-2.5,-3.));
#48360=CARTESIAN_POINT('',(1.44337567297406,-2.5,-6.));
#48361=CARTESIAN_POINT('Origin',(-2.88675134594813,3.53525079574969E-16,
-6.));
#48362=CARTESIAN_POINT('',(-2.88675134594813,3.53525079574969E-16,-6.));
#48363=CARTESIAN_POINT('',(-2.52590742770461,-0.625,-6.));
#48364=CARTESIAN_POINT('',(-2.88675134594813,5.55111512312578E-16,-3.));
#48365=CARTESIAN_POINT('',(-2.88675134594813,3.53525079574969E-16,-6.));
#48366=CARTESIAN_POINT('',(-2.88675134594813,3.53525079574969E-16,-3.));
#48367=CARTESIAN_POINT('Origin',(-1.44337567297406,2.5,-6.));
#48368=CARTESIAN_POINT('',(-1.44337567297406,2.5,-6.));
#48369=CARTESIAN_POINT('',(-1.80421959121758,1.875,-6.));
#48370=CARTESIAN_POINT('',(-1.44337567297406,2.5,-3.));
#48371=CARTESIAN_POINT('',(-1.44337567297406,2.5,-6.));
#48372=CARTESIAN_POINT('',(-1.44337567297406,2.5,-3.));
#48373=CARTESIAN_POINT('Origin',(1.44337567297406,2.5,-6.));
#48374=CARTESIAN_POINT('',(1.44337567297406,2.5,-6.));
#48375=CARTESIAN_POINT('',(0.721687836487033,2.5,-6.));
#48376=CARTESIAN_POINT('',(1.44337567297406,2.5,-3.));
#48377=CARTESIAN_POINT('',(1.44337567297406,2.5,-6.));
#48378=CARTESIAN_POINT('',(1.44337567297406,2.5,-3.));
#48379=CARTESIAN_POINT('Origin',(2.88675134594813,0.,-6.));
#48380=CARTESIAN_POINT('',(2.88675134594813,0.,-6.));
#48381=CARTESIAN_POINT('',(2.52590742770461,0.625,-6.));
#48382=CARTESIAN_POINT('',(2.88675134594813,0.,-3.));
#48383=CARTESIAN_POINT('',(2.88675134594813,0.,-6.));
#48384=CARTESIAN_POINT('',(2.88675134594813,0.,-3.));
#48385=CARTESIAN_POINT('Origin',(1.44337567297406,-2.5,-6.));
#48386=CARTESIAN_POINT('',(1.80421959121758,-1.875,-6.));
#48387=CARTESIAN_POINT('',(1.44337567297406,-2.5,-3.));
#48388=CARTESIAN_POINT('Origin',(0.,0.,-3.));
#48389=CARTESIAN_POINT('Origin',(0.,0.,0.));
#48390=CARTESIAN_POINT('',(-5.,-6.12323399573677E-16,0.));
#48391=CARTESIAN_POINT('Origin',(0.,0.,0.));
#48392=CARTESIAN_POINT('Origin',(0.,0.,-6.));
#48393=CARTESIAN_POINT('',(-5.,-6.12323399573677E-16,-6.));
#48394=CARTESIAN_POINT('',(-5.,-6.12323399573677E-16,-6.));
#48395=CARTESIAN_POINT('Origin',(0.,0.,-6.));
#48396=CARTESIAN_POINT('Origin',(0.,0.,-6.));
#48397=CARTESIAN_POINT('Origin',(0.,0.,12.));
#94384=UNCERTAINTY_MEASURE_WITH_UNIT(LENGTH_MEASURE(0.01),#94413,
'DISTANCE_ACCURACY_VALUE',
'Maximum model space distance between geometric entities at asserted c
onnectivities');
#94394=UNCERTAINTY_MEASURE_WITH_UNIT(LENGTH_MEASURE(0.01),#94413,
'DISTANCE_ACCURACY_VALUE',
'Maximum model space distance between geometric entities at asserted c
onnectivities');
#94402=(
GEOMETRIC_REPRESENTATION_CONTEXT(3)
GLOBAL_UNCERTAINTY_ASSIGNED_CONTEXT((#94384))
GLOBAL_UNIT_ASSIGNED_CONTEXT((#94413,#94415,#94416))
REPRESENTATION_CONTEXT('','3D')
);
#94412=(
GEOMETRIC_REPRESENTATION_CONTEXT(3)
GLOBAL_UNCERTAINTY_ASSIGNED_CONTEXT((#94394))
GLOBAL_UNIT_ASSIGNED_CONTEXT((#94413,#94415,#94416))
REPRESENTATION_CONTEXT('','3D')
);
#94413=(
LENGTH_UNIT()
NAMED_UNIT(*)
SI_UNIT(.MILLI.,.METRE.)
);
#94415=(
NAMED_UNIT(*)
PLANE_ANGLE_UNIT()
SI_UNIT($,.RADIAN.)
);
#94416=(
NAMED_UNIT(*)
SI_UNIT($,.STERADIAN.)
SOLID_ANGLE_UNIT()
);
#94424=SHAPE_DEFINITION_REPRESENTATION(#94441,#94493);
#94441=PRODUCT_DEFINITION_SHAPE('',$,#94511);
#94493=SHAPE_REPRESENTATION('',(#8614),#94402);
#94503=PRODUCT_DEFINITION_CONTEXT('part definition',#94556,'design');
#94511=PRODUCT_DEFINITION('Socket head cap screw M6x12',
'Socket head cap screw M6x12',#94528,#94503);
#94528=PRODUCT_DEFINITION_FORMATION('',$,#94565);
#94556=APPLICATION_CONTEXT(
'Core Data for Automotive Mechanical Design Process');
#94557=PRODUCT_CONTEXT('part definition',#94556,'mechanical');
#94565=PRODUCT('Socket head cap screw M6x12',
'Socket head cap screw M6x12',$,(#94557));
#94578=PRESENTATION_STYLE_ASSIGNMENT((#94585));
#94585=SURFACE_STYLE_USAGE(.BOTH.,#94592);
#94592=SURFACE_SIDE_STYLE('',(#94599));
#94599=SURFACE_STYLE_FILL_AREA(#94606);
#94606=FILL_AREA_STYLE('Opaque(64,72,82)',(#94613));
#94613=FILL_AREA_STYLE_COLOUR('Opaque(64,72,82)',#94620);
#94620=COLOUR_RGB('Opaque(64,72,82)',0.250980392156863,0.282352941176471,
0.32156862745098);
ENDSEC;
END-ISO-10303-21;
